ISO-10303-21;
HEADER;
FILE_DESCRIPTION((''),'2;1');
FILE_NAME('Pan_Head_Screw.step','2026-10-09T10:33:02-07:00',(''),(''),'','','');
FILE_SCHEMA (('AUTOMOTIVE_DESIGN { 1 0 10303 214 3 1 1 }'));
ENDSEC;
DATA;
#10=MECHANICAL_DESIGN_GEOMETRIC_PRESENTATION_REPRESENTATION('',(#843),#86330);
#83=SPHERICAL_SURFACE('',#35563,0.1) ;
#84=SPHERICAL_SURFACE('',#35577,0.1) ;
#85=SPHERICAL_SURFACE('',#35579,0.1) ;
#86=SPHERICAL_SURFACE('',#35598,0.1) ;
#87=SPHERICAL_SURFACE('',#35605,0.1) ;
#88=SPHERICAL_SURFACE('',#35624,0.1) ;
#89=SPHERICAL_SURFACE('',#35641,0.1) ;
#90=SPHERICAL_SURFACE('',#35652,0.1) ;
#91=SPHERICAL_SURFACE('',#35677,0.1) ;
#92=SPHERICAL_SURFACE('',#35686,0.1) ;
#93=SPHERICAL_SURFACE('',#35710,0.1) ;
#94=SPHERICAL_SURFACE('',#35713,0.1) ;
#95=SPHERICAL_SURFACE('',#35719,0.1) ;
#96=SPHERICAL_SURFACE('',#35730,0.1) ;
#97=SPHERICAL_SURFACE('',#35737,0.1) ;
#98=SPHERICAL_SURFACE('',#35749,0.1) ;
#99=SPHERICAL_SURFACE('',#35772,0.1) ;
#100=SPHERICAL_SURFACE('',#35781,0.1) ;
#101=SPHERICAL_SURFACE('',#35806,0.1) ;
#102=SPHERICAL_SURFACE('',#35809,0.1) ;
#103=SPHERICAL_SURFACE('',#35816,0.1) ;
#104=SPHERICAL_SURFACE('',#35828,0.1) ;
#105=SPHERICAL_SURFACE('',#35835,0.1) ;
#106=SPHERICAL_SURFACE('',#35845,0.1) ;
#107=SPHERICAL_SURFACE('',#35878,5.38826958762885) ;
#108=SPHERICAL_SURFACE('',#35892,5.38826958762885) ;
#150=ELLIPSE('',#35501,0.0961348525953907,0.0789674582653757) ;
#151=ELLIPSE('',#35502,0.181135134462203,0.157351167100413) ;
#152=ELLIPSE('',#35506,0.179452491476591,0.152051329111869) ;
#153=ELLIPSE('',#35509,0.17945249124005,0.152051328979059) ;
#154=ELLIPSE('',#35511,0.173242568385421,0.148461954688806) ;
#155=ELLIPSE('',#35514,0.173242568255686,0.148461954613973) ;
#156=ELLIPSE('',#35520,0.0961348009085155,0.0789673736338199) ;
#157=ELLIPSE('',#35526,0.18113516065876,0.157351212612531) ;
#158=ELLIPSE('',#35537,0.0961347917913063,0.0789673586439759) ;
#159=ELLIPSE('',#35538,0.181135145593687,0.157351186447307) ;
#160=ELLIPSE('',#35544,0.0961348054140246,0.0789673810185351) ;
#161=ELLIPSE('',#35550,0.18113516065876,0.157351212612531) ;
#162=ELLIPSE('',#35557,0.301518169878764,0.257262372521227) ;
#163=ELLIPSE('',#35559,0.107622698330153,0.1) ;
#164=ELLIPSE('',#35560,0.107622698330153,0.1) ;
#165=ELLIPSE('',#35570,0.170365066914478,0.147415894551294) ;
#166=ELLIPSE('',#35575,0.0854022854049574,0.0779713270951896) ;
#167=ELLIPSE('',#35585,0.085402285745328,0.0779713277049084) ;
#168=ELLIPSE('',#35586,0.170365066783361,0.147415894323676) ;
#169=ELLIPSE('',#35593,0.107622698330153,0.1) ;
#170=ELLIPSE('',#35595,0.107622698330153,0.1) ;
#171=ELLIPSE('',#35601,0.217305352531138,0.2) ;
#172=ELLIPSE('',#35604,0.129857287089145,0.1) ;
#173=ELLIPSE('',#35610,0.0854022855711418,0.0779713273931643) ;
#174=ELLIPSE('',#35612,0.170365066781204,0.147415894320068) ;
#175=ELLIPSE('',#35615,0.0854022856622134,0.0779713275582352) ;
#176=ELLIPSE('',#35623,0.107622698330153,0.1) ;
#177=ELLIPSE('',#35629,0.17036506667425,0.147415894132821) ;
#178=ELLIPSE('',#35636,0.107622698330153,0.1) ;
#179=ELLIPSE('',#35638,0.107622698330153,0.1) ;
#180=ELLIPSE('',#35644,0.217305352531139,0.2) ;
#181=ELLIPSE('',#35647,0.129857287089145,0.1) ;
#182=ELLIPSE('',#35649,0.107622698330153,0.1) ;
#183=ELLIPSE('',#35658,0.129857287089145,0.1) ;
#184=ELLIPSE('',#35659,1.80295526461806,1.74359985651392) ;
#185=ELLIPSE('',#35663,1.44368220806618,1.24694668207658) ;
#186=ELLIPSE('',#35667,0.325215841526545,0.1384674618534) ;
#187=ELLIPSE('',#35668,0.179960384676197,0.0842561394706778) ;
#188=ELLIPSE('',#35669,0.143757456365121,0.0572377473682424) ;
#189=ELLIPSE('',#35670,0.178426613998649,0.0895872224985392) ;
#190=ELLIPSE('',#35671,0.180280902012032,0.0868949646061415) ;
#191=ELLIPSE('',#35672,0.318318659412206,0.139006967439323) ;
#192=ELLIPSE('',#35674,0.181500403086132,0.1649478028119) ;
#193=ELLIPSE('',#35675,0.0992598259423044,0.0779564848832496) ;
#194=ELLIPSE('',#35691,0.0992598257926529,0.0779564846898224) ;
#195=ELLIPSE('',#35693,0.181500403012281,0.164947802681056) ;
#196=ELLIPSE('',#35698,0.107622698330153,0.1) ;
#197=ELLIPSE('',#35701,0.129857287089145,0.1) ;
#198=ELLIPSE('',#35705,0.21730535253114,0.2) ;
#199=ELLIPSE('',#35707,0.13123115574696,0.0999999999999999) ;
#200=ELLIPSE('',#35716,0.107622698330153,0.1) ;
#201=ELLIPSE('',#35727,0.131231155746957,0.1) ;
#202=ELLIPSE('',#35736,0.129857287089145,0.1) ;
#203=ELLIPSE('',#35746,0.301519549160911,0.257265094389927) ;
#204=ELLIPSE('',#35755,0.107622698330153,0.1) ;
#205=ELLIPSE('',#35756,0.107622698330153,0.1) ;
#206=ELLIPSE('',#35760,0.131231155746959,0.1) ;
#207=ELLIPSE('',#35762,0.325215841518844,0.138467461839436) ;
#208=ELLIPSE('',#35763,0.179960384640109,0.084256139441645) ;
#209=ELLIPSE('',#35764,0.143757456333512,0.0572377473425655) ;
#210=ELLIPSE('',#35765,0.178426614167312,0.0895872226348807) ;
#211=ELLIPSE('',#35766,0.180280902020227,0.086894964614583) ;
#212=ELLIPSE('',#35767,0.318318659448403,0.139006967461565) ;
#213=ELLIPSE('',#35769,0.181500403028042,0.164947802708139) ;
#214=ELLIPSE('',#35770,0.0992598259984378,0.0779564849579177) ;
#215=ELLIPSE('',#35786,0.0992598258762505,0.0779564847990513) ;
#216=ELLIPSE('',#35788,0.181500403117952,0.164947802867497) ;
#217=ELLIPSE('',#35793,0.107622698330153,0.1) ;
#218=ELLIPSE('',#35798,0.129857287089145,0.1) ;
#219=ELLIPSE('',#35799,0.129857287089145,0.1) ;
#220=ELLIPSE('',#35801,0.217305352531139,0.2) ;
#221=ELLIPSE('',#35803,0.131231155746959,0.1) ;
#222=ELLIPSE('',#35813,0.107622698330153,0.1) ;
#223=ELLIPSE('',#35834,0.129857287089145,0.1) ;
#224=ELLIPSE('',#35851,0.107622698330153,0.1) ;
#225=ELLIPSE('',#35852,0.107622698330153,0.1) ;
#410=TOROIDAL_SURFACE('',#35507,2.985516,0.443484) ;
#411=TOROIDAL_SURFACE('',#35518,3.2727760605723,0.1) ;
#412=TOROIDAL_SURFACE('',#35542,3.2727760605723,0.1) ;
#413=TOROIDAL_SURFACE('',#35566,5.28650897109211,0.1) ;
#414=TOROIDAL_SURFACE('',#35587,5.28650897109211,0.1) ;
#415=TOROIDAL_SURFACE('',#35613,2.31499663839041,0.1) ;
#416=TOROIDAL_SURFACE('',#35619,1.74337006393707,0.1) ;
#417=TOROIDAL_SURFACE('',#35630,5.28650897109211,0.1) ;
#418=TOROIDAL_SURFACE('',#35661,1.8526,0.1) ;
#419=TOROIDAL_SURFACE('',#35683,1.99389469750719,0.1) ;
#420=TOROIDAL_SURFACE('',#35739,5.25939963812285,0.1) ;
#421=TOROIDAL_SURFACE('',#35741,5.21754264299203,0.1) ;
#422=TOROIDAL_SURFACE('',#35778,1.99389469750719,0.1) ;
#423=TOROIDAL_SURFACE('',#35837,5.25939963812284,0.1) ;
#424=TOROIDAL_SURFACE('',#35839,5.21754264299203,0.1) ;
#425=TOROIDAL_SURFACE('',#35855,1.74337006393707,0.1) ;
#426=TOROIDAL_SURFACE('',#35858,1.74337006393707,0.1) ;
#427=TOROIDAL_SURFACE('',#35861,1.74337006393707,0.1) ;
#428=TOROIDAL_SURFACE('',#35868,5.21754264299203,0.1) ;
#429=TOROIDAL_SURFACE('',#35871,5.25939963812284,0.1) ;
#430=TOROIDAL_SURFACE('',#35873,2.31499663839041,0.1) ;
#431=TOROIDAL_SURFACE('',#35880,2.985516,0.443484) ;
#432=TOROIDAL_SURFACE('',#35884,5.21754264299203,0.1) ;
#433=TOROIDAL_SURFACE('',#35886,5.25939963812284,0.1) ;
#434=TOROIDAL_SURFACE('',#35888,5.28650897109211,0.1) ;
#435=TOROIDAL_SURFACE('',#35894,2.985516,0.443484) ;
#744=(
BOUNDED_SURFACE()
B_SPLINE_SURFACE(1,2,((#76706,#76707,#76708,#76709,#76710,#76711,#76712,
#76713,#76714,#76715,#76716,#76717,#76718,#76719,#76720,#76721,#76722,#76723,
#76724,#76725,#76726,#76727,#76728,#76729,#76730,#76731,#76732,#76733,#76734,
#76735,#76736,#76737,#76738,#76739,#76740,#76741,#76742,#76743,#76744,#76745,
#76746,#76747,#76748,#76749,#76750,#76751,#76752,#76753,#76754,#76755,#76756,
#76757,#76758,#76759,#76760,#76761,#76762,#76763,#76764,#76765,#76766,#76767,
#76768,#76769,#76770,#76771,#76772,#76773,#76774,#76775,#76776,#76777,#76778,
#76779,#76780,#76781,#76782,#76783,#76784,#76785,#76786,#76787,#76788,#76789,
#76790,#76791,#76792,#76793,#76794,#76795,#76796,#76797,#76798,#76799,#76800,
#76801,#76802,#76803,#76804,#76805,#76806,#76807,#76808,#76809,#76810,#76811,
#76812,#76813,#76814,#76815,#76816,#76817,#76818,#76819,#76820,#76821,#76822,
#76823,#76824,#76825,#76826,#76827,#76828,#76829,#76830,#76831,#76832,#76833,
#76834,#76835,#76836,#76837,#76838,#76839,#76840,#76841,#76842,#76843,#76844,
#76845,#76846,#76847,#76848,#76849,#76850),(#76851,#76852,#76853,#76854,
#76855,#76856,#76857,#76858,#76859,#76860,#76861,#76862,#76863,#76864,#76865,
#76866,#76867,#76868,#76869,#76870,#76871,#76872,#76873,#76874,#76875,#76876,
#76877,#76878,#76879,#76880,#76881,#76882,#76883,#76884,#76885,#76886,#76887,
#76888,#76889,#76890,#76891,#76892,#76893,#76894,#76895,#76896,#76897,#76898,
#76899,#76900,#76901,#76902,#76903,#76904,#76905,#76906,#76907,#76908,#76909,
#76910,#76911,#76912,#76913,#76914,#76915,#76916,#76917,#76918,#76919,#76920,
#76921,#76922,#76923,#76924,#76925,#76926,#76927,#76928,#76929,#76930,#76931,
#76932,#76933,#76934,#76935,#76936,#76937,#76938,#76939,#76940,#76941,#76942,
#76943,#76944,#76945,#76946,#76947,#76948,#76949,#76950,#76951,#76952,#76953,
#76954,#76955,#76956,#76957,#76958,#76959,#76960,#76961,#76962,#76963,#76964,
#76965,#76966,#76967,#76968,#76969,#76970,#76971,#76972,#76973,#76974,#76975,
#76976,#76977,#76978,#76979,#76980,#76981,#76982,#76983,#76984,#76985,#76986,
#76987,#76988,#76989,#76990,#76991,#76992,#76993,#76994,#76995),(#76996,
#76997,#76998,#76999,#77000,#77001,#77002,#77003,#77004,#77005,#77006,#77007,
#77008,#77009,#77010,#77011,#77012,#77013,#77014,#77015,#77016,#77017,#77018,
#77019,#77020,#77021,#77022,#77023,#77024,#77025,#77026,#77027,#77028,#77029,
#77030,#77031,#77032,#77033,#77034,#77035,#77036,#77037,#77038,#77039,#77040,
#77041,#77042,#77043,#77044,#77045,#77046,#77047,#77048,#77049,#77050,#77051,
#77052,#77053,#77054,#77055,#77056,#77057,#77058,#77059,#77060,#77061,#77062,
#77063,#77064,#77065,#77066,#77067,#77068,#77069,#77070,#77071,#77072,#77073,
#77074,#77075,#77076,#77077,#77078,#77079,#77080,#77081,#77082,#77083,#77084,
#77085,#77086,#77087,#77088,#77089,#77090,#77091,#77092,#77093,#77094,#77095,
#77096,#77097,#77098,#77099,#77100,#77101,#77102,#77103,#77104,#77105,#77106,
#77107,#77108,#77109,#77110,#77111,#77112,#77113,#77114,#77115,#77116,#77117,
#77118,#77119,#77120,#77121,#77122,#77123,#77124,#77125,#77126,#77127,#77128,
#77129,#77130,#77131,#77132,#77133,#77134,#77135,#77136,#77137,#77138,#77139,
#77140),(#77141,#77142,#77143,#77144,#77145,#77146,#77147,#77148,#77149,
#77150,#77151,#77152,#77153,#77154,#77155,#77156,#77157,#77158,#77159,#77160,
#77161,#77162,#77163,#77164,#77165,#77166,#77167,#77168,#77169,#77170,#77171,
#77172,#77173,#77174,#77175,#77176,#77177,#77178,#77179,#77180,#77181,#77182,
#77183,#77184,#77185,#77186,#77187,#77188,#77189,#77190,#77191,#77192,#77193,
#77194,#77195,#77196,#77197,#77198,#77199,#77200,#77201,#77202,#77203,#77204,
#77205,#77206,#77207,#77208,#77209,#77210,#77211,#77212,#77213,#77214,#77215,
#77216,#77217,#77218,#77219,#77220,#77221,#77222,#77223,#77224,#77225,#77226,
#77227,#77228,#77229,#77230,#77231,#77232,#77233,#77234,#77235,#77236,#77237,
#77238,#77239,#77240,#77241,#77242,#77243,#77244,#77245,#77246,#77247,#77248,
#77249,#77250,#77251,#77252,#77253,#77254,#77255,#77256,#77257,#77258,#77259,
#77260,#77261,#77262,#77263,#77264,#77265,#77266,#77267,#77268,#77269,#77270,
#77271,#77272,#77273,#77274,#77275,#77276,#77277,#77278,#77279,#77280,#77281,
#77282,#77283,#77284,#77285)),.UNSPECIFIED.,.F.,.F.,.F.)
B_SPLINE_SURFACE_WITH_KNOTS((2,1,1,2),(3,2,2,2,2,2,2,2,2,2,2,2,2,2,2,2,
2,2,2,2,2,2,2,2,2,2,2,2,2,2,2,2,2,2,2,2,2,2,2,2,2,2,2,2,2,2,2,2,2,2,2,2,
2,2,2,2,2,2,2,2,2,2,2,2,2,2,2,2,2,2,2,2,3),(-5.32860868657006,0.,1.,2.58924025826637),
(0.,0.0138888888888889,0.0277777777777778,0.0416666666666667,0.0555555555555556,
0.0694444444444444,0.0833333333333333,0.0972222222222222,0.111111111111111,
0.125,0.138888888888889,0.152777777777778,0.166666666666667,0.180555555555556,
0.194444444444444,0.208333333333333,0.222222222222222,0.236111111111111,
0.25,0.263888888888889,0.277777777777778,0.291666666666667,0.305555555555556,
0.319444444444444,0.333333333333333,0.347222222222222,0.361111111111111,
0.375,0.388888888888889,0.402777777777778,0.416666666666667,0.430555555555556,
0.444444444444444,0.458333333333333,0.472222222222222,0.486111111111111,
0.5,0.513888888888889,0.527777777777778,0.541666666666667,0.555555555555556,
0.569444444444444,0.583333333333333,0.597222222222222,0.611111111111111,
0.625,0.638888888888889,0.652777777777778,0.666666666666667,0.680555555555556,
0.694444444444444,0.708333333333333,0.722222222222222,0.736111111111111,
0.75,0.763888888888889,0.777777777777778,0.791666666666667,0.805555555555556,
0.819444444444444,0.833333333333333,0.847222222222222,0.861111111111111,
0.875,0.888888888888889,0.902777777777778,0.916666666666667,0.930555555555556,
0.944444444444444,0.958333333333333,0.972222222222222,0.986111111111111,
1.),.UNSPECIFIED.)
GEOMETRIC_REPRESENTATION_ITEM()
RATIONAL_B_SPLINE_SURFACE(((1.,0.923879532511287,1.,0.923879532511287,1.,
0.923879532511287,1.,0.923879532511287,1.,0.923879532511287,1.,0.923879532511287,
1.,0.923879532511287,1.,0.923879532511287,1.,0.923879532511287,1.,0.923879532511287,
1.,0.923879532511287,1.,0.923879532511287,1.,0.923879532511287,1.,0.923879532511287,
1.,0.923879532511287,1.,0.923879532511287,1.,0.923879532511287,1.,0.923879532511287,
1.,0.923879532511287,1.,0.923879532511287,1.,0.923879532511287,1.,0.923879532511287,
1.,0.923879532511287,1.,0.923879532511287,1.,0.923879532511287,1.,0.923879532511287,
1.,0.923879532511287,1.,0.923879532511287,1.,0.923879532511287,1.,0.923879532511287,
1.,0.923879532511287,1.,0.923879532511287,1.,0.923879532511287,1.,0.923879532511287,
1.,0.923879532511287,1.,0.923879532511287,1.,0.923879532511287,1.,0.923879532511287,
1.,0.923879532511287,1.,0.923879532511287,1.,0.923879532511287,1.,0.923879532511287,
1.,0.923879532511287,1.,0.923879532511287,1.,0.923879532511287,1.,0.923879532511287,
1.,0.923879532511287,1.,0.923879532511287,1.,0.923879532511287,1.,0.923879532511287,
1.,0.923879532511287,1.,0.923879532511287,1.,0.923879532511287,1.,0.923879532511287,
1.,0.923879532511287,1.,0.923879532511287,1.,0.923879532511287,1.,0.923879532511287,
1.,0.923879532511287,1.,0.923879532511287,1.,0.923879532511287,1.,0.923879532511287,
1.,0.923879532511287,1.,0.923879532511287,1.,0.923879532511287,1.,0.923879532511287,
1.,0.923879532511287,1.,0.923879532511287,1.,0.923879532511287,1.,0.923879532511287,
1.,0.923879532511287,1.,0.923879532511287,1.),(1.,0.923879532511287,1.,
0.923879532511287,1.,0.923879532511287,1.,0.923879532511287,1.,0.923879532511287,
1.,0.923879532511287,1.,0.923879532511287,1.,0.923879532511287,1.,0.923879532511287,
1.,0.923879532511287,1.,0.923879532511287,1.,0.923879532511287,1.,0.923879532511287,
1.,0.923879532511287,1.,0.923879532511287,1.,0.923879532511287,1.,0.923879532511287,
1.,0.923879532511287,1.,0.923879532511287,1.,0.923879532511287,1.,0.923879532511287,
1.,0.923879532511287,1.,0.923879532511287,1.,0.923879532511287,1.,0.923879532511287,
1.,0.923879532511287,1.,0.923879532511287,1.,0.923879532511287,1.,0.923879532511287,
1.,0.923879532511287,1.,0.923879532511287,1.,0.923879532511287,1.,0.923879532511287,
1.,0.923879532511287,1.,0.923879532511287,1.,0.923879532511287,1.,0.923879532511287,
1.,0.923879532511287,1.,0.923879532511287,1.,0.923879532511287,1.,0.923879532511287,
1.,0.923879532511287,1.,0.923879532511287,1.,0.923879532511287,1.,0.923879532511287,
1.,0.923879532511287,1.,0.923879532511287,1.,0.923879532511287,1.,0.923879532511287,
1.,0.923879532511287,1.,0.923879532511287,1.,0.923879532511287,1.,0.923879532511287,
1.,0.923879532511287,1.,0.923879532511287,1.,0.923879532511287,1.,0.923879532511287,
1.,0.923879532511287,1.,0.923879532511287,1.,0.923879532511287,1.,0.923879532511287,
1.,0.923879532511287,1.,0.923879532511287,1.,0.923879532511287,1.,0.923879532511287,
1.,0.923879532511287,1.,0.923879532511287,1.,0.923879532511287,1.,0.923879532511287,
1.,0.923879532511287,1.,0.923879532511287,1.,0.923879532511287,1.),(1.,
0.923879532511287,1.,0.923879532511287,1.,0.923879532511287,1.,0.923879532511287,
1.,0.923879532511287,1.,0.923879532511287,1.,0.923879532511287,1.,0.923879532511287,
1.,0.923879532511287,1.,0.923879532511287,1.,0.923879532511287,1.,0.923879532511287,
1.,0.923879532511287,1.,0.923879532511287,1.,0.923879532511287,1.,0.923879532511287,
1.,0.923879532511287,1.,0.923879532511287,1.,0.923879532511287,1.,0.923879532511287,
1.,0.923879532511287,1.,0.923879532511287,1.,0.923879532511287,1.,0.923879532511287,
1.,0.923879532511287,1.,0.923879532511287,1.,0.923879532511287,1.,0.923879532511287,
1.,0.923879532511287,1.,0.923879532511287,1.,0.923879532511287,1.,0.923879532511287,
1.,0.923879532511287,1.,0.923879532511287,1.,0.923879532511287,1.,0.923879532511287,
1.,0.923879532511287,1.,0.923879532511287,1.,0.923879532511287,1.,0.923879532511287,
1.,0.923879532511287,1.,0.923879532511287,1.,0.923879532511287,1.,0.923879532511287,
1.,0.923879532511287,1.,0.923879532511287,1.,0.923879532511287,1.,0.923879532511287,
1.,0.923879532511287,1.,0.923879532511287,1.,0.923879532511287,1.,0.923879532511287,
1.,0.923879532511287,1.,0.923879532511287,1.,0.923879532511287,1.,0.923879532511287,
1.,0.923879532511287,1.,0.923879532511287,1.,0.923879532511287,1.,0.923879532511287,
1.,0.923879532511287,1.,0.923879532511287,1.,0.923879532511287,1.,0.923879532511287,
1.,0.923879532511287,1.,0.923879532511287,1.,0.923879532511287,1.,0.923879532511287,
1.,0.923879532511287,1.,0.923879532511287,1.,0.923879532511287,1.,0.923879532511287,
1.),(1.,0.923879532511287,1.,0.923879532511287,1.,0.923879532511287,1.,
0.923879532511287,1.,0.923879532511287,1.,0.923879532511287,1.,0.923879532511287,
1.,0.923879532511287,1.,0.923879532511287,1.,0.923879532511287,1.,0.923879532511287,
1.,0.923879532511287,1.,0.923879532511287,1.,0.923879532511287,1.,0.923879532511287,
1.,0.923879532511287,1.,0.923879532511287,1.,0.923879532511287,1.,0.923879532511287,
1.,0.923879532511287,1.,0.923879532511287,1.,0.923879532511287,1.,0.923879532511287,
1.,0.923879532511287,1.,0.923879532511287,1.,0.923879532511287,1.,0.923879532511287,
1.,0.923879532511287,1.,0.923879532511287,1.,0.923879532511287,1.,0.923879532511287,
1.,0.923879532511287,1.,0.923879532511287,1.,0.923879532511287,1.,0.923879532511287,
1.,0.923879532511287,1.,0.923879532511287,1.,0.923879532511287,1.,0.923879532511287,
1.,0.923879532511287,1.,0.923879532511287,1.,0.923879532511287,1.,0.923879532511287,
1.,0.923879532511287,1.,0.923879532511287,1.,0.923879532511287,1.,0.923879532511287,
1.,0.923879532511287,1.,0.923879532511287,1.,0.923879532511287,1.,0.923879532511287,
1.,0.923879532511287,1.,0.923879532511287,1.,0.923879532511287,1.,0.923879532511287,
1.,0.923879532511287,1.,0.923879532511287,1.,0.923879532511287,1.,0.923879532511287,
1.,0.923879532511287,1.,0.923879532511287,1.,0.923879532511287,1.,0.923879532511287,
1.,0.923879532511287,1.,0.923879532511287,1.,0.923879532511287,1.,0.923879532511287,
1.,0.923879532511287,1.,0.923879532511287,1.,0.923879532511287,1.,0.923879532511287,
1.,0.923879532511287,1.)))
REPRESENTATION_ITEM('')
SURFACE()
) ;
#745=(
BOUNDED_SURFACE()
B_SPLINE_SURFACE(1,2,((#78487,#78488,#78489,#78490,#78491,#78492,#78493,
#78494,#78495,#78496,#78497,#78498,#78499,#78500,#78501,#78502,#78503,#78504,
#78505,#78506,#78507,#78508,#78509,#78510,#78511,#78512,#78513,#78514,#78515,
#78516,#78517,#78518,#78519,#78520,#78521,#78522,#78523,#78524,#78525,#78526,
#78527,#78528,#78529,#78530,#78531,#78532,#78533,#78534,#78535,#78536,#78537,
#78538,#78539,#78540,#78541,#78542,#78543,#78544,#78545,#78546,#78547,#78548,
#78549,#78550,#78551,#78552,#78553,#78554,#78555,#78556,#78557,#78558,#78559,
#78560,#78561,#78562,#78563,#78564,#78565,#78566,#78567,#78568,#78569,#78570,
#78571,#78572,#78573,#78574,#78575,#78576,#78577,#78578,#78579,#78580,#78581,
#78582,#78583,#78584,#78585,#78586,#78587,#78588,#78589,#78590,#78591,#78592,
#78593,#78594,#78595,#78596,#78597,#78598,#78599,#78600,#78601,#78602,#78603,
#78604,#78605,#78606,#78607,#78608,#78609,#78610,#78611,#78612,#78613,#78614,
#78615,#78616,#78617,#78618,#78619,#78620,#78621,#78622,#78623,#78624,#78625,
#78626,#78627,#78628,#78629,#78630,#78631),(#78632,#78633,#78634,#78635,
#78636,#78637,#78638,#78639,#78640,#78641,#78642,#78643,#78644,#78645,#78646,
#78647,#78648,#78649,#78650,#78651,#78652,#78653,#78654,#78655,#78656,#78657,
#78658,#78659,#78660,#78661,#78662,#78663,#78664,#78665,#78666,#78667,#78668,
#78669,#78670,#78671,#78672,#78673,#78674,#78675,#78676,#78677,#78678,#78679,
#78680,#78681,#78682,#78683,#78684,#78685,#78686,#78687,#78688,#78689,#78690,
#78691,#78692,#78693,#78694,#78695,#78696,#78697,#78698,#78699,#78700,#78701,
#78702,#78703,#78704,#78705,#78706,#78707,#78708,#78709,#78710,#78711,#78712,
#78713,#78714,#78715,#78716,#78717,#78718,#78719,#78720,#78721,#78722,#78723,
#78724,#78725,#78726,#78727,#78728,#78729,#78730,#78731,#78732,#78733,#78734,
#78735,#78736,#78737,#78738,#78739,#78740,#78741,#78742,#78743,#78744,#78745,
#78746,#78747,#78748,#78749,#78750,#78751,#78752,#78753,#78754,#78755,#78756,
#78757,#78758,#78759,#78760,#78761,#78762,#78763,#78764,#78765,#78766,#78767,
#78768,#78769,#78770,#78771,#78772,#78773,#78774,#78775,#78776)),
 .UNSPECIFIED.,.F.,.F.,.F.)
B_SPLINE_SURFACE_WITH_KNOTS((2,2),(3,2,2,2,2,2,2,2,2,2,2,2,2,2,2,2,2,2,
2,2,2,2,2,2,2,2,2,2,2,2,2,2,2,2,2,2,2,2,2,2,2,2,2,2,2,2,2,2,2,2,2,2,2,2,
2,2,2,2,2,2,2,2,2,2,2,2,2,2,2,2,2,2,3),(0.,1.00005636984077),(0.,0.0138888888888889,
0.0277777777777778,0.0416666666666667,0.0555555555555556,0.0694444444444444,
0.0833333333333333,0.0972222222222222,0.111111111111111,0.125,0.138888888888889,
0.152777777777778,0.166666666666667,0.180555555555556,0.194444444444444,
0.208333333333333,0.222222222222222,0.236111111111111,0.25,0.263888888888889,
0.277777777777778,0.291666666666667,0.305555555555556,0.319444444444444,
0.333333333333333,0.347222222222222,0.361111111111111,0.375,0.388888888888889,
0.402777777777778,0.416666666666667,0.430555555555556,0.444444444444444,
0.458333333333333,0.472222222222222,0.486111111111111,0.5,0.513888888888889,
0.527777777777778,0.541666666666667,0.555555555555556,0.569444444444444,
0.583333333333333,0.597222222222222,0.611111111111111,0.625,0.638888888888889,
0.652777777777778,0.666666666666667,0.680555555555556,0.694444444444444,
0.708333333333333,0.722222222222222,0.736111111111111,0.75,0.763888888888889,
0.777777777777778,0.791666666666667,0.805555555555556,0.819444444444444,
0.833333333333333,0.847222222222222,0.861111111111111,0.875,0.888888888888889,
0.902777777777778,0.916666666666667,0.930555555555556,0.944444444444444,
0.958333333333333,0.972222222222222,0.986111111111111,1.),.UNSPECIFIED.)
GEOMETRIC_REPRESENTATION_ITEM()
RATIONAL_B_SPLINE_SURFACE(((1.,0.923879532511287,1.,0.923879532511287,1.,
0.923879532511287,1.,0.923879532511287,1.,0.923879532511287,1.,0.923879532511287,
1.,0.923879532511287,1.,0.923879532511287,1.,0.923879532511287,1.,0.923879532511287,
1.,0.923879532511287,1.,0.923879532511287,1.,0.923879532511287,1.,0.923879532511287,
1.,0.923879532511287,1.,0.923879532511287,1.,0.923879532511287,1.,0.923879532511287,
1.,0.923879532511287,1.,0.923879532511287,1.,0.923879532511287,1.,0.923879532511287,
1.,0.923879532511287,1.,0.923879532511287,1.,0.923879532511287,1.,0.923879532511287,
1.,0.923879532511287,1.,0.923879532511287,1.,0.923879532511287,1.,0.923879532511287,
1.,0.923879532511287,1.,0.923879532511287,1.,0.923879532511287,1.,0.923879532511287,
1.,0.923879532511287,1.,0.923879532511287,1.,0.923879532511287,1.,0.923879532511287,
1.,0.923879532511287,1.,0.923879532511287,1.,0.923879532511287,1.,0.923879532511287,
1.,0.923879532511287,1.,0.923879532511287,1.,0.923879532511287,1.,0.923879532511287,
1.,0.923879532511287,1.,0.923879532511287,1.,0.923879532511287,1.,0.923879532511287,
1.,0.923879532511287,1.,0.923879532511287,1.,0.923879532511287,1.,0.923879532511287,
1.,0.923879532511287,1.,0.923879532511287,1.,0.923879532511287,1.,0.923879532511287,
1.,0.923879532511287,1.,0.923879532511287,1.,0.923879532511287,1.,0.923879532511287,
1.,0.923879532511287,1.,0.923879532511287,1.,0.923879532511287,1.,0.923879532511287,
1.,0.923879532511287,1.,0.923879532511287,1.,0.923879532511287,1.,0.923879532511287,
1.,0.923879532511287,1.,0.923879532511287,1.),(1.,0.923879532511287,1.,
0.923879532511287,1.,0.923879532511287,1.,0.923879532511287,1.,0.923879532511287,
1.,0.923879532511287,1.,0.923879532511287,1.,0.923879532511287,1.,0.923879532511287,
1.,0.923879532511287,1.,0.923879532511287,1.,0.923879532511287,1.,0.923879532511287,
1.,0.923879532511287,1.,0.923879532511287,1.,0.923879532511287,1.,0.923879532511287,
1.,0.923879532511287,1.,0.923879532511287,1.,0.923879532511287,1.,0.923879532511287,
1.,0.923879532511287,1.,0.923879532511287,1.,0.923879532511287,1.,0.923879532511287,
1.,0.923879532511287,1.,0.923879532511287,1.,0.923879532511287,1.,0.923879532511287,
1.,0.923879532511287,1.,0.923879532511287,1.,0.923879532511287,1.,0.923879532511287,
1.,0.923879532511287,1.,0.923879532511287,1.,0.923879532511287,1.,0.923879532511287,
1.,0.923879532511287,1.,0.923879532511287,1.,0.923879532511287,1.,0.923879532511287,
1.,0.923879532511287,1.,0.923879532511287,1.,0.923879532511287,1.,0.923879532511287,
1.,0.923879532511287,1.,0.923879532511287,1.,0.923879532511287,1.,0.923879532511287,
1.,0.923879532511287,1.,0.923879532511287,1.,0.923879532511287,1.,0.923879532511287,
1.,0.923879532511287,1.,0.923879532511287,1.,0.923879532511287,1.,0.923879532511287,
1.,0.923879532511287,1.,0.923879532511287,1.,0.923879532511287,1.,0.923879532511287,
1.,0.923879532511287,1.,0.923879532511287,1.,0.923879532511287,1.,0.923879532511287,
1.,0.923879532511287,1.,0.923879532511287,1.,0.923879532511287,1.,0.923879532511287,
1.,0.923879532511287,1.,0.923879532511287,1.,0.923879532511287,1.)))
REPRESENTATION_ITEM('')
SURFACE()
) ;
#804=(
BOUNDED_CURVE()
B_SPLINE_CURVE(2,(#73318,#73319,#73320,#73321,#73322,#73323,#73324,#73325,
#73326,#73327,#73328,#73329,#73330,#73331,#73332),.UNSPECIFIED.,.F.,.F.)
B_SPLINE_CURVE_WITH_KNOTS((3,2,2,2,2,2,2,3),(0.833333333333333,0.847222222222222,
0.861111111111111,0.875,0.888888888888889,0.902777777777778,0.916666666666667,
0.921887868180636),.UNSPECIFIED.)
CURVE()
GEOMETRIC_REPRESENTATION_ITEM()
RATIONAL_B_SPLINE_CURVE((1.,0.923879532511287,1.,0.923879532511287,1.,0.923879532511287,
1.,0.923879532511287,1.,0.923879532511287,1.,0.923879532511287,1.,0.971384298393079,
0.964283398401841))
REPRESENTATION_ITEM('')
) ;
#819=SHAPE_REPRESENTATION_RELATIONSHIP('SRR','None',#86463,#831) ;
#831=ADVANCED_BREP_SHAPE_REPRESENTATION('',(#855),#86317) ;
#843=STYLED_ITEM('',(#86582),#855) ;
#855=MANIFOLD_SOLID_BREP('Body1',#32642) ;
#892=CONICAL_SURFACE('',#35617,2.38125,0.26179938779915) ;
#893=CONICAL_SURFACE('',#35866,2.38125,0.26179938779915) ;
#894=CONICAL_SURFACE('',#35897,1.7526,0.78539816339745) ;
#895=CONICAL_SURFACE('',#35899,2.38125,0.26179938779915) ;
#896=CONICAL_SURFACE('',#35900,2.38125,0.26179938779915) ;
#922=B_SPLINE_SURFACE_WITH_KNOTS('',3,3,((#74438,#74439,#74440,#74441,#74442,
#74443),(#74444,#74445,#74446,#74447,#74448,#74449),(#74450,#74451,#74452,
#74453,#74454,#74455),(#74456,#74457,#74458,#74459,#74460,#74461)),
 .UNSPECIFIED.,.F.,.F.,.F.,(4,4),(4,2,4),(0.,1.),(-0.0362588513985796,-0.0343987133118532,
0.),.UNSPECIFIED.) ;
#923=B_SPLINE_SURFACE_WITH_KNOTS('',3,3,((#74478,#74479,#74480,#74481),
(#74482,#74483,#74484,#74485),(#74486,#74487,#74488,#74489),(#74490,#74491,
#74492,#74493),(#74494,#74495,#74496,#74497)),.UNSPECIFIED.,.F.,.F.,.F.,
(4,1,4),(4,4),(0.,0.571428571428571,1.),(0.,0.00945665398132608),
 .UNSPECIFIED.) ;
#924=B_SPLINE_SURFACE_WITH_KNOTS('',3,3,((#74513,#74514,#74515,#74516,#74517),
(#74518,#74519,#74520,#74521,#74522),(#74523,#74524,#74525,#74526,#74527),
(#74528,#74529,#74530,#74531,#74532),(#74533,#74534,#74535,#74536,#74537)),
 .UNSPECIFIED.,.F.,.F.,.F.,(4,1,4),(4,1,4),(0.,0.571428571428571,1.),(0.,
0.0040902611621181,0.00954394271160891),.UNSPECIFIED.) ;
#925=B_SPLINE_SURFACE_WITH_KNOTS('',3,3,((#74551,#74552,#74553,#74554),
(#74555,#74556,#74557,#74558),(#74559,#74560,#74561,#74562),(#74563,#74564,
#74565,#74566),(#74567,#74568,#74569,#74570)),.UNSPECIFIED.,.F.,.F.,.F.,
(4,1,4),(4,4),(0.,0.571428571428571,1.),(0.126991784547804,0.128026026143509),
 .UNSPECIFIED.) ;
#926=B_SPLINE_SURFACE_WITH_KNOTS('',3,3,((#74576,#74577,#74578,#74579,#74580,
#74581,#74582,#74583),(#74584,#74585,#74586,#74587,#74588,#74589,#74590,
#74591),(#74592,#74593,#74594,#74595,#74596,#74597,#74598,#74599),(#74600,
#74601,#74602,#74603,#74604,#74605,#74606,#74607),(#74608,#74609,#74610,
#74611,#74612,#74613,#74614,#74615),(#74616,#74617,#74618,#74619,#74620,
#74621,#74622,#74623),(#74624,#74625,#74626,#74627,#74628,#74629,#74630,
#74631),(#74632,#74633,#74634,#74635,#74636,#74637,#74638,#74639),(#74640,
#74641,#74642,#74643,#74644,#74645,#74646,#74647)),.UNSPECIFIED.,.F.,.F.,
 .F.,(4,1,1,1,1,1,4),(4,2,1,1,4),(0.,0.714285714285714,0.857142857142857,
0.928571428571429,0.964285714285714,0.982142857142857,1.00710268589528),
(-0.000154777169791509,0.,0.00161206075000591,0.00241809112500886,0.00444864477949539),
 .UNSPECIFIED.) ;
#927=B_SPLINE_SURFACE_WITH_KNOTS('',3,3,((#74661,#74662,#74663,#74664),
(#74665,#74666,#74667,#74668),(#74669,#74670,#74671,#74672),(#74673,#74674,
#74675,#74676),(#74677,#74678,#74679,#74680)),.UNSPECIFIED.,.F.,.F.,.F.,
(4,1,4),(4,4),(0.,0.571428571428571,1.),(0.,0.00216800481456508),
 .UNSPECIFIED.) ;
#928=B_SPLINE_SURFACE_WITH_KNOTS('',3,3,((#74689,#74690,#74691,#74692,#74693,
#74694,#74695,#74696,#74697),(#74698,#74699,#74700,#74701,#74702,#74703,
#74704,#74705,#74706),(#74707,#74708,#74709,#74710,#74711,#74712,#74713,
#74714,#74715),(#74716,#74717,#74718,#74719,#74720,#74721,#74722,#74723,
#74724),(#74725,#74726,#74727,#74728,#74729,#74730,#74731,#74732,#74733)),
 .UNSPECIFIED.,.F.,.F.,.F.,(4,1,4),(4,1,1,1,1,1,4),(0.,0.571428571428571,
1.),(1.11022302462521E-16,0.000121096313570565,0.00024219262714102,0.000363288940711474,
0.000484385254281929,0.00145315576284556,0.00339069677997283),
 .UNSPECIFIED.) ;
#929=B_SPLINE_SURFACE_WITH_KNOTS('',3,3,((#74755,#74756,#74757,#74758),
(#74759,#74760,#74761,#74762),(#74763,#74764,#74765,#74766),(#74767,#74768,
#74769,#74770)),.UNSPECIFIED.,.F.,.F.,.F.,(4,4),(4,4),(0.,0.47085965842338),
(0.179999904671396,0.182852270042874),.UNSPECIFIED.) ;
#930=B_SPLINE_SURFACE_WITH_KNOTS('',3,3,((#74826,#74827,#74828,#74829,#74830,
#74831),(#74832,#74833,#74834,#74835,#74836,#74837),(#74838,#74839,#74840,
#74841,#74842,#74843),(#74844,#74845,#74846,#74847,#74848,#74849)),
 .UNSPECIFIED.,.F.,.F.,.F.,(4,4),(4,2,4),(0.,1.),(-0.00186013808672659,
0.,0.0343987133118501),.UNSPECIFIED.) ;
#931=B_SPLINE_SURFACE_WITH_KNOTS('',3,3,((#74858,#74859,#74860,#74861),
(#74862,#74863,#74864,#74865),(#74866,#74867,#74868,#74869),(#74870,#74871,
#74872,#74873),(#74874,#74875,#74876,#74877)),.UNSPECIFIED.,.F.,.F.,.F.,
(4,1,4),(4,4),(0.,0.571428571428571,1.),(7.96865975725692E-14,0.00945665401173728),
 .UNSPECIFIED.) ;
#932=B_SPLINE_SURFACE_WITH_KNOTS('',3,3,((#74890,#74891,#74892,#74893,#74894),
(#74895,#74896,#74897,#74898,#74899),(#74900,#74901,#74902,#74903,#74904),
(#74905,#74906,#74907,#74908,#74909),(#74910,#74911,#74912,#74913,#74914)),
 .UNSPECIFIED.,.F.,.F.,.F.,(4,1,4),(4,1,4),(0.,0.571428571428571,1.),(0.,
0.00545368154943955,0.00954394271151922),.UNSPECIFIED.) ;
#933=B_SPLINE_SURFACE_WITH_KNOTS('',3,3,((#74922,#74923,#74924,#74925),
(#74926,#74927,#74928,#74929),(#74930,#74931,#74932,#74933),(#74934,#74935,
#74936,#74937),(#74938,#74939,#74940,#74941)),.UNSPECIFIED.,.F.,.F.,.F.,
(4,1,4),(4,4),(0.,0.571428571428571,1.),(0.126991784443102,0.128026026038763),
 .UNSPECIFIED.) ;
#934=B_SPLINE_SURFACE_WITH_KNOTS('',3,3,((#74945,#74946,#74947,#74948,#74949,
#74950,#74951,#74952,#74953),(#74954,#74955,#74956,#74957,#74958,#74959,
#74960,#74961,#74962),(#74963,#74964,#74965,#74966,#74967,#74968,#74969,
#74970,#74971),(#74972,#74973,#74974,#74975,#74976,#74977,#74978,#74979,
#74980),(#74981,#74982,#74983,#74984,#74985,#74986,#74987,#74988,#74989)),
 .UNSPECIFIED.,.F.,.F.,.F.,(4,1,4),(4,1,1,1,2,4),(0.,0.571428571428571,
1.),(0.,0.000799914108848609,0.00159982821769722,0.00239974232654583,0.00399957054424305,
0.00418497063961359),.UNSPECIFIED.) ;
#935=B_SPLINE_SURFACE_WITH_KNOTS('',3,3,((#75017,#75018,#75019,#75020),
(#75021,#75022,#75023,#75024),(#75025,#75026,#75027,#75028),(#75029,#75030,
#75031,#75032),(#75033,#75034,#75035,#75036)),.UNSPECIFIED.,.F.,.F.,.F.,
(4,1,4),(4,4),(0.,0.571428571428571,1.),(0.,0.00216800481456542),
 .UNSPECIFIED.) ;
#936=B_SPLINE_SURFACE_WITH_KNOTS('',3,3,((#75045,#75046,#75047,#75048,#75049,
#75050,#75051,#75052,#75053),(#75054,#75055,#75056,#75057,#75058,#75059,
#75060,#75061,#75062),(#75063,#75064,#75065,#75066,#75067,#75068,#75069,
#75070,#75071),(#75072,#75073,#75074,#75075,#75076,#75077,#75078,#75079,
#75080),(#75081,#75082,#75083,#75084,#75085,#75086,#75087,#75088,#75089)),
 .UNSPECIFIED.,.F.,.F.,.F.,(4,1,4),(4,1,1,1,1,1,4),(0.,0.571428571428571,
1.),(0.,0.000121096313570718,0.000242192627141436,0.000363288940712154,
0.000484385254282872,0.00145315576284862,0.00339069677998011),
 .UNSPECIFIED.) ;
#937=B_SPLINE_SURFACE_WITH_KNOTS('',3,3,((#75129,#75130,#75131,#75132,#75133,
#75134),(#75135,#75136,#75137,#75138,#75139,#75140),(#75141,#75142,#75143,
#75144,#75145,#75146),(#75147,#75148,#75149,#75150,#75151,#75152)),
 .UNSPECIFIED.,.F.,.F.,.F.,(4,4),(4,2,4),(0.,1.),(-0.0362588513985796,-0.0343987133118529,
0.),.UNSPECIFIED.) ;
#938=B_SPLINE_SURFACE_WITH_KNOTS('',3,3,((#75161,#75162,#75163,#75164),
(#75165,#75166,#75167,#75168),(#75169,#75170,#75171,#75172),(#75173,#75174,
#75175,#75176),(#75177,#75178,#75179,#75180)),.UNSPECIFIED.,.F.,.F.,.F.,
(4,1,4),(4,4),(0.,0.571428571428571,1.),(0.,0.00945665398132565),
 .UNSPECIFIED.) ;
#939=B_SPLINE_SURFACE_WITH_KNOTS('',3,3,((#75196,#75197,#75198,#75199,#75200),
(#75201,#75202,#75203,#75204,#75205),(#75206,#75207,#75208,#75209,#75210),
(#75211,#75212,#75213,#75214,#75215),(#75216,#75217,#75218,#75219,#75220)),
 .UNSPECIFIED.,.F.,.F.,.F.,(4,1,4),(4,1,4),(0.,0.571428571428571,1.),(5.7658280050909E-17,
0.00409026116211842,0.00954394271160956),.UNSPECIFIED.) ;
#940=B_SPLINE_SURFACE_WITH_KNOTS('',3,3,((#75234,#75235,#75236,#75237),
(#75238,#75239,#75240,#75241),(#75242,#75243,#75244,#75245),(#75246,#75247,
#75248,#75249),(#75250,#75251,#75252,#75253)),.UNSPECIFIED.,.F.,.F.,.F.,
(4,1,4),(4,4),(0.,0.571428571428571,1.),(0.253983569095608,0.255017810691314),
 .UNSPECIFIED.) ;
#941=B_SPLINE_SURFACE_WITH_KNOTS('',3,3,((#75259,#75260,#75261,#75262,#75263,
#75264,#75265,#75266,#75267),(#75268,#75269,#75270,#75271,#75272,#75273,
#75274,#75275,#75276),(#75277,#75278,#75279,#75280,#75281,#75282,#75283,
#75284,#75285),(#75286,#75287,#75288,#75289,#75290,#75291,#75292,#75293,
#75294),(#75295,#75296,#75297,#75298,#75299,#75300,#75301,#75302,#75303)),
 .UNSPECIFIED.,.F.,.F.,.F.,(4,1,4),(4,2,1,1,1,4),(0.,0.571428571428571,
1.00181493187422),(-0.000154790814778927,0.,0.00161206074594362,0.00241809111891543,
0.00322412149188724,0.00444864613282186),.UNSPECIFIED.) ;
#942=B_SPLINE_SURFACE_WITH_KNOTS('',3,3,((#75370,#75371,#75372,#75373),
(#75374,#75375,#75376,#75377),(#75378,#75379,#75380,#75381),(#75382,#75383,
#75384,#75385),(#75386,#75387,#75388,#75389)),.UNSPECIFIED.,.F.,.F.,.F.,
(4,1,4),(4,4),(0.,0.571428571428571,1.),(1.21699733691425E-15,0.00216800481456625),
 .UNSPECIFIED.) ;
#943=B_SPLINE_SURFACE_WITH_KNOTS('',3,3,((#75398,#75399,#75400,#75401,#75402,
#75403,#75404,#75405,#75406),(#75407,#75408,#75409,#75410,#75411,#75412,
#75413,#75414,#75415),(#75416,#75417,#75418,#75419,#75420,#75421,#75422,
#75423,#75424),(#75425,#75426,#75427,#75428,#75429,#75430,#75431,#75432,
#75433),(#75434,#75435,#75436,#75437,#75438,#75439,#75440,#75441,#75442)),
 .UNSPECIFIED.,.F.,.F.,.F.,(4,1,4),(4,1,1,1,1,1,4),(0.,0.571428571428571,
1.),(2.74316139050604E-16,0.000121096313570731,0.000242192627141187,0.0004843852542821,
0.000968770508563926,0.00193754101712758,0.00339069677997306),
 .UNSPECIFIED.) ;
#944=B_SPLINE_SURFACE_WITH_KNOTS('',3,3,((#75462,#75463,#75464,#75465),
(#75466,#75467,#75468,#75469),(#75470,#75471,#75472,#75473),(#75474,#75475,
#75476,#75477)),.UNSPECIFIED.,.F.,.F.,.F.,(4,4),(4,4),(0.,0.470859658423347),
(0.179999904671396,0.182852270042875),.UNSPECIFIED.) ;
#945=B_SPLINE_SURFACE_WITH_KNOTS('',3,3,((#75491,#75492,#75493,#75494,#75495,
#75496),(#75497,#75498,#75499,#75500,#75501,#75502),(#75503,#75504,#75505,
#75506,#75507,#75508),(#75509,#75510,#75511,#75512,#75513,#75514)),
 .UNSPECIFIED.,.F.,.F.,.F.,(4,4),(4,2,4),(0.,1.),(-0.00186013808672611,
0.,0.0343987133118504),.UNSPECIFIED.) ;
#946=B_SPLINE_SURFACE_WITH_KNOTS('',3,3,((#75523,#75524,#75525,#75526),
(#75527,#75528,#75529,#75530),(#75531,#75532,#75533,#75534),(#75535,#75536,
#75537,#75538),(#75539,#75540,#75541,#75542)),.UNSPECIFIED.,.F.,.F.,.F.,
(4,1,4),(4,4),(0.,0.571428571428571,1.),(7.97441283497418E-14,0.00945665401173742),
 .UNSPECIFIED.) ;
#947=B_SPLINE_SURFACE_WITH_KNOTS('',3,3,((#75555,#75556,#75557,#75558,#75559),
(#75560,#75561,#75562,#75563,#75564),(#75565,#75566,#75567,#75568,#75569),
(#75570,#75571,#75572,#75573,#75574),(#75575,#75576,#75577,#75578,#75579)),
 .UNSPECIFIED.,.F.,.F.,.F.,(4,1,4),(4,1,4),(0.,0.571428571428571,1.),(0.,
0.00409026116207964,0.00954394271151917),.UNSPECIFIED.) ;
#948=B_SPLINE_SURFACE_WITH_KNOTS('',3,3,((#75587,#75588,#75589,#75590),
(#75591,#75592,#75593,#75594),(#75595,#75596,#75597,#75598),(#75599,#75600,
#75601,#75602),(#75603,#75604,#75605,#75606)),.UNSPECIFIED.,.F.,.F.,.F.,
(4,1,4),(4,4),(0.,0.571428571428571,1.),(0.126991784443102,0.128026026038763),
 .UNSPECIFIED.) ;
#949=B_SPLINE_SURFACE_WITH_KNOTS('',3,3,((#75610,#75611,#75612,#75613,#75614,
#75615,#75616,#75617,#75618),(#75619,#75620,#75621,#75622,#75623,#75624,
#75625,#75626,#75627),(#75628,#75629,#75630,#75631,#75632,#75633,#75634,
#75635,#75636),(#75637,#75638,#75639,#75640,#75641,#75642,#75643,#75644,
#75645),(#75646,#75647,#75648,#75649,#75650,#75651,#75652,#75653,#75654)),
 .UNSPECIFIED.,.F.,.F.,.F.,(4,1,4),(4,1,1,1,2,4),(0.,0.571428571428571,
1.),(0.,0.000799914107796385,0.00159982821559277,0.00239974232338915,0.00399957053898192,
0.00418493275019483),.UNSPECIFIED.) ;
#950=B_SPLINE_SURFACE_WITH_KNOTS('',3,3,((#75682,#75683,#75684,#75685),
(#75686,#75687,#75688,#75689),(#75690,#75691,#75692,#75693),(#75694,#75695,
#75696,#75697),(#75698,#75699,#75700,#75701)),.UNSPECIFIED.,.F.,.F.,.F.,
(4,1,4),(4,4),(0.,0.571428571428571,1.),(0.,0.00216800481456436),
 .UNSPECIFIED.) ;
#951=B_SPLINE_SURFACE_WITH_KNOTS('',3,3,((#75710,#75711,#75712,#75713,#75714,
#75715,#75716,#75717,#75718),(#75719,#75720,#75721,#75722,#75723,#75724,
#75725,#75726,#75727),(#75728,#75729,#75730,#75731,#75732,#75733,#75734,
#75735,#75736),(#75737,#75738,#75739,#75740,#75741,#75742,#75743,#75744,
#75745),(#75746,#75747,#75748,#75749,#75750,#75751,#75752,#75753,#75754)),
 .UNSPECIFIED.,.F.,.F.,.F.,(4,1,4),(4,1,1,1,1,1,4),(0.,0.571428571428571,
1.),(0.,0.000121096313570705,0.00024219262714141,0.000363288940712115,0.00048438525428282,
0.00145315576284846,0.00339069677997974),.UNSPECIFIED.) ;
#952=B_SPLINE_SURFACE_WITH_KNOTS('',3,3,((#75790,#75791,#75792,#75793),
(#75794,#75795,#75796,#75797),(#75798,#75799,#75800,#75801),(#75802,#75803,
#75804,#75805)),.UNSPECIFIED.,.F.,.F.,.F.,(4,4),(4,4),(0.,1.),(-1.5707963267949,
-0.0872664625997159),.UNSPECIFIED.) ;
#953=B_SPLINE_SURFACE_WITH_KNOTS('',3,3,((#75846,#75847,#75848,#75849,#75850,
#75851),(#75852,#75853,#75854,#75855,#75856,#75857),(#75858,#75859,#75860,
#75861,#75862,#75863),(#75864,#75865,#75866,#75867,#75868,#75869),(#75870,
#75871,#75872,#75873,#75874,#75875)),.UNSPECIFIED.,.F.,.F.,.F.,(4,1,4),
(4,2,4),(0.,0.571428571428571,1.),(0.,0.0361627499148956,0.0364117611345324),
 .UNSPECIFIED.) ;
#954=B_SPLINE_SURFACE_WITH_KNOTS('',3,3,((#75884,#75885,#75886,#75887),
(#75888,#75889,#75890,#75891),(#75892,#75893,#75894,#75895),(#75896,#75897,
#75898,#75899),(#75900,#75901,#75902,#75903)),.UNSPECIFIED.,.F.,.F.,.F.,
(4,1,4),(4,4),(0.,0.571428571428571,1.),(2.33694858927792E-16,0.00331127956228568),
 .UNSPECIFIED.) ;
#955=B_SPLINE_SURFACE_WITH_KNOTS('',3,3,((#75907,#75908,#75909,#75910),
(#75911,#75912,#75913,#75914),(#75915,#75916,#75917,#75918),(#75919,#75920,
#75921,#75922),(#75923,#75924,#75925,#75926)),.UNSPECIFIED.,.F.,.F.,.F.,
(4,1,4),(4,4),(0.,0.571428571428571,1.00022442227795),(-0.00022442227795638,
0.146595920707548),.UNSPECIFIED.) ;
#956=B_SPLINE_SURFACE_WITH_KNOTS('',3,3,((#75946,#75947,#75948,#75949),
(#75950,#75951,#75952,#75953),(#75954,#75955,#75956,#75957),(#75958,#75959,
#75960,#75961),(#75962,#75963,#75964,#75965)),.UNSPECIFIED.,.F.,.F.,.F.,
(4,1,4),(4,4),(-0.000224423998443304,0.571428571428571,1.),(-0.000224423998443185,
0.146595922429139),.UNSPECIFIED.) ;
#957=B_SPLINE_SURFACE_WITH_KNOTS('',3,3,((#75981,#75982,#75983,#75984),
(#75985,#75986,#75987,#75988),(#75989,#75990,#75991,#75992),(#75993,#75994,
#75995,#75996),(#75997,#75998,#75999,#76000)),.UNSPECIFIED.,.F.,.F.,.F.,
(4,1,4),(4,4),(0.,0.571428571428571,1.),(1.76333003250469E-16,0.00331127956228543),
 .UNSPECIFIED.) ;
#958=B_SPLINE_SURFACE_WITH_KNOTS('',3,3,((#76006,#76007,#76008,#76009,#76010,
#76011),(#76012,#76013,#76014,#76015,#76016,#76017),(#76018,#76019,#76020,
#76021,#76022,#76023),(#76024,#76025,#76026,#76027,#76028,#76029),(#76030,
#76031,#76032,#76033,#76034,#76035)),.UNSPECIFIED.,.F.,.F.,.F.,(4,1,4),
(4,2,4),(0.,0.571428571428571,1.),(8.84614312661979E-17,0.0361913306097799,
0.0364133025372201),.UNSPECIFIED.) ;
#959=B_SPLINE_SURFACE_WITH_KNOTS('',3,3,((#76063,#76064,#76065,#76066),
(#76067,#76068,#76069,#76070),(#76071,#76072,#76073,#76074),(#76075,#76076,
#76077,#76078)),.UNSPECIFIED.,.F.,.F.,.F.,(4,4),(4,4),(0.,1.),(-1.5707963267949,
-0.0872664625997159),.UNSPECIFIED.) ;
#960=B_SPLINE_SURFACE_WITH_KNOTS('',3,3,((#76109,#76110,#76111,#76112),
(#76113,#76114,#76115,#76116),(#76117,#76118,#76119,#76120),(#76121,#76122,
#76123,#76124),(#76125,#76126,#76127,#76128)),.UNSPECIFIED.,.F.,.F.,.F.,
(4,1,4),(4,4),(0.,0.571428571428571,1.00022442227796),(-0.000224422277962333,
0.146595920707853),.UNSPECIFIED.) ;
#961=B_SPLINE_SURFACE_WITH_KNOTS('',3,3,((#76144,#76145,#76146,#76147),
(#76148,#76149,#76150,#76151),(#76152,#76153,#76154,#76155),(#76156,#76157,
#76158,#76159),(#76160,#76161,#76162,#76163)),.UNSPECIFIED.,.F.,.F.,.F.,
(4,1,4),(4,4),(0.,0.571428571428571,1.),(0.,0.00331127956228537),
 .UNSPECIFIED.) ;
#962=B_SPLINE_SURFACE_WITH_KNOTS('',3,3,((#76169,#76170,#76171,#76172,#76173,
#76174),(#76175,#76176,#76177,#76178,#76179,#76180),(#76181,#76182,#76183,
#76184,#76185,#76186),(#76187,#76188,#76189,#76190,#76191,#76192),(#76193,
#76194,#76195,#76196,#76197,#76198)),.UNSPECIFIED.,.F.,.F.,.F.,(4,1,4),
(4,2,4),(0.,0.571428571428571,1.),(0.,0.0361629958429266,0.0364117772057813),
 .UNSPECIFIED.) ;
#963=B_SPLINE_SURFACE_WITH_KNOTS('',3,3,((#76250,#76251,#76252,#76253),
(#76254,#76255,#76256,#76257),(#76258,#76259,#76260,#76261),(#76262,#76263,
#76264,#76265),(#76266,#76267,#76268,#76269)),.UNSPECIFIED.,.F.,.F.,.F.,
(4,1,4),(4,4),(-0.000224423998441357,0.571428571428571,1.),(-0.000224423998442386,
0.146595922428333),.UNSPECIFIED.) ;
#964=B_SPLINE_SURFACE_WITH_KNOTS('',3,3,((#76276,#76277,#76278,#76279),
(#76280,#76281,#76282,#76283),(#76284,#76285,#76286,#76287),(#76288,#76289,
#76290,#76291),(#76292,#76293,#76294,#76295)),.UNSPECIFIED.,.F.,.F.,.F.,
(4,1,4),(4,4),(0.,0.571428571428571,1.),(1.64044101459669E-16,0.00331127956228544),
 .UNSPECIFIED.) ;
#965=B_SPLINE_SURFACE_WITH_KNOTS('',3,3,((#76299,#76300,#76301,#76302,#76303,
#76304),(#76305,#76306,#76307,#76308,#76309,#76310),(#76311,#76312,#76313,
#76314,#76315,#76316),(#76317,#76318,#76319,#76320,#76321,#76322),(#76323,
#76324,#76325,#76326,#76327,#76328)),.UNSPECIFIED.,.F.,.F.,.F.,(4,1,4),
(4,2,4),(0.,0.571428571428571,1.),(0.,0.0361913306296307,0.0364133025382447),
 .UNSPECIFIED.) ;
#966=B_SPLINE_SURFACE_WITH_KNOTS('',3,3,((#76349,#76350,#76351,#76352),
(#76353,#76354,#76355,#76356),(#76357,#76358,#76359,#76360),(#76361,#76362,
#76363,#76364)),.UNSPECIFIED.,.F.,.F.,.F.,(4,4),(4,4),(0.,1.),(-1.5707963267949,
-0.0872664625997158),.UNSPECIFIED.) ;
#967=B_SPLINE_SURFACE_WITH_KNOTS('',3,3,((#76388,#76389,#76390,#76391),
(#76392,#76393,#76394,#76395),(#76396,#76397,#76398,#76399),(#76400,#76401,
#76402,#76403)),.UNSPECIFIED.,.F.,.F.,.F.,(4,4),(4,4),(0.,1.),(-1.5707963267949,
-0.0872664625997159),.UNSPECIFIED.) ;
#968=B_SPLINE_SURFACE_WITH_KNOTS('',3,3,((#76425,#76426,#76427,#76428,#76429,
#76430,#76431,#76432,#76433,#76434),(#76435,#76436,#76437,#76438,#76439,
#76440,#76441,#76442,#76443,#76444),(#76445,#76446,#76447,#76448,#76449,
#76450,#76451,#76452,#76453,#76454),(#76455,#76456,#76457,#76458,#76459,
#76460,#76461,#76462,#76463,#76464)),.UNSPECIFIED.,.F.,.F.,.F.,(4,4),(4,
2,2,2,4),(-0.0343546625814549,1.0000001624628),(-0.32865367100704,-0.273443015535847,
-0.153352882404738,-0.0199317405198332,0.0415869283876659),
 .UNSPECIFIED.) ;
#969=B_SPLINE_SURFACE_WITH_KNOTS('',3,3,((#76599,#76600,#76601,#76602,#76603,
#76604,#76605,#76606,#76607,#76608),(#76609,#76610,#76611,#76612,#76613,
#76614,#76615,#76616,#76617,#76618),(#76619,#76620,#76621,#76622,#76623,
#76624,#76625,#76626,#76627,#76628),(#76629,#76630,#76631,#76632,#76633,
#76634,#76635,#76636,#76637,#76638),(#76639,#76640,#76641,#76642,#76643,
#76644,#76645,#76646,#76647,#76648),(#76649,#76650,#76651,#76652,#76653,
#76654,#76655,#76656,#76657,#76658),(#76659,#76660,#76661,#76662,#76663,
#76664,#76665,#76666,#76667,#76668)),.UNSPECIFIED.,.F.,.F.,.F.,(4,1,1,1,
4),(4,2,2,2,4),(-0.000134967941931711,0.285714285714286,0.571428571428571,
0.857142857142857,1.00001222043739),(-0.408276645255811,-0.349022909463275,
-0.215144182724569,-0.094503731574,3.81138728867237E-14),.UNSPECIFIED.) ;
#970=B_SPLINE_SURFACE_WITH_KNOTS('',3,3,((#77299,#77300,#77301,#77302,#77303,
#77304),(#77305,#77306,#77307,#77308,#77309,#77310),(#77311,#77312,#77313,
#77314,#77315,#77316),(#77317,#77318,#77319,#77320,#77321,#77322)),
 .UNSPECIFIED.,.F.,.F.,.F.,(4,4),(4,2,4),(0.,1.),(-0.0308408628658576,-0.0306076340858662,
0.),.UNSPECIFIED.) ;
#971=B_SPLINE_SURFACE_WITH_KNOTS('',3,3,((#77341,#77342,#77343,#77344),
(#77345,#77346,#77347,#77348),(#77349,#77350,#77351,#77352),(#77353,#77354,
#77355,#77356),(#77357,#77358,#77359,#77360)),.UNSPECIFIED.,.F.,.F.,.F.,
(4,1,4),(4,4),(0.,0.571428571428571,1.),(0.,0.00359123636946031),
 .UNSPECIFIED.) ;
#972=B_SPLINE_SURFACE_WITH_KNOTS('',3,3,((#77366,#77367,#77368,#77369),
(#77370,#77371,#77372,#77373),(#77374,#77375,#77376,#77377),(#77378,#77379,
#77380,#77381),(#77382,#77383,#77384,#77385)),.UNSPECIFIED.,.F.,.F.,.F.,
(4,1,4),(4,4),(0.,0.571428571428571,1.),(0.,0.0186228334819338),
 .UNSPECIFIED.) ;
#973=B_SPLINE_SURFACE_WITH_KNOTS('',3,3,((#77428,#77429,#77430,#77431),
(#77432,#77433,#77434,#77435),(#77436,#77437,#77438,#77439),(#77440,#77441,
#77442,#77443),(#77444,#77445,#77446,#77447)),.UNSPECIFIED.,.F.,.F.,.F.,
(4,1,4),(4,4),(0.,0.571428571428571,1.),(0.,0.0186228334823064),
 .UNSPECIFIED.) ;
#974=B_SPLINE_SURFACE_WITH_KNOTS('',3,3,((#77453,#77454,#77455,#77456),
(#77457,#77458,#77459,#77460),(#77461,#77462,#77463,#77464),(#77465,#77466,
#77467,#77468),(#77469,#77470,#77471,#77472)),.UNSPECIFIED.,.F.,.F.,.F.,
(4,1,4),(4,4),(0.,0.571428571428571,1.),(0.,0.00359123636948427),
 .UNSPECIFIED.) ;
#975=B_SPLINE_SURFACE_WITH_KNOTS('',3,3,((#77477,#77478,#77479,#77480,#77481,
#77482),(#77483,#77484,#77485,#77486,#77487,#77488),(#77489,#77490,#77491,
#77492,#77493,#77494),(#77495,#77496,#77497,#77498,#77499,#77500),(#77501,
#77502,#77503,#77504,#77505,#77506)),.UNSPECIFIED.,.F.,.F.,.F.,(4,1,4),
(4,2,4),(0.,0.571428571428571,1.),(-0.0306076446211308,0.,0.000233218663520837),
 .UNSPECIFIED.) ;
#976=B_SPLINE_SURFACE_WITH_KNOTS('',3,3,((#77539,#77540,#77541,#77542),
(#77543,#77544,#77545,#77546),(#77547,#77548,#77549,#77550),(#77551,#77552,
#77553,#77554)),.UNSPECIFIED.,.F.,.F.,.F.,(4,4),(4,4),(0.,1.),(0.0872664625997159,
1.5707963267949),.UNSPECIFIED.) ;
#977=B_SPLINE_SURFACE_WITH_KNOTS('',3,3,((#77564,#77565,#77566,#77567,#77568),
(#77569,#77570,#77571,#77572,#77573),(#77574,#77575,#77576,#77577,#77578),
(#77579,#77580,#77581,#77582,#77583),(#77584,#77585,#77586,#77587,#77588)),
 .UNSPECIFIED.,.F.,.F.,.F.,(4,1,4),(4,1,4),(-0.00252299082537574,0.571428571428571,
1.00133658399285),(-1.34809870897391,-0.448243149014699,0.227279268661048),
 .UNSPECIFIED.) ;
#978=B_SPLINE_SURFACE_WITH_KNOTS('',3,3,((#77620,#77621,#77622,#77623),
(#77624,#77625,#77626,#77627),(#77628,#77629,#77630,#77631),(#77632,#77633,
#77634,#77635)),.UNSPECIFIED.,.F.,.F.,.F.,(4,4),(4,4),(0.,1.),(0.0872664625997158,
1.5707963267949),.UNSPECIFIED.) ;
#979=B_SPLINE_SURFACE_WITH_KNOTS('',3,3,((#77636,#77637,#77638,#77639,#77640),
(#77641,#77642,#77643,#77644,#77645),(#77646,#77647,#77648,#77649,#77650),
(#77651,#77652,#77653,#77654,#77655),(#77656,#77657,#77658,#77659,#77660)),
 .UNSPECIFIED.,.F.,.F.,.F.,(4,1,4),(4,1,4),(-0.00252299071549198,0.571428571428571,
1.00133658396291),(-0.227279268551174,0.44824314284206,1.34809869654654),
 .UNSPECIFIED.) ;
#980=B_SPLINE_SURFACE_WITH_KNOTS('',3,3,((#77679,#77680,#77681,#77682),
(#77683,#77684,#77685,#77686),(#77687,#77688,#77689,#77690),(#77691,#77692,
#77693,#77694)),.UNSPECIFIED.,.F.,.F.,.F.,(4,4),(4,4),(0.,1.),(0.0872664625997159,
1.5707963267949),.UNSPECIFIED.) ;
#981=B_SPLINE_SURFACE_WITH_KNOTS('',3,3,((#77724,#77725,#77726,#77727),
(#77728,#77729,#77730,#77731),(#77732,#77733,#77734,#77735),(#77736,#77737,
#77738,#77739)),.UNSPECIFIED.,.F.,.F.,.F.,(4,4),(4,4),(0.,1.),(0.0872664625997159,
1.5707963267949),.UNSPECIFIED.) ;
#982=B_SPLINE_SURFACE_WITH_KNOTS('',3,3,((#77747,#77748,#77749,#77750),
(#77751,#77752,#77753,#77754),(#77755,#77756,#77757,#77758),(#77759,#77760,
#77761,#77762)),.UNSPECIFIED.,.F.,.F.,.F.,(4,4),(4,4),(0.,0.470859658428145),
(0.177146934337171,0.179997619857109),.UNSPECIFIED.) ;
#983=B_SPLINE_SURFACE_WITH_KNOTS('',3,3,((#77763,#77764,#77765,#77766),
(#77767,#77768,#77769,#77770),(#77771,#77772,#77773,#77774),(#77775,#77776,
#77777,#77778)),.UNSPECIFIED.,.F.,.F.,.F.,(4,4),(4,4),(0.,0.470859658428137),
(0.177146934337171,0.17999761985711),.UNSPECIFIED.) ;
#984=B_SPLINE_SURFACE_WITH_KNOTS('',3,3,((#77785,#77786,#77787,#77788,#77789,
#77790),(#77791,#77792,#77793,#77794,#77795,#77796),(#77797,#77798,#77799,
#77800,#77801,#77802),(#77803,#77804,#77805,#77806,#77807,#77808)),
 .UNSPECIFIED.,.F.,.F.,.F.,(4,4),(4,2,4),(0.,1.),(-0.0308408628658596,-0.0306076340858954,
0.),.UNSPECIFIED.) ;
#985=B_SPLINE_SURFACE_WITH_KNOTS('',3,3,((#77827,#77828,#77829,#77830),
(#77831,#77832,#77833,#77834),(#77835,#77836,#77837,#77838),(#77839,#77840,
#77841,#77842),(#77843,#77844,#77845,#77846)),.UNSPECIFIED.,.F.,.F.,.F.,
(4,1,4),(4,4),(0.,0.571428571428571,1.),(0.,0.00359123636946112),
 .UNSPECIFIED.) ;
#986=B_SPLINE_SURFACE_WITH_KNOTS('',3,3,((#77852,#77853,#77854,#77855),
(#77856,#77857,#77858,#77859),(#77860,#77861,#77862,#77863),(#77864,#77865,
#77866,#77867),(#77868,#77869,#77870,#77871)),.UNSPECIFIED.,.F.,.F.,.F.,
(4,1,4),(4,4),(0.,0.571428571428571,1.),(0.,0.0186228334818513),
 .UNSPECIFIED.) ;
#987=B_SPLINE_SURFACE_WITH_KNOTS('',3,3,((#77914,#77915,#77916,#77917),
(#77918,#77919,#77920,#77921),(#77922,#77923,#77924,#77925),(#77926,#77927,
#77928,#77929),(#77930,#77931,#77932,#77933)),.UNSPECIFIED.,.F.,.F.,.F.,
(4,1,4),(4,4),(0.,0.571428571428571,1.),(0.,0.0186228334823063),
 .UNSPECIFIED.) ;
#988=B_SPLINE_SURFACE_WITH_KNOTS('',3,3,((#77939,#77940,#77941,#77942),
(#77943,#77944,#77945,#77946),(#77947,#77948,#77949,#77950),(#77951,#77952,
#77953,#77954),(#77955,#77956,#77957,#77958)),.UNSPECIFIED.,.F.,.F.,.F.,
(4,1,4),(4,4),(0.,0.571428571428571,1.),(0.,0.00359123636948379),
 .UNSPECIFIED.) ;
#989=B_SPLINE_SURFACE_WITH_KNOTS('',3,3,((#77963,#77964,#77965,#77966,#77967,
#77968),(#77969,#77970,#77971,#77972,#77973,#77974),(#77975,#77976,#77977,
#77978,#77979,#77980),(#77981,#77982,#77983,#77984,#77985,#77986),(#77987,
#77988,#77989,#77990,#77991,#77992)),.UNSPECIFIED.,.F.,.F.,.F.,(4,1,4),
(4,2,4),(0.,0.571428571428571,1.),(-0.0306076446211596,0.,0.0002332186634917),
 .UNSPECIFIED.) ;
#990=B_SPLINE_SURFACE_WITH_KNOTS('',3,3,((#78032,#78033,#78034,#78035),
(#78036,#78037,#78038,#78039),(#78040,#78041,#78042,#78043),(#78044,#78045,
#78046,#78047)),.UNSPECIFIED.,.F.,.F.,.F.,(4,4),(4,4),(0.,1.),(0.0872664625997158,
1.5707963267949),.UNSPECIFIED.) ;
#991=B_SPLINE_SURFACE_WITH_KNOTS('',3,3,((#78051,#78052,#78053,#78054,#78055),
(#78056,#78057,#78058,#78059,#78060),(#78061,#78062,#78063,#78064,#78065),
(#78066,#78067,#78068,#78069,#78070),(#78071,#78072,#78073,#78074,#78075)),
 .UNSPECIFIED.,.F.,.F.,.F.,(4,1,4),(4,1,4),(-0.00218136360640586,0.571428571428571,
1.00166487948942),(-1.34775708175487,-0.672576291298116,0.226937641442087),
 .UNSPECIFIED.) ;
#992=B_SPLINE_SURFACE_WITH_KNOTS('',3,3,((#78108,#78109,#78110,#78111),
(#78112,#78113,#78114,#78115),(#78116,#78117,#78118,#78119),(#78120,#78121,
#78122,#78123)),.UNSPECIFIED.,.F.,.F.,.F.,(4,4),(4,4),(0.,1.),(-1.5707963267949,
-0.0872664625997159),.UNSPECIFIED.) ;
#993=B_SPLINE_SURFACE_WITH_KNOTS('',3,3,((#78128,#78129,#78130,#78131,#78132),
(#78133,#78134,#78135,#78136,#78137),(#78138,#78139,#78140,#78141,#78142),
(#78143,#78144,#78145,#78146,#78147),(#78148,#78149,#78150,#78151,#78152)),
 .UNSPECIFIED.,.F.,.F.,.F.,(4,1,4),(4,1,4),(-0.00252299071546332,0.571428571428571,
1.00133658396291),(-0.22727926855115,0.44824314284204,1.34809869654644),
 .UNSPECIFIED.) ;
#994=B_SPLINE_SURFACE_WITH_KNOTS('',3,3,((#78169,#78170,#78171,#78172),
(#78173,#78174,#78175,#78176),(#78177,#78178,#78179,#78180),(#78181,#78182,
#78183,#78184)),.UNSPECIFIED.,.F.,.F.,.F.,(4,4),(4,4),(0.,1.),(0.0872664625997154,
1.5707963267949),.UNSPECIFIED.) ;
#995=B_SPLINE_SURFACE_WITH_KNOTS('',3,3,((#78216,#78217,#78218,#78219),
(#78220,#78221,#78222,#78223),(#78224,#78225,#78226,#78227),(#78228,#78229,
#78230,#78231)),.UNSPECIFIED.,.F.,.F.,.F.,(4,4),(4,4),(0.,1.),(0.087266462599716,
1.5707963267949),.UNSPECIFIED.) ;
#996=B_SPLINE_SURFACE_WITH_KNOTS('',3,3,((#78256,#78257,#78258,#78259),
(#78260,#78261,#78262,#78263),(#78264,#78265,#78266,#78267),(#78268,#78269,
#78270,#78271),(#78272,#78273,#78274,#78275),(#78276,#78277,#78278,#78279)),
 .UNSPECIFIED.,.F.,.F.,.F.,(4,1,1,4),(4,4),(0.,0.285714285714286,0.571428571428571,
1.),(0.,0.0319729496810593),.UNSPECIFIED.) ;
#997=B_SPLINE_SURFACE_WITH_KNOTS('',3,3,((#78293,#78294,#78295,#78296),
(#78297,#78298,#78299,#78300),(#78301,#78302,#78303,#78304),(#78305,#78306,
#78307,#78308),(#78309,#78310,#78311,#78312),(#78313,#78314,#78315,#78316)),
 .UNSPECIFIED.,.F.,.F.,.F.,(4,1,1,4),(4,4),(0.,0.285714285714286,0.571428571428571,
1.),(0.,0.0319729764593517),.UNSPECIFIED.) ;
#998=B_SPLINE_SURFACE_WITH_KNOTS('',3,3,((#78326,#78327,#78328,#78329,#78330),
(#78331,#78332,#78333,#78334,#78335),(#78336,#78337,#78338,#78339,#78340),
(#78341,#78342,#78343,#78344,#78345),(#78346,#78347,#78348,#78349,#78350),
(#78351,#78352,#78353,#78354,#78355)),.UNSPECIFIED.,.F.,.F.,.F.,(4,1,1,
4),(4,1,4),(0.,0.285714285714286,0.571428571428571,1.),(0.,0.013702704196865,
0.0319729764593517),.UNSPECIFIED.) ;
#999=B_SPLINE_SURFACE_WITH_KNOTS('',3,3,((#78380,#78381,#78382,#78383,#78384),
(#78385,#78386,#78387,#78388,#78389),(#78390,#78391,#78392,#78393,#78394),
(#78395,#78396,#78397,#78398,#78399),(#78400,#78401,#78402,#78403,#78404),
(#78405,#78406,#78407,#78408,#78409)),.UNSPECIFIED.,.F.,.F.,.F.,(4,1,1,
4),(4,1,4),(0.,0.285714285714286,0.571428571428571,1.),(1.29610738810862E-16,
0.0182702569606054,0.0319729496810593),.UNSPECIFIED.) ;
#1169=FACE_BOUND('',#5787,.T.) ;
#1465=B_SPLINE_CURVE_WITH_KNOTS('',3,(#73267,#73268,#73269,#73270,#73271,
#73272,#73273,#73274,#73275,#73276,#73277,#73278,#73279,#73280,#73281,#73282,
#73283,#73284,#73285,#73286,#73287,#73288,#73289,#73290,#73291,#73292,#73293,
#73294,#73295,#73296),.UNSPECIFIED.,.F.,.F.,(4,2,2,2,2,2,2,2,2,2,2,2,2,
2,4),(5.38322315691615,5.39304224466059,5.44283774773947,5.49094177554178,
5.54078719639314,5.58893137971754,5.63882779437621,5.68701378651527,5.73696225957411,
5.78519165817847,5.83519324032231,5.88346758749165,5.93352331326918,5.96001227251581,
5.9859643020004),.UNSPECIFIED.) ;
#1466=B_SPLINE_CURVE_WITH_KNOTS('',3,(#73298,#73299,#73300,#73301,#73302,
#73303,#73304,#73305,#73306,#73307,#73308,#73309,#73310,#73311,#73312,#73313,
#73314,#73315,#73316,#73317),.UNSPECIFIED.,.F.,.F.,(4,2,2,2,2,2,2,2,2,4),
(7.31782604883876E-6,0.0263666176495937,0.037553661598818,0.0425964016162713,
0.0454386289948368,0.047407628077252,0.0492660600371864,0.0517020860709678,
0.0562207204627482,0.0621887848993301),.UNSPECIFIED.) ;
#1467=B_SPLINE_CURVE_WITH_KNOTS('',3,(#73337,#73338,#73339,#73340,#73341,
#73342,#73343,#73344,#73345,#73346,#73347,#73348,#73349,#73350,#73351,#73352,
#73353,#73354,#73355,#73356,#73357,#73358,#73359,#73360,#73361,#73362,#73363,
#73364,#73365,#73366,#73367,#73368,#73369,#73370,#73371,#73372),
 .UNSPECIFIED.,.F.,.F.,(4,2,2,2,2,2,2,2,2,2,2,2,2,2,2,2,2,4),(4.60003021189608,
4.61274167729195,4.66217697523756,4.71002576797143,4.75950232363626,4.80737612312307,
4.85689499325532,4.90479586715314,4.95435812268451,5.00228809284381,5.05189481547456,
5.09985585554143,5.14950813428105,5.19750216765418,5.24720109538024,5.29522999351585,
5.3449766636052,5.38322315691615),.UNSPECIFIED.) ;
#1468=B_SPLINE_CURVE_WITH_KNOTS('',3,(#73373,#73374,#73375,#73376,#73377,
#73378,#73379,#73380,#73381,#73382,#73383,#73384,#73385,#73386,#73387,#73388,
#73389,#73390,#73391,#73392,#73393,#73394,#73395,#73396,#73397,#73398,#73399,
#73400,#73401,#73402,#73403,#73404,#73405,#73406,#73407,#73408),
 .UNSPECIFIED.,.F.,.F.,(4,2,2,2,2,2,2,2,2,2,2,2,2,2,2,2,2,4),(9.99999999529826E-7,
0.0459602279933998,0.0920695348905101,0.139957279080918,0.189615634502391,
0.237441516424779,0.287034114948666,0.334798867035155,0.384326339251411,
0.432030727703635,0.481493727813977,0.529138554079275,0.578537760391974,
0.626123862656481,0.675459978011906,0.722988232703908,0.772261984819088,
0.778702098235824),.UNSPECIFIED.) ;
#1469=B_SPLINE_CURVE_WITH_KNOTS('',3,(#73413,#73414,#73415,#73416,#73417,
#73418,#73419,#73420,#73421,#73422,#73423,#73424,#73425,#73426,#73427,#73428,
#73429,#73430,#73431,#73432,#73433,#73434,#73435,#73436,#73437,#73438,#73439,
#73440,#73441,#73442,#73443,#73444,#73445,#73446,#73447,#73448),
 .UNSPECIFIED.,.F.,.F.,(4,2,2,2,2,2,2,2,2,2,2,2,2,2,2,2,2,4),(3.81988880202525,
3.83647397316643,3.88561458706625,3.9333421952396,3.98251645873818,4.03025128324564,
4.07946004725098,4.12720439576857,4.17644854178362,4.22420470701037,4.27348514691473,
4.32125540179386,4.37057307694049,4.41835967007874,4.46771554978086,4.5155207011067,
4.56491578059664,4.60003021189608),.UNSPECIFIED.) ;
#1470=B_SPLINE_CURVE_WITH_KNOTS('',3,(#73449,#73450,#73451,#73452,#73453,
#73454,#73455,#73456,#73457,#73458,#73459,#73460,#73461,#73462,#73463,#73464,
#73465,#73466,#73467,#73468,#73469,#73470,#73471,#73472,#73473,#73474,#73475,
#73476,#73477,#73478,#73479,#73480,#73481,#73482,#73483,#73484),
 .UNSPECIFIED.,.F.,.F.,(4,2,2,2,2,2,2,2,2,2,2,2,2,2,2,2,2,4),(0.778702098235824,
0.819733360806915,0.868945565724245,0.916360975939174,0.965512348499289,
1.01287278482948,1.06196412844517,1.10927063523921,1.1583027785071,1.20555644572237,
1.25453024216171,1.30173220673077,1.35064853435815,1.39779998148816,1.44665974221353,
1.49376190660287,1.54256602543321,1.55035468946618),.UNSPECIFIED.) ;
#1471=B_SPLINE_CURVE_WITH_KNOTS('',3,(#73489,#73490,#73491,#73492,#73493,
#73494,#73495,#73496,#73497,#73498,#73499,#73500,#73501,#73502,#73503,#73504,
#73505,#73506,#73507,#73508,#73509,#73510,#73511,#73512,#73513,#73514,#73515,
#73516,#73517,#73518,#73519,#73520,#73521,#73522,#73523,#73524),
 .UNSPECIFIED.,.F.,.F.,(4,2,2,2,2,2,2,2,2,2,2,2,2,2,2,2,2,4),(3.04133107078369,
3.0626282680782,3.11152720317147,3.15928030527985,3.20820694674183,3.25594886385393,
3.30490390645472,3.35263688694587,3.40162102871175,3.44934734517854,3.49836129357941,
3.54608323836105,3.59512771579646,3.64284759626698,3.69192334477632,3.73964347845932,
3.78875126360541,3.81988880202525),.UNSPECIFIED.) ;
#1472=B_SPLINE_CURVE_WITH_KNOTS('',3,(#73525,#73526,#73527,#73528,#73529,
#73530,#73531,#73532,#73533,#73534,#73535,#73536,#73537,#73538,#73539,#73540,
#73541,#73542,#73543,#73544,#73545,#73546,#73547,#73548,#73549,#73550,#73551,
#73552,#73553,#73554,#73555,#73556,#73557,#73558,#73559,#73560),
 .UNSPECIFIED.,.F.,.F.,(4,2,2,2,2,2,2,2,2,2,2,2,2,2,2,2,2,4),(1.55035468946618,
1.58962019238811,1.63836961642577,1.6853771228589,1.73407282008343,1.78103505537499,
1.82967801319886,1.87659641990022,1.92518764349159,1.97206371785068,2.02060422821941,
2.06743952050657,2.1159303523536,2.16272646696657,2.21116866630124,2.2579272616282,
2.30632188316308,2.31615270446751),.UNSPECIFIED.) ;
#1473=B_SPLINE_CURVE_WITH_KNOTS('',3,(#73565,#73566,#73567,#73568,#73569,
#73570,#73571,#73572,#73573,#73574,#73575,#73576,#73577,#73578,#73579,#73580,
#73581,#73582,#73583,#73584,#73585,#73586,#73587,#73588,#73589,#73590,#73591,
#73592,#73593,#73594,#73595,#73596,#73597,#73598,#73599,#73600),
 .UNSPECIFIED.,.F.,.F.,(4,2,2,2,2,2,2,2,2,2,2,2,2,2,2,2,2,4),(2.26324251216357,
2.2896302179728,2.33849886420532,2.38628348179271,2.43512592494221,2.48292857175856,
2.5317455424296,2.5795683258518,2.62836058194701,2.67620556889162,2.7249739108993,
2.77284340349392,2.82158867422688,2.86948464897585,2.91820773434636,2.96598983399257,
3.014861761022,3.04133107078369),.UNSPECIFIED.) ;
#1474=B_SPLINE_CURVE_WITH_KNOTS('',3,(#73601,#73602,#73603,#73604,#73605,
#73606,#73607,#73608,#73609,#73610,#73611,#73612,#73613,#73614,#73615,#73616,
#73617,#73618,#73619,#73620,#73621,#73622,#73623,#73624,#73625,#73626,#73627,
#73628,#73629,#73630,#73631,#73632,#73633,#73634,#73635,#73636),
 .UNSPECIFIED.,.F.,.F.,(4,2,2,2,2,2,2,2,2,2,2,2,2,2,2,2,2,4),(2.31615270446751,
2.35304467118319,2.40139277552237,2.44808152112438,2.49638417176711,2.54304069176822,
2.59129895195733,2.63792511380657,2.68614004325833,2.73273776341155,2.78091041497174,
2.82838060378041,2.87561838875644,2.92303320166402,2.97026178624372,3.01762223630918,
3.06484368446366,3.07757844456771),.UNSPECIFIED.) ;
#1475=B_SPLINE_CURVE_WITH_KNOTS('',3,(#73641,#73642,#73643,#73644,#73645,
#73646,#73647,#73648,#73649,#73650,#73651,#73652,#73653,#73654,#73655,#73656,
#73657,#73658,#73659,#73660,#73661,#73662,#73663,#73664,#73665,#73666,#73667,
#73668,#73669,#73670,#73671,#73672,#73673,#73674,#73675,#73676),
 .UNSPECIFIED.,.F.,.F.,(4,2,2,2,2,2,2,2,2,2,2,2,2,2,2,2,2,4),(1.4846964099853,
1.5157609729567,1.56486470780561,1.61258494268306,1.66165674452716,1.70937703638255,
1.75841766745033,1.80614033275151,1.85515053221796,1.90287787662182,1.95185836460461,
1.9995926780924,2.04854416046925,2.09628771266648,2.14521088665979,2.19296592239185,
2.24186148284303,2.26324251216357),.UNSPECIFIED.) ;
#1476=B_SPLINE_CURVE_WITH_KNOTS('',3,(#73677,#73678,#73679,#73680,#73681,
#73682,#73683,#73684,#73685,#73686,#73687,#73688,#73689,#73690,#73691,#73692,
#73693,#73694,#73695,#73696,#73697,#73698,#73699,#73700,#73701,#73702,#73703,
#73704,#73705,#73706,#73707,#73708,#73709,#73710,#73711,#73712),
 .UNSPECIFIED.,.F.,.F.,(4,2,2,2,2,2,2,2,2,2,2,2,2,2,2,2,2,4),(3.07757844456771,
3.11215082170642,3.15936717543428,3.20662208779349,3.25383536010487,3.30103917439352,
3.34825134234439,3.39540522519537,3.44261822307777,3.48972338187794,3.53693909467871,
3.58399677848582,3.63121703572986,3.67822853616582,3.72545510626173,3.7724217583735,
3.81965634357723,3.83617648296158),.UNSPECIFIED.) ;
#1477=B_SPLINE_CURVE_WITH_KNOTS('',3,(#73717,#73718,#73719,#73720,#73721,
#73722,#73723,#73724,#73725,#73726,#73727,#73728,#73729,#73730,#73731,#73732,
#73733,#73734,#73735,#73736,#73737,#73738,#73739,#73740,#73741,#73742,#73743,
#73744,#73745,#73746,#73747,#73748,#73749,#73750,#73751,#73752),
 .UNSPECIFIED.,.F.,.F.,(4,2,2,2,2,2,2,2,2,2,2,2,2,2,2,2,2,4),(0.704588249065147,
0.739643318471497,0.789033378547931,0.836836191747535,0.886187186262916,
0.933971736098218,0.983284656960893,1.03105316744818,1.08032898034688,1.12808370361566,
1.17732334604404,1.22506655796113,1.27427093778155,1.32200493334144,1.37117492796903,
1.41890201649186,1.46803847277299,1.4846964099853),.UNSPECIFIED.) ;
#1478=B_SPLINE_CURVE_WITH_KNOTS('',3,(#73753,#73754,#73755,#73756,#73757,
#73758,#73759,#73760,#73761,#73762,#73763,#73764,#73765,#73766,#73767,#73768,
#73769,#73770,#73771,#73772,#73773,#73774,#73775,#73776,#73777,#73778,#73779,
#73780,#73781,#73782,#73783,#73784,#73785,#73786,#73787,#73788),
 .UNSPECIFIED.,.F.,.F.,(4,2,2,2,2,2,2,2,2,2,2,2,2,2,2,2,2,4),(3.83617648296158,
3.86657952665484,3.91382375876177,3.96070489710061,4.00796033396756,4.05480089755955,
4.10206902054539,4.14887052568134,4.1961527380787,4.24291674784165,4.29021437435275,
4.33694249897978,4.38425678626683,4.43095068335512,4.4782828016714,4.5249441762026,
4.57229522208415,4.59332517121579),.UNSPECIFIED.) ;
#1479=B_SPLINE_CURVE_WITH_KNOTS('',3,(#73795,#73796,#73797,#73798,#73799,
#73800,#73801,#73802,#73803,#73804,#73805,#73806,#73807,#73808,#73809,#73810,
#73811,#73812,#73813,#73814,#73815,#73816,#73817,#73818,#73819,#73820,#73821,
#73822,#73823,#73824,#73825,#73826,#73827,#73828),.UNSPECIFIED.,.F.,.F.,
(4,2,2,2,2,2,2,2,2,2,2,2,2,2,2,2,4),(9.99999993491271E-7,0.0284828516056796,
0.0574221916505215,0.107115030582226,0.155104747126672,0.204751083061182,
0.252708060286527,0.302308985786131,0.350235153921418,0.399791757223437,
0.447689096492581,0.497202458062411,0.545072996594067,0.594544185668009,
0.64238999705136,0.691820068232682,0.704588249065147),.UNSPECIFIED.) ;
#1480=B_SPLINE_CURVE_WITH_KNOTS('',3,(#73829,#73830,#73831,#73832,#73833,
#73834,#73835,#73836,#73837,#73838,#73839,#73840,#73841,#73842,#73843,#73844,
#73845,#73846,#73847,#73848,#73849,#73850,#73851,#73852,#73853,#73854,#73855,
#73856,#73857,#73858,#73859,#73860,#73861,#73862,#73863,#73864),
 .UNSPECIFIED.,.F.,.F.,(4,2,2,2,2,2,2,2,2,2,2,2,2,2,2,2,2,4),(4.59332517121579,
4.61892582624069,4.66629682621224,4.71289845895872,4.76029037418151,4.80686488058551,
4.85427861235024,4.90082788261854,4.94826427856474,4.99479032010428,5.04225019170015,
5.08875518358285,5.13623929546219,5.18272525768414,5.23023433896211,5.27670333178905,
5.32423808711373,5.35005945872097),.UNSPECIFIED.) ;
#1481=B_SPLINE_CURVE_WITH_KNOTS('',3,(#73870,#73871,#73872,#73873,#73874,
#73875,#73876,#73877,#73878,#73879,#73880,#73881,#73882,#73883,#73884,#73885,
#73886,#73887,#73888,#73889,#73890,#73891,#73892,#73893),.UNSPECIFIED.,
 .F.,.F.,(4,2,2,2,2,2,2,2,2,2,2,4),(-0.691228479706931,-0.659683515426214,
-0.590402494363344,-0.522681206763571,-0.453350201583115,-0.385661106476045,
-0.316279606507643,-0.248618200834772,-0.179185758627054,-0.111547513813486,
-0.0554456429886268,-9.99999999917733E-7),.UNSPECIFIED.) ;
#1482=B_SPLINE_CURVE_WITH_KNOTS('',3,(#73896,#73897,#73898,#73899,#73900,
#73901,#73902,#73903,#73904,#73905,#73906,#73907,#73908,#73909,#73910,#73911,
#73912,#73913,#73914,#73915),.UNSPECIFIED.,.F.,.F.,(4,2,2,2,2,2,2,2,2,4),
(-7.84378181003724,-7.77919511183515,-7.71433746063211,-7.64677308418302,
-7.57667425155804,-7.50915779735907,-7.43912043216624,-7.37164984836796,
-7.30167321308063,-7.29122091273785),.UNSPECIFIED.) ;
#1483=B_SPLINE_CURVE_WITH_KNOTS('',3,(#73920,#73921,#73922,#73923,#73924,
#73925,#73926,#73927,#73928,#73929,#73930,#73931,#73932,#73933,#73934,#73935,
#73936,#73937,#73938,#73939,#73940,#73941,#73942,#73943,#73944,#73945,#73946,
#73947,#73948,#73949,#73950,#73951,#73952,#73953,#73954,#73955),
 .UNSPECIFIED.,.F.,.F.,(4,2,2,2,2,2,2,2,2,2,2,2,2,2,2,2,2,4),(-1.79728453555456,
-1.75567547618576,-1.68676294920706,-1.61863137912338,-1.54967710328783,
-1.4816103119917,-1.41261273732186,-1.34460723868831,-1.27556498377158,
-1.20761709837854,-1.13852894357061,-1.07063481440011,-1.00149969247415,
-0.93365530296354,-0.864472282250888,-0.796673228266311,-0.727441500680126,
-0.691228479706931),.UNSPECIFIED.) ;
#1484=B_SPLINE_CURVE_WITH_KNOTS('',3,(#73956,#73957,#73958,#73959,#73960,
#73961,#73962,#73963,#73964,#73965,#73966,#73967,#73968,#73969,#73970,#73971,
#73972,#73973,#73974,#73975,#73976,#73977,#73978,#73979,#73980,#73981,#73982,
#73983,#73984,#73985,#73986,#73987,#73988,#73989,#73990,#73991),
 .UNSPECIFIED.,.F.,.F.,(4,2,2,2,2,2,2,2,2,2,2,2,2,2,2,2,2,4),(-7.29122091273785,
-7.23424621011276,-7.16432944604514,-7.09694378135534,-7.02708629245721,
-6.95973951256943,-6.88994058993847,-6.82263007226313,-6.75288902505584,
-6.68561199296562,-6.61592815258376,-6.54868167254206,-6.47905439657241,
-6.4118353764163,-6.34226405216014,-6.27506924073054,-6.20555328814192,
-6.18915326500312),.UNSPECIFIED.) ;
#1485=B_SPLINE_CURVE_WITH_KNOTS('',3,(#73996,#73997,#73998,#73999,#74000,
#74001,#74002,#74003,#74004,#74005,#74006,#74007,#74008,#74009,#74010,#74011,
#74012,#74013,#74014,#74015,#74016,#74017,#74018,#74019,#74020,#74021,#74022,
#74023,#74024,#74025,#74026,#74027,#74028,#74029,#74030,#74031),
 .UNSPECIFIED.,.F.,.F.,(4,2,2,2,2,2,2,2,2,2,2,2,2,2,2,2,2,4),(-2.90409970887492,
-2.85344626473094,-2.78479167510497,-2.71604260957267,-2.64736463458598,
-2.57870028926952,-2.50999611763196,-2.44141479173892,-2.37268173758173,
-2.30418150908912,-2.23541702550073,-2.16699574561677,-2.0981974363858,
-2.02985272627047,-1.96101835549974,-1.89274760547224,-1.82387510477095,
-1.79728453555456),.UNSPECIFIED.) ;
#1486=B_SPLINE_CURVE_WITH_KNOTS('',3,(#74032,#74033,#74034,#74035,#74036,
#74037,#74038,#74039,#74040,#74041,#74042,#74043,#74044,#74045,#74046,#74047,
#74048,#74049,#74050,#74051,#74052,#74053,#74054,#74055,#74056,#74057,#74058,
#74059,#74060,#74061,#74062,#74063,#74064,#74065,#74066,#74067),
 .UNSPECIFIED.,.F.,.F.,(4,2,2,2,2,2,2,2,2,2,2,2,2,2,2,2,2,4),(-6.18915326500312,
-6.13837927645232,-6.06891815029146,-6.00176137441837,-5.93235456541957,
-5.86521131128223,-5.79585834613613,-5.72872475630891,-5.65942519626852,
-5.59229727893649,-5.52305071687626,-5.45592435700272,-5.3867304127907,
-5.31960138551605,-5.2504596996016,-5.1833236858355,-5.1142339110082,-5.08964542517064),
 .UNSPECIFIED.) ;
#1487=B_SPLINE_CURVE_WITH_KNOTS('',3,(#74072,#74073,#74074,#74075,#74076,
#74077,#74078,#74079,#74080,#74081,#74082,#74083,#74084,#74085,#74086,#74087,
#74088,#74089,#74090,#74091,#74092,#74093,#74094,#74095,#74096,#74097,#74098,
#74099,#74100,#74101,#74102,#74103,#74104,#74105,#74106,#74107),
 .UNSPECIFIED.,.F.,.F.,(4,2,2,2,2,2,2,2,2,2,2,2,2,2,2,2,2,4),(-4.01310959987262,
-3.95710163714007,-3.88680966073369,-3.81734501486128,-3.74876820198224,
-3.6793951062838,-3.61081675511574,-3.54153490121183,-3.47295177522944,
-3.40376072516744,-3.33516959884117,-3.26606877167578,-3.19746644656107,
-3.128455104976,-3.05983842638392,-2.99091566358799,-2.92228153757466,-2.90409970887492),
 .UNSPECIFIED.) ;
#1488=B_SPLINE_CURVE_WITH_KNOTS('',3,(#74108,#74109,#74110,#74111,#74112,
#74113,#74114,#74115,#74116,#74117,#74118,#74119,#74120,#74121,#74122,#74123,
#74124,#74125,#74126,#74127,#74128,#74129,#74130,#74131,#74132,#74133,#74134,
#74135,#74136,#74137,#74138,#74139,#74140,#74141,#74142,#74143),
 .UNSPECIFIED.,.F.,.F.,(4,2,2,2,2,2,2,2,2,2,2,2,2,2,2,2,2,4),(-5.08964542517064,
-5.0470865151152,-4.97804830645332,-4.91088507586657,-4.8418980789635,-4.77471452549557,
-4.70577836312752,-4.63856998568399,-4.56968424315711,-4.50244655150175,
-4.43361076098885,-4.36633930016088,-4.29755292440106,-4.2302432993488,
-4.16150571513528,-4.09415361510854,-4.02546409653717,-3.9911154034222),
 .UNSPECIFIED.) ;
#1489=B_SPLINE_CURVE_WITH_KNOTS('',3,(#74148,#74149,#74150,#74151,#74152,
#74153,#74154,#74155,#74156,#74157,#74158,#74159,#74160,#74161,#74162,#74163,
#74164,#74165,#74166,#74167,#74168,#74169,#74170,#74171,#74172,#74173,#74174,
#74175,#74176,#74177,#74178,#74179,#74180,#74181,#74182,#74183),
 .UNSPECIFIED.,.F.,.F.,(4,2,2,2,2,2,2,2,2,2,2,2,2,2,2,2,2,4),(-5.12619780738417,
-5.06542824424112,-4.99464397936999,-4.92649998313525,-4.85577983905526,
-4.78768784617287,-4.71703108666039,-4.64898928292674,-4.57839516608918,
-4.51040161405816,-4.43986939573268,-4.37192202842994,-4.3014509658916,
-4.23354758073747,-4.16313693667261,-4.09527518973588,-4.02492423641919,
-4.01310959987262),.UNSPECIFIED.) ;
#1490=B_SPLINE_CURVE_WITH_KNOTS('',3,(#74184,#74185,#74186,#74187,#74188,
#74189,#74190,#74191,#74192,#74193,#74194,#74195,#74196,#74197,#74198,#74199,
#74200,#74201,#74202,#74203,#74204,#74205,#74206,#74207,#74208,#74209,#74210,
#74211,#74212,#74213,#74214,#74215,#74216,#74217,#74218,#74219),
 .UNSPECIFIED.,.F.,.F.,(4,2,2,2,2,2,2,2,2,2,2,2,2,2,2,2,2,4),(-3.9911154034222,
-3.95806517212602,-3.88942286249412,-3.82211773010324,-3.75332596539371,
-3.68605851423656,-3.61721727138992,-3.54998309857507,-3.48109184883234,
-3.41388649428363,-3.34494477649593,-3.27776374758436,-3.20877115196306,
-3.14160994787275,-3.07256610042072,-3.0054202358165,-2.93632478380748,
-2.89252148335294),.UNSPECIFIED.) ;
#1491=B_SPLINE_CURVE_WITH_KNOTS('',3,(#74224,#74225,#74226,#74227,#74228,
#74229,#74230,#74231,#74232,#74233,#74234,#74235,#74236,#74237,#74238,#74239,
#74240,#74241,#74242,#74243,#74244,#74245,#74246,#74247,#74248,#74249,#74250,
#74251,#74252,#74253,#74254,#74255,#74256,#74257,#74258,#74259),
 .UNSPECIFIED.,.F.,.F.,(4,2,2,2,2,2,2,2,2,2,2,2,2,2,2,2,2,4),(-6.24525857708354,
-6.18130123341136,-6.10997902666339,-6.0413663967305,-5.97011370244159,
-5.90156390629546,-5.83038011470152,-5.76189210067836,-5.69077658140171,
-5.6223492228121,-5.5513013256323,-5.48293341540393,-5.41195247130259,-5.34364271637003,
-5.27272803887387,-5.2044750543344,-5.13362594117844,-5.12619780738417),
 .UNSPECIFIED.) ;
#1492=B_SPLINE_CURVE_WITH_KNOTS('',3,(#74260,#74261,#74262,#74263,#74264,
#74265,#74266,#74267,#74268,#74269,#74270,#74271,#74272,#74273,#74274,#74275,
#74276,#74277,#74278,#74279,#74280,#74281,#74282,#74283,#74284,#74285,#74286,
#74287,#74288,#74289,#74290,#74291,#74292,#74293,#74294,#74295),
 .UNSPECIFIED.,.F.,.F.,(4,2,2,2,2,2,2,2,2,2,2,2,2,2,2,2,2,4),(-2.89252148335294,
-2.86918981140948,-2.80004241021797,-2.73291394193786,-2.66371424344966,
-2.59658796980102,-2.52733561255909,-2.46020732011817,-2.3909019212844,
-2.32376750804314,-2.25440865718688,-2.18726414570545,-2.1178514003682,
-2.05069294869569,-1.98122583162893,-1.91404974201738,-1.8445277399499,
-1.7927676458979),.UNSPECIFIED.) ;
#1493=B_SPLINE_CURVE_WITH_KNOTS('',3,(#74300,#74301,#74302,#74303,#74304,
#74305,#74306,#74307,#74308,#74309,#74310,#74311,#74312,#74313,#74314,#74315,
#74316,#74317,#74318,#74319,#74320,#74321,#74322,#74323,#74324,#74325,#74326,
#74327,#74328,#74329,#74330,#74331,#74332,#74333,#74334,#74335),
 .UNSPECIFIED.,.F.,.F.,(4,2,2,2,2,2,2,2,2,2,2,2,2,2,2,2,2,4),(-7.3718042771804,
-7.30571575682601,-7.23381805398239,-7.16467234115743,-7.09284826442791,
-7.02377165232048,-6.95202076013123,-6.88301263647231,-6.81133446730259,
-6.7423941780996,-6.67078824995235,-6.6019150962137,-6.53038090617178,-6.46157414039527,
-6.39011116428207,-6.3213699866964,-6.24997767886145,-6.24525857708354),
 .UNSPECIFIED.) ;
#1494=B_SPLINE_CURVE_WITH_KNOTS('',3,(#74336,#74337,#74338,#74339,#74340,
#74341,#74342,#74343,#74344,#74345,#74346,#74347,#74348,#74349,#74350,#74351,
#74352,#74353,#74354,#74355,#74356,#74357,#74358,#74359,#74360,#74361,#74362,
#74363,#74364,#74365,#74366,#74367,#74368,#74369,#74370,#74371),
 .UNSPECIFIED.,.F.,.F.,(4,2,2,2,2,2,2,2,2,2,2,2,2,2,2,2,2,4),(-1.7927676458979,
-1.77733046543547,-1.70775302919658,-1.64053117816249,-1.57089772396895,
-1.5036480628367,-1.43395797454286,-1.3666774287613,-1.29693006087219,-1.22961571438907,
-1.1598103956439,-1.09245948905149,-1.02259552639848,-0.955205453945968,
-0.885282136746782,-0.817850442406927,-0.747867046729006,-0.690191867186042),
 .UNSPECIFIED.) ;
#1495=B_SPLINE_CURVE_WITH_KNOTS('',3,(#74374,#74375,#74376,#74377,#74378,
#74379,#74380,#74381,#74382,#74383,#74384,#74385,#74386,#74387,#74388,#74389,
#74390,#74391,#74392,#74393,#74394,#74395,#74396,#74397),.UNSPECIFIED.,
 .F.,.F.,(4,2,2,2,2,2,2,2,2,2,2,4),(-0.690191867186042,-0.680391433697344,
-0.610347328058405,-0.54282569448384,-0.472720039614924,-0.405150264626143,
-0.334982321666482,-0.267362495862928,-0.197131528611868,-0.129459864241514,
-0.0646142531593531,-9.99996274231307E-7),.UNSPECIFIED.) ;
#1496=B_SPLINE_CURVE_WITH_KNOTS('',3,(#74401,#74402,#74403,#74404,#74405,
#74406,#74407,#74408,#74409,#74410,#74411,#74412),.UNSPECIFIED.,.F.,.F.,
(4,2,2,2,2,4),(0.,0.0447884204369107,0.0556867274581508,0.0578926554125182,
0.0592288520665145,0.0597188515297013),.UNSPECIFIED.) ;
#1497=B_SPLINE_CURVE_WITH_KNOTS('',3,(#74413,#74414,#74415,#74416,#74417,
#74418,#74419,#74420,#74421,#74422,#74423,#74424,#74425,#74426,#74427,#74428,
#74429,#74430),.UNSPECIFIED.,.F.,.F.,(4,2,2,2,2,2,2,2,4),(-7.81395263639748,
-7.77230563804403,-7.72971205369717,-7.65759101326273,-7.58823469740948,
-7.5161884943611,-7.44690289514721,-7.37493114396469,-7.3718042771804),
 .UNSPECIFIED.) ;
#1498=B_SPLINE_CURVE_WITH_KNOTS('',3,(#74433,#74434,#74435,#74436),
 .UNSPECIFIED.,.F.,.F.,(4,4),(5.35005945872097,5.36908038653652),
 .UNSPECIFIED.) ;
#1499=B_SPLINE_CURVE_WITH_KNOTS('',3,(#74466,#74467,#74468,#74469,#74470,
#74471),.UNSPECIFIED.,.F.,.F.,(4,2,4),(0.,0.0343987133118532,0.0362588513985796),
 .UNSPECIFIED.) ;
#1500=B_SPLINE_CURVE_WITH_KNOTS('',3,(#74472,#74473,#74474,#74475,#74476,
#74477),.UNSPECIFIED.,.F.,.F.,(4,2,4),(-0.0362588513985796,-0.0343987133118532,
0.),.UNSPECIFIED.) ;
#1501=B_SPLINE_CURVE_WITH_KNOTS('',3,(#74499,#74500,#74501,#74502),
 .UNSPECIFIED.,.F.,.F.,(4,4),(-0.00945665398132608,0.),.UNSPECIFIED.) ;
#1502=B_SPLINE_CURVE_WITH_KNOTS('',3,(#74505,#74506,#74507,#74508,#74509,
#74510,#74511,#74512),.UNSPECIFIED.,.F.,.F.,(4,2,2,4),(0.,0.00451226188197751,
0.00913764751162957,0.00945665398132608),.UNSPECIFIED.) ;
#1503=B_SPLINE_CURVE_WITH_KNOTS('',3,(#74541,#74542,#74543,#74544,#74545),
 .UNSPECIFIED.,.F.,.F.,(4,1,4),(-0.00954394271160891,-0.0040902611621181,
0.),.UNSPECIFIED.) ;
#1504=B_SPLINE_CURVE_WITH_KNOTS('',3,(#74546,#74547,#74548,#74549,#74550),
 .UNSPECIFIED.,.F.,.F.,(4,1,4),(0.,0.0040902611621181,0.00954394271160891),
 .UNSPECIFIED.) ;
#1505=B_SPLINE_CURVE_WITH_KNOTS('',3,(#74653,#74654,#74655,#74656,#74657,
#74658,#74659,#74660),.UNSPECIFIED.,.F.,.F.,(4,2,2,4),(-8.07088867651252E-5,
0.00669596786608275,0.0128600360749486,0.0167125787054897),
 .UNSPECIFIED.) ;
#1506=B_SPLINE_CURVE_WITH_KNOTS('',3,(#74685,#74686,#74687,#74688),
 .UNSPECIFIED.,.F.,.F.,(4,4),(0.107090369358838,0.113521242067949),
 .UNSPECIFIED.) ;
#1507=B_SPLINE_CURVE_WITH_KNOTS('',3,(#74734,#74735,#74736,#74737,#74738,
#74739,#74740,#74741,#74742,#74743,#74744,#74745,#74746,#74747,#74748,#74749,
#74750,#74751,#74752,#74753),.UNSPECIFIED.,.F.,.F.,(4,2,2,2,2,2,2,2,2,4),
(-0.189691985209992,-0.186922819341822,-0.184515948817362,-0.184153653473652,
-0.18260925271764,-0.181384487605481,-0.18103834187196,-0.180692196138438,
-0.180346050404917,-0.179999904671396),.UNSPECIFIED.) ;
#1508=B_SPLINE_CURVE_WITH_KNOTS('',3,(#74779,#74780,#74781,#74782,#74783,
#74784),.UNSPECIFIED.,.F.,.F.,(4,2,4),(0.,0.0343987133118529,0.0362588513985796),
 .UNSPECIFIED.) ;
#1509=B_SPLINE_CURVE_WITH_KNOTS('',3,(#74792,#74793,#74794,#74795,#74796,
#74797),.UNSPECIFIED.,.F.,.F.,(4,2,4),(-0.00186013808672611,0.,0.0343987133118504),
 .UNSPECIFIED.) ;
#1510=B_SPLINE_CURVE_WITH_KNOTS('',3,(#74804,#74805,#74806,#74807,#74808,
#74809),.UNSPECIFIED.,.F.,.F.,(4,2,4),(-0.00186013808672659,0.,0.0343987133118501),
 .UNSPECIFIED.) ;
#1511=B_SPLINE_CURVE_WITH_KNOTS('',3,(#74820,#74821,#74822,#74823,#74824),
 .UNSPECIFIED.,.F.,.F.,(4,1,4),(0.,0.00545368154943955,0.00954394271151922),
 .UNSPECIFIED.) ;
#1512=B_SPLINE_CURVE_WITH_KNOTS('',3,(#74852,#74853,#74854,#74855,#74856,
#74857),.UNSPECIFIED.,.F.,.F.,(4,2,4),(-0.0343987133118501,0.,0.00186013808672659),
 .UNSPECIFIED.) ;
#1513=B_SPLINE_CURVE_WITH_KNOTS('',3,(#74880,#74881,#74882,#74883),
 .UNSPECIFIED.,.F.,.F.,(4,4),(-0.00945665401173728,-7.96865975725692E-14),
 .UNSPECIFIED.) ;
#1514=B_SPLINE_CURVE_WITH_KNOTS('',3,(#74884,#74885,#74886,#74887,#74888,
#74889),.UNSPECIFIED.,.F.,.F.,(4,2,4),(7.96865975725692E-14,0.0047494858717794,
0.00945665401173728),.UNSPECIFIED.) ;
#1515=B_SPLINE_CURVE_WITH_KNOTS('',3,(#74917,#74918,#74919,#74920,#74921),
 .UNSPECIFIED.,.F.,.F.,(4,1,4),(-0.00954394271151922,-0.00545368154943955,
0.),.UNSPECIFIED.) ;
#1516=B_SPLINE_CURVE_WITH_KNOTS('',3,(#74992,#74993,#74994,#74995,#74996,
#74997,#74998,#74999,#75000,#75001,#75002,#75003,#75004,#75005,#75006,#75007,
#75008,#75009,#75010,#75011,#75012,#75013),.UNSPECIFIED.,.F.,.F.,(4,2,2,
2,2,2,2,2,2,2,4),(0.,0.00178735894887589,0.00328754343915599,0.00522227948307641,
0.00581324616239635,0.0066458744035453,0.00954455547535216,0.00985052209277086,
0.0134309724899257,0.0160797277273677,0.0167952489709647),.UNSPECIFIED.) ;
#1517=B_SPLINE_CURVE_WITH_KNOTS('',3,(#75041,#75042,#75043,#75044),
 .UNSPECIFIED.,.F.,.F.,(4,4),(0.11352033938527,0.119949480178501),
 .UNSPECIFIED.) ;
#1518=B_SPLINE_CURVE_WITH_KNOTS('',3,(#75091,#75092,#75093,#75094,#75095,
#75096,#75097,#75098,#75099,#75100,#75101,#75102,#75103,#75104,#75105,#75106,
#75107,#75108,#75109,#75110),.UNSPECIFIED.,.F.,.F.,(4,2,2,2,2,2,2,2,2,4),
(-0.179997619857109,-0.179651531266927,-0.179305442676744,-0.178959354086561,
-0.178613265496379,-0.177069119697205,-0.175844556774918,-0.173438083587768,
-0.170813788147114,-0.170307139331997),.UNSPECIFIED.) ;
#1519=B_SPLINE_CURVE_WITH_KNOTS('',3,(#75124,#75125,#75126,#75127,#75128),
 .UNSPECIFIED.,.F.,.F.,(4,1,4),(0.,0.013702704196865,0.0319729764593517),
 .UNSPECIFIED.) ;
#1520=B_SPLINE_CURVE_WITH_KNOTS('',3,(#75155,#75156,#75157,#75158,#75159,
#75160),.UNSPECIFIED.,.F.,.F.,(4,2,4),(-0.0362588513985796,-0.0343987133118529,
0.),.UNSPECIFIED.) ;
#1521=B_SPLINE_CURVE_WITH_KNOTS('',3,(#75182,#75183,#75184,#75185),
 .UNSPECIFIED.,.F.,.F.,(4,4),(-0.00945665398132565,0.),.UNSPECIFIED.) ;
#1522=B_SPLINE_CURVE_WITH_KNOTS('',3,(#75188,#75189,#75190,#75191,#75192,
#75193,#75194,#75195),.UNSPECIFIED.,.F.,.F.,(4,2,2,4),(0.,0.00451226188133782,
0.00913764751100092,0.00945665398132565),.UNSPECIFIED.) ;
#1523=B_SPLINE_CURVE_WITH_KNOTS('',3,(#75224,#75225,#75226,#75227,#75228),
 .UNSPECIFIED.,.F.,.F.,(4,1,4),(-0.00954394271160956,-0.00409026116211842,
-5.7658280050909E-17),.UNSPECIFIED.) ;
#1524=B_SPLINE_CURVE_WITH_KNOTS('',3,(#75229,#75230,#75231,#75232,#75233),
 .UNSPECIFIED.,.F.,.F.,(4,1,4),(5.7658280050909E-17,0.00409026116211842,
0.00954394271160956),.UNSPECIFIED.) ;
#1525=B_SPLINE_CURVE_WITH_KNOTS('',3,(#75309,#75310,#75311,#75312,#75313,
#75314,#75315,#75316,#75317,#75318,#75319,#75320,#75321,#75322,#75323,#75324,
#75325,#75326,#75327,#75328,#75329,#75330,#75331,#75332,#75333,#75334,#75335,
#75336,#75337,#75338,#75339,#75340,#75341,#75342,#75343,#75344,#75345,#75346,
#75347,#75348,#75349,#75350,#75351,#75352,#75353,#75354,#75355,#75356,#75357,
#75358,#75359,#75360,#75361,#75362,#75363,#75364,#75365,#75366,#75367,#75368,
#75369),.UNSPECIFIED.,.F.,.F.,(4,3,3,3,3,3,3,3,3,3,3,3,3,3,3,3,3,3,3,3,
4),(-8.09857184636461E-5,0.000317028515094856,0.000374632195319235,0.000383937353632409,
0.000450354935360417,0.000627468486635104,0.00133592269173385,0.00275283110193136,
0.00369743670872969,0.00519672563943589,0.00605516800959267,0.00669601457014209,
0.00784471646450152,0.00899341835886094,0.00962565333192913,0.0112908221475798,
0.0128600542553739,0.0133505813712207,0.0152272244608216,0.0162383352828185,
0.0167125790586438),.UNSPECIFIED.) ;
#1526=B_SPLINE_CURVE_WITH_KNOTS('',3,(#75394,#75395,#75396,#75397),
 .UNSPECIFIED.,.F.,.F.,(4,4),(0.107092094291284,0.11352518691992),
 .UNSPECIFIED.) ;
#1527=B_SPLINE_CURVE_WITH_KNOTS('',3,(#75443,#75444,#75445,#75446,#75447,
#75448,#75449,#75450,#75451,#75452,#75453,#75454,#75455,#75456,#75457,#75458,
#75459,#75460),.UNSPECIFIED.,.F.,.F.,(4,2,2,2,2,2,2,2,4),(-0.189691985209994,
-0.186989953236899,-0.185538236407738,-0.183626840293631,-0.182769070539567,
-0.181384487605482,-0.180692196138439,-0.180346050404917,-0.179999904671396),
 .UNSPECIFIED.) ;
#1528=B_SPLINE_CURVE_WITH_KNOTS('',3,(#75485,#75486,#75487,#75488,#75489),
 .UNSPECIFIED.,.F.,.F.,(4,1,4),(0.,0.00409026116207964,0.00954394271151917),
 .UNSPECIFIED.) ;
#1529=B_SPLINE_CURVE_WITH_KNOTS('',3,(#75517,#75518,#75519,#75520,#75521,
#75522),.UNSPECIFIED.,.F.,.F.,(4,2,4),(-0.0343987133118504,0.,0.00186013808672611),
 .UNSPECIFIED.) ;
#1530=B_SPLINE_CURVE_WITH_KNOTS('',3,(#75545,#75546,#75547,#75548),
 .UNSPECIFIED.,.F.,.F.,(4,4),(-0.00945665401173742,-7.97441283497418E-14),
 .UNSPECIFIED.) ;
#1531=B_SPLINE_CURVE_WITH_KNOTS('',3,(#75549,#75550,#75551,#75552,#75553,
#75554),.UNSPECIFIED.,.F.,.F.,(4,2,4),(7.97441283497418E-14,0.00474948587256806,
0.00945665401173742),.UNSPECIFIED.) ;
#1532=B_SPLINE_CURVE_WITH_KNOTS('',3,(#75582,#75583,#75584,#75585,#75586),
 .UNSPECIFIED.,.F.,.F.,(4,1,4),(-0.00954394271151917,-0.00409026116207964,
0.),.UNSPECIFIED.) ;
#1533=B_SPLINE_CURVE_WITH_KNOTS('',3,(#75657,#75658,#75659,#75660,#75661,
#75662,#75663,#75664,#75665,#75666,#75667,#75668,#75669,#75670,#75671,#75672,
#75673,#75674,#75675,#75676,#75677,#75678),.UNSPECIFIED.,.F.,.F.,(4,2,2,
2,2,2,2,2,2,2,4),(0.,0.00178736671760306,0.00328754690174189,0.00522231021806468,
0.00581324616239624,0.00664590032475465,0.0095446545394002,0.00985058182527603,
0.0134311236465911,0.0160798648246182,0.0167952493652102),.UNSPECIFIED.) ;
#1534=B_SPLINE_CURVE_WITH_KNOTS('',3,(#75706,#75707,#75708,#75709),
 .UNSPECIFIED.,.F.,.F.,(4,4),(0.11353089859696,0.119959972115571),
 .UNSPECIFIED.) ;
#1535=B_SPLINE_CURVE_WITH_KNOTS('',3,(#75756,#75757,#75758,#75759,#75760,
#75761,#75762,#75763,#75764,#75765,#75766,#75767,#75768,#75769,#75770,#75771,
#75772,#75773,#75774,#75775),.UNSPECIFIED.,.F.,.F.,(4,2,2,2,2,2,2,2,2,4),
(-0.179997619857109,-0.179651531266927,-0.179305442676744,-0.178959354086562,
-0.178613265496379,-0.177069119697188,-0.175844556774918,-0.173438083587785,
-0.170813788147149,-0.170307139331997),.UNSPECIFIED.) ;
#1536=B_SPLINE_CURVE_WITH_KNOTS('',3,(#75826,#75827,#75828,#75829,#75830,
#75831),.UNSPECIFIED.,.F.,.F.,(4,2,4),(-0.0364117611345324,-0.0361627499148956,
0.),.UNSPECIFIED.) ;
#1537=B_SPLINE_CURVE_WITH_KNOTS('',3,(#75837,#75838,#75839,#75840),
 .UNSPECIFIED.,.F.,.F.,(4,4),(-0.146371498429592,0.),.UNSPECIFIED.) ;
#1538=B_SPLINE_CURVE_WITH_KNOTS('',3,(#75877,#75878,#75879,#75880,#75881,
#75882),.UNSPECIFIED.,.F.,.F.,(4,2,4),(0.,0.0361627499148956,0.0364117611345324),
 .UNSPECIFIED.) ;
#1539=B_SPLINE_CURVE_WITH_KNOTS('',3,(#75929,#75930,#75931,#75932,#75933,
#75934,#75935,#75936),.UNSPECIFIED.,.F.,.F.,(4,2,2,4),(0.,0.0586623890662813,
0.117369996722224,0.146371498429592),.UNSPECIFIED.) ;
#1540=B_SPLINE_CURVE_WITH_KNOTS('',3,(#75969,#75970,#75971,#75972,#75973,
#75974,#75975,#75976),.UNSPECIFIED.,.F.,.F.,(4,2,2,4),(-0.146371498430696,
-0.0876595232426458,-0.0289914100866822,-8.05248431948221E-13),
 .UNSPECIFIED.) ;
#1541=B_SPLINE_CURVE_WITH_KNOTS('',3,(#75977,#75978,#75979,#75980),
 .UNSPECIFIED.,.F.,.F.,(4,4),(0.,0.146371498430696),.UNSPECIFIED.) ;
#1542=B_SPLINE_CURVE_WITH_KNOTS('',3,(#76037,#76038,#76039,#76040,#76041,
#76042),.UNSPECIFIED.,.F.,.F.,(4,2,4),(8.84614312661979E-17,0.0361913306097799,
0.0364133025372201),.UNSPECIFIED.) ;
#1543=B_SPLINE_CURVE_WITH_KNOTS('',3,(#76043,#76044,#76045,#76046,#76047,
#76048),.UNSPECIFIED.,.F.,.F.,(4,2,4),(-0.0364133025372201,-0.0361913306097799,
-8.84614312661979E-17),.UNSPECIFIED.) ;
#1544=B_SPLINE_CURVE_WITH_KNOTS('',3,(#76132,#76133,#76134,#76135),
 .UNSPECIFIED.,.F.,.F.,(4,4),(-0.146371498429891,0.),.UNSPECIFIED.) ;
#1545=B_SPLINE_CURVE_WITH_KNOTS('',3,(#76136,#76137,#76138,#76139,#76140,
#76141,#76142,#76143),.UNSPECIFIED.,.F.,.F.,(4,2,2,4),(0.,0.0586623890660135,
0.117369996721865,0.146371498429891),.UNSPECIFIED.) ;
#1546=B_SPLINE_CURVE_WITH_KNOTS('',3,(#76200,#76201,#76202,#76203,#76204,
#76205),.UNSPECIFIED.,.F.,.F.,(4,2,4),(0.,0.0361629958429266,0.0364117772057813),
 .UNSPECIFIED.) ;
#1547=B_SPLINE_CURVE_WITH_KNOTS('',3,(#76206,#76207,#76208,#76209,#76210,
#76211),.UNSPECIFIED.,.F.,.F.,(4,2,4),(-0.0364117772057813,-0.0361629958429266,
0.),.UNSPECIFIED.) ;
#1548=B_SPLINE_CURVE_WITH_KNOTS('',3,(#76218,#76219,#76220,#76221,#76222,
#76223),.UNSPECIFIED.,.F.,.F.,(4,2,4),(-0.0364133025382447,-0.0361913306296307,
0.),.UNSPECIFIED.) ;
#1549=B_SPLINE_CURVE_WITH_KNOTS('',3,(#76228,#76229,#76230,#76231,#76232,
#76233,#76234,#76235),.UNSPECIFIED.,.F.,.F.,(4,2,2,4),(-0.146371498429891,
-0.0876595232417657,-0.0289914100858698,0.),.UNSPECIFIED.) ;
#1550=B_SPLINE_CURVE_WITH_KNOTS('',3,(#76272,#76273,#76274,#76275),
 .UNSPECIFIED.,.F.,.F.,(4,4),(0.,0.146371498429891),.UNSPECIFIED.) ;
#1551=B_SPLINE_CURVE_WITH_KNOTS('',3,(#76329,#76330,#76331,#76332,#76333,
#76334),.UNSPECIFIED.,.F.,.F.,(4,2,4),(0.,0.0361913306296307,0.0364133025382447),
 .UNSPECIFIED.) ;
#1552=B_SPLINE_CURVE_WITH_KNOTS('',3,(#76467,#76468,#76469,#76470,#76471,
#76472,#76473,#76474),.UNSPECIFIED.,.F.,.F.,(4,2,2,4),(-0.00449779612828801,
-0.00440391402779913,-0.00244544984037645,-0.000128411811047494),
 .UNSPECIFIED.) ;
#1553=B_SPLINE_CURVE_WITH_KNOTS('',3,(#76476,#76477,#76478,#76479,#76480,
#76481,#76482,#76483,#76484,#76485),.UNSPECIFIED.,.F.,.F.,(4,2,2,2,4),(-0.326963021080646,
-0.273443015535847,-0.153352882404738,-0.0199317405198332,0.0415869283876659),
 .UNSPECIFIED.) ;
#1554=B_SPLINE_CURVE_WITH_KNOTS('',3,(#76487,#76488,#76489,#76490,#76491,
#76492,#76493),.UNSPECIFIED.,.F.,.F.,(4,3,4),(-0.00528739892062153,-0.00264209583824454,
-1.05158573648755E-5),.UNSPECIFIED.) ;
#1555=B_SPLINE_CURVE_WITH_KNOTS('',3,(#76499,#76500,#76501,#76502,#76503,
#76504,#76505,#76506,#76507,#76508,#76509,#76510,#76511,#76512,#76513,#76514,
#76515,#76516),.UNSPECIFIED.,.F.,.F.,(4,2,2,2,2,2,2,2,4),(0.0199485255308491,
0.0405677462825902,0.0613530454994567,0.0817043692001714,0.100854971904388,
0.119363166385794,0.13699176518755,0.153352882404738,0.153410004281816),
 .UNSPECIFIED.) ;
#1556=B_SPLINE_CURVE_WITH_KNOTS('',3,(#76518,#76519,#76520,#76521,#76522,
#76523,#76524,#76525,#76526,#76527,#76528,#76529,#76530,#76531,#76532,#76533,
#76534,#76535),.UNSPECIFIED.,.F.,.F.,(4,2,2,2,2,2,2,2,4),(0.153410004867272,
0.172771538902472,0.192188682136839,0.210985897145968,0.228496077033556,
0.245368537241394,0.261430894732374,0.273443015535847,0.273454607678092),
 .UNSPECIFIED.) ;
#1557=B_SPLINE_CURVE_WITH_KNOTS('',3,(#76536,#76537,#76538,#76539,#76540,
#76541,#76542,#76543),.UNSPECIFIED.,.F.,.F.,(4,2,2,4),(0.273454609116393,
0.292643022549525,0.310270283905659,0.327829791007539),.UNSPECIFIED.) ;
#1558=B_SPLINE_CURVE_WITH_KNOTS('',3,(#76545,#76546,#76547,#76548,#76549,
#76550,#76551,#76552,#76553,#76554,#76555,#76556,#76557,#76558,#76559,#76560,
#76561,#76562),.UNSPECIFIED.,.F.,.F.,(4,2,2,2,2,2,2,2,4),(1.00000407856514E-6,
0.0270461031048522,0.0463717419686661,0.0669688246402426,0.0808296434149286,
0.0869444645666349,0.0890594351739109,0.0898799261523484,0.0905817008981732),
 .UNSPECIFIED.) ;
#1559=B_SPLINE_CURVE_WITH_KNOTS('',3,(#76565,#76566,#76567,#76568,#76569,
#76570,#76571,#76572,#76573,#76574,#76575,#76576,#76577,#76578,#76579,#76580,
#76581,#76582,#76583,#76584,#76585,#76586,#76587,#76588,#76589,#76590,#76591,
#76592,#76593,#76594,#76595,#76596,#76597,#76598),.UNSPECIFIED.,.F.,.F.,
(4,3,3,3,3,3,3,3,3,3,3,4),(-0.015771486666387,-0.0156499135546454,-0.0132688478173875,
-0.0120178036343787,-0.0117138282636781,-0.00932822941246477,-0.00780237427572918,
-0.00542308690722213,-0.00451600742544575,-0.00389905627547958,-0.00151468045248576,
0.),.UNSPECIFIED.) ;
#1560=B_SPLINE_CURVE_WITH_KNOTS('',3,(#76669,#76670,#76671,#76672,#76673,
#76674,#76675,#76676,#76677,#76678,#76679,#76680),.UNSPECIFIED.,.F.,.F.,
(4,2,2,2,2,4),(0.000180857407629647,0.00793560140118584,0.0125099257471543,
0.0143669747674358,0.0151422884351474,0.015668827114255),.UNSPECIFIED.) ;
#1561=B_SPLINE_CURVE_WITH_KNOTS('',3,(#76682,#76683,#76684,#76685),
 .UNSPECIFIED.,.F.,.F.,(4,4),(5.47634473919011E-6,0.094453216066185),
 .UNSPECIFIED.) ;
#1562=B_SPLINE_CURVE_WITH_KNOTS('',3,(#76687,#76688,#76689,#76690,#76691,
#76692),.UNSPECIFIED.,.F.,.F.,(4,2,4),(0.094453216066185,0.094503731574,
0.215053629751941),.UNSPECIFIED.) ;
#1563=B_SPLINE_CURVE_WITH_KNOTS('',3,(#76696,#76697,#76698,#76699,#76700,
#76701,#76702,#76703,#76704,#76705),.UNSPECIFIED.,.F.,.F.,(4,2,2,2,4),(-0.408276645255811,
-0.349022909463275,-0.215144182724569,-0.094503731574,-0.0393180761061371),
 .UNSPECIFIED.) ;
#1564=B_SPLINE_CURVE_WITH_KNOTS('',3,(#77286,#77287,#77288,#77289,#77290,
#77291,#77292,#77293,#77294,#77295,#77296,#77297),.UNSPECIFIED.,.F.,.F.,
(4,2,2,2,2,4),(-0.10355030182359,-0.0894083769331069,-0.0705862367589278,
-0.0476572871556061,-0.0284912878296623,-9.99964373940782E-7),
 .UNSPECIFIED.) ;
#1565=B_SPLINE_CURVE_WITH_KNOTS('',3,(#77409,#77410,#77411,#77412),
 .UNSPECIFIED.,.F.,.F.,(4,4),(0.00294758963503899,0.0306076446211308),
 .UNSPECIFIED.) ;
#1566=B_SPLINE_CURVE_WITH_KNOTS('',3,(#77414,#77415,#77416,#77417,#77418,
#77419),.UNSPECIFIED.,.F.,.F.,(4,2,4),(-0.000233218663520837,0.,0.00294758963503899),
 .UNSPECIFIED.) ;
#1567=B_SPLINE_CURVE_WITH_KNOTS('',3,(#77508,#77509,#77510,#77511),
 .UNSPECIFIED.,.F.,.F.,(4,4),(-0.0306076446211308,-0.00287612766258956),
 .UNSPECIFIED.) ;
#1568=B_SPLINE_CURVE_WITH_KNOTS('',3,(#77512,#77513,#77514,#77515,#77516,
#77517),.UNSPECIFIED.,.F.,.F.,(4,2,4),(-0.00287612766258956,0.,0.000233218663520837),
 .UNSPECIFIED.) ;
#1569=B_SPLINE_CURVE_WITH_KNOTS('',3,(#77895,#77896,#77897,#77898),
 .UNSPECIFIED.,.F.,.F.,(4,4),(0.0029475896360751,0.0306076446211596),
 .UNSPECIFIED.) ;
#1570=B_SPLINE_CURVE_WITH_KNOTS('',3,(#77900,#77901,#77902,#77903,#77904,
#77905),.UNSPECIFIED.,.F.,.F.,(4,2,4),(-0.0002332186634917,0.,0.0029475896360751),
 .UNSPECIFIED.) ;
#1571=B_SPLINE_CURVE_WITH_KNOTS('',3,(#77994,#77995,#77996,#77997),
 .UNSPECIFIED.,.F.,.F.,(4,4),(-0.0306076446211596,-0.00287612766194185),
 .UNSPECIFIED.) ;
#1572=B_SPLINE_CURVE_WITH_KNOTS('',3,(#77998,#77999,#78000,#78001,#78002,
#78003),.UNSPECIFIED.,.F.,.F.,(4,2,4),(-0.00287612766194185,0.,0.0002332186634917),
 .UNSPECIFIED.) ;
#1573=B_SPLINE_CURVE_WITH_KNOTS('',3,(#78199,#78200,#78201,#78202,#78203),
 .UNSPECIFIED.,.F.,.F.,(4,1,4),(1.29610738810862E-16,0.0182702569606054,
0.0319729496810593),.UNSPECIFIED.) ;
#1574=B_SPLINE_CURVE_WITH_KNOTS('',3,(#78280,#78281,#78282,#78283),
 .UNSPECIFIED.,.F.,.F.,(4,4),(0.,0.0319729496810593),.UNSPECIFIED.) ;
#1575=B_SPLINE_CURVE_WITH_KNOTS('',3,(#78317,#78318,#78319,#78320),
 .UNSPECIFIED.,.F.,.F.,(4,4),(0.,0.0319729764593517),.UNSPECIFIED.) ;
#1576=B_SPLINE_CURVE_WITH_KNOTS('',3,(#78358,#78359,#78360,#78361,#78362,
#78363,#78364,#78365,#78366,#78367,#78368,#78369,#78370,#78371,#78372,#78373),
 .UNSPECIFIED.,.F.,.F.,(4,2,2,2,2,2,2,4),(-0.0319729764593517,-0.026487794895197,
-0.0210191260320854,-0.0155681323168053,-0.013702704196865,-0.00853358219385316,
-0.00336875022758298,0.),.UNSPECIFIED.) ;
#1577=B_SPLINE_CURVE_WITH_KNOTS('',3,(#78412,#78413,#78414,#78415,#78416,
#78417,#78418,#78419,#78420,#78421,#78422,#78423,#78424,#78425,#78426,#78427),
 .UNSPECIFIED.,.F.,.F.,(4,2,2,2,2,2,2,4),(-0.0319729496810593,-0.0268019298577068,
-0.0216243054581297,-0.0182702569606054,-0.0128223821098292,-0.00736410383994217,
-0.00188441434238895,-1.29610738810862E-16),.UNSPECIFIED.) ;
#1578=B_SPLINE_CURVE_WITH_KNOTS('',3,(#78437,#78438,#78439,#78440,#78441,
#78442,#78443,#78444,#78445,#78446,#78447,#78448,#78449,#78450,#78451,#78452,
#78453,#78454,#78455,#78456),.UNSPECIFIED.,.F.,.F.,(4,2,2,2,2,2,2,2,2,4),
(2.44073605373652,2.65599013224616,2.99553615799378,3.69719379632858,4.0424469091546,
4.7496870461374,5.56463964981499,6.33322372310358,6.72166834008255,7.2429082378436),
 .UNSPECIFIED.) ;
#1579=B_SPLINE_CURVE_WITH_KNOTS('',3,(#78460,#78461,#78462,#78463,#78464,
#78465,#78466,#78467,#78468,#78469,#78470,#78471,#78472,#78473,#78474,#78475,
#78476,#78477,#78478,#78479,#78480,#78481,#78482,#78483),.UNSPECIFIED.,
 .F.,.F.,(4,2,2,2,2,2,2,2,2,2,2,4),(0.,0.046946185965169,0.0949502462023891,
0.166325664716851,0.266616518174325,0.400158134448206,0.59170384360669,
0.83908927216011,1.1747465058088,1.58388496113465,2.07198027474184,2.44073605373652),
 .UNSPECIFIED.) ;
#2148=PLANE('',#35531) ;
#2149=PLANE('',#35555) ;
#2150=PLANE('',#35569) ;
#2151=PLANE('',#35591) ;
#2152=PLANE('',#35600) ;
#2153=PLANE('',#35634) ;
#2154=PLANE('',#35643) ;
#2155=PLANE('',#35655) ;
#2156=PLANE('',#35665) ;
#2157=PLANE('',#35680) ;
#2158=PLANE('',#35696) ;
#2159=PLANE('',#35699) ;
#2160=PLANE('',#35717) ;
#2161=PLANE('',#35745) ;
#2162=PLANE('',#35748) ;
#2163=PLANE('',#35775) ;
#2164=PLANE('',#35791) ;
#2165=PLANE('',#35794) ;
#2166=PLANE('',#35814) ;
#2167=PLANE('',#35822) ;
#2168=PLANE('',#35843) ;
#2169=PLANE('',#35844) ;
#2170=PLANE('',#35864) ;
#2171=PLANE('',#35867) ;
#2172=PLANE('',#35901) ;
#3624=FACE_OUTER_BOUND('',#5681,.T.) ;
#3625=FACE_OUTER_BOUND('',#5682,.T.) ;
#3626=FACE_OUTER_BOUND('',#5683,.T.) ;
#3627=FACE_OUTER_BOUND('',#5684,.T.) ;
#3628=FACE_OUTER_BOUND('',#5685,.T.) ;
#3629=FACE_OUTER_BOUND('',#5686,.T.) ;
#3630=FACE_OUTER_BOUND('',#5687,.T.) ;
#3631=FACE_OUTER_BOUND('',#5688,.T.) ;
#3632=FACE_OUTER_BOUND('',#5689,.T.) ;
#3633=FACE_OUTER_BOUND('',#5690,.T.) ;
#3634=FACE_OUTER_BOUND('',#5691,.T.) ;
#3635=FACE_OUTER_BOUND('',#5692,.T.) ;
#3636=FACE_OUTER_BOUND('',#5693,.T.) ;
#3637=FACE_OUTER_BOUND('',#5694,.T.) ;
#3638=FACE_OUTER_BOUND('',#5695,.T.) ;
#3639=FACE_OUTER_BOUND('',#5696,.T.) ;
#3640=FACE_OUTER_BOUND('',#5697,.T.) ;
#3641=FACE_OUTER_BOUND('',#5698,.T.) ;
#3642=FACE_OUTER_BOUND('',#5699,.T.) ;
#3643=FACE_OUTER_BOUND('',#5700,.T.) ;
#3644=FACE_OUTER_BOUND('',#5701,.T.) ;
#3645=FACE_OUTER_BOUND('',#5702,.T.) ;
#3646=FACE_OUTER_BOUND('',#5703,.T.) ;
#3647=FACE_OUTER_BOUND('',#5704,.T.) ;
#3648=FACE_OUTER_BOUND('',#5705,.T.) ;
#3649=FACE_OUTER_BOUND('',#5706,.T.) ;
#3650=FACE_OUTER_BOUND('',#5707,.T.) ;
#3651=FACE_OUTER_BOUND('',#5708,.T.) ;
#3652=FACE_OUTER_BOUND('',#5709,.T.) ;
#3653=FACE_OUTER_BOUND('',#5710,.T.) ;
#3654=FACE_OUTER_BOUND('',#5711,.T.) ;
#3655=FACE_OUTER_BOUND('',#5712,.T.) ;
#3656=FACE_OUTER_BOUND('',#5713,.T.) ;
#3657=FACE_OUTER_BOUND('',#5714,.T.) ;
#3658=FACE_OUTER_BOUND('',#5715,.T.) ;
#3659=FACE_OUTER_BOUND('',#5716,.T.) ;
#3660=FACE_OUTER_BOUND('',#5717,.T.) ;
#3661=FACE_OUTER_BOUND('',#5718,.T.) ;
#3662=FACE_OUTER_BOUND('',#5719,.T.) ;
#3663=FACE_OUTER_BOUND('',#5720,.T.) ;
#3664=FACE_OUTER_BOUND('',#5721,.T.) ;
#3665=FACE_OUTER_BOUND('',#5722,.T.) ;
#3666=FACE_OUTER_BOUND('',#5723,.T.) ;
#3667=FACE_OUTER_BOUND('',#5724,.T.) ;
#3668=FACE_OUTER_BOUND('',#5725,.T.) ;
#3669=FACE_OUTER_BOUND('',#5726,.T.) ;
#3670=FACE_OUTER_BOUND('',#5727,.T.) ;
#3671=FACE_OUTER_BOUND('',#5728,.T.) ;
#3672=FACE_OUTER_BOUND('',#5729,.T.) ;
#3673=FACE_OUTER_BOUND('',#5730,.T.) ;
#3674=FACE_OUTER_BOUND('',#5731,.T.) ;
#3675=FACE_OUTER_BOUND('',#5732,.T.) ;
#3676=FACE_OUTER_BOUND('',#5733,.T.) ;
#3677=FACE_OUTER_BOUND('',#5734,.T.) ;
#3678=FACE_OUTER_BOUND('',#5735,.T.) ;
#3679=FACE_OUTER_BOUND('',#5736,.T.) ;
#3680=FACE_OUTER_BOUND('',#5737,.T.) ;
#3681=FACE_OUTER_BOUND('',#5738,.T.) ;
#3682=FACE_OUTER_BOUND('',#5739,.T.) ;
#3683=FACE_OUTER_BOUND('',#5740,.T.) ;
#3684=FACE_OUTER_BOUND('',#5741,.T.) ;
#3685=FACE_OUTER_BOUND('',#5742,.T.) ;
#3686=FACE_OUTER_BOUND('',#5743,.T.) ;
#3687=FACE_OUTER_BOUND('',#5744,.T.) ;
#3688=FACE_OUTER_BOUND('',#5745,.T.) ;
#3689=FACE_OUTER_BOUND('',#5746,.T.) ;
#3690=FACE_OUTER_BOUND('',#5747,.T.) ;
#3691=FACE_OUTER_BOUND('',#5748,.T.) ;
#3692=FACE_OUTER_BOUND('',#5749,.T.) ;
#3693=FACE_OUTER_BOUND('',#5750,.T.) ;
#3694=FACE_OUTER_BOUND('',#5751,.T.) ;
#3695=FACE_OUTER_BOUND('',#5752,.T.) ;
#3696=FACE_OUTER_BOUND('',#5753,.T.) ;
#3697=FACE_OUTER_BOUND('',#5754,.T.) ;
#3698=FACE_OUTER_BOUND('',#5755,.T.) ;
#3699=FACE_OUTER_BOUND('',#5756,.T.) ;
#3700=FACE_OUTER_BOUND('',#5757,.T.) ;
#3701=FACE_OUTER_BOUND('',#5758,.T.) ;
#3702=FACE_OUTER_BOUND('',#5759,.T.) ;
#3703=FACE_OUTER_BOUND('',#5760,.T.) ;
#3704=FACE_OUTER_BOUND('',#5761,.T.) ;
#3705=FACE_OUTER_BOUND('',#5762,.T.) ;
#3706=FACE_OUTER_BOUND('',#5763,.T.) ;
#3707=FACE_OUTER_BOUND('',#5764,.T.) ;
#3708=FACE_OUTER_BOUND('',#5765,.T.) ;
#3709=FACE_OUTER_BOUND('',#5766,.T.) ;
#3710=FACE_OUTER_BOUND('',#5767,.T.) ;
#3711=FACE_OUTER_BOUND('',#5768,.T.) ;
#3712=FACE_OUTER_BOUND('',#5769,.T.) ;
#3713=FACE_OUTER_BOUND('',#5770,.T.) ;
#3714=FACE_OUTER_BOUND('',#5771,.T.) ;
#3715=FACE_OUTER_BOUND('',#5772,.T.) ;
#3716=FACE_OUTER_BOUND('',#5773,.T.) ;
#3717=FACE_OUTER_BOUND('',#5774,.T.) ;
#3718=FACE_OUTER_BOUND('',#5775,.T.) ;
#3719=FACE_OUTER_BOUND('',#5776,.T.) ;
#3720=FACE_OUTER_BOUND('',#5777,.T.) ;
#3721=FACE_OUTER_BOUND('',#5778,.T.) ;
#3722=FACE_OUTER_BOUND('',#5779,.T.) ;
#3723=FACE_OUTER_BOUND('',#5780,.T.) ;
#3724=FACE_OUTER_BOUND('',#5781,.T.) ;
#3725=FACE_OUTER_BOUND('',#5782,.T.) ;
#3726=FACE_OUTER_BOUND('',#5783,.T.) ;
#3727=FACE_OUTER_BOUND('',#5784,.T.) ;
#3728=FACE_OUTER_BOUND('',#5785,.T.) ;
#3729=FACE_OUTER_BOUND('',#5786,.T.) ;
#3730=FACE_OUTER_BOUND('',#5788,.T.) ;
#3731=FACE_OUTER_BOUND('',#5789,.T.) ;
#3732=FACE_OUTER_BOUND('',#5790,.T.) ;
#3733=FACE_OUTER_BOUND('',#5791,.T.) ;
#3734=FACE_OUTER_BOUND('',#5792,.T.) ;
#3735=FACE_OUTER_BOUND('',#5793,.T.) ;
#3736=FACE_OUTER_BOUND('',#5794,.T.) ;
#3737=FACE_OUTER_BOUND('',#5795,.T.) ;
#3738=FACE_OUTER_BOUND('',#5796,.T.) ;
#3739=FACE_OUTER_BOUND('',#5797,.T.) ;
#3740=FACE_OUTER_BOUND('',#5798,.T.) ;
#3741=FACE_OUTER_BOUND('',#5799,.T.) ;
#3742=FACE_OUTER_BOUND('',#5800,.T.) ;
#3743=FACE_OUTER_BOUND('',#5801,.T.) ;
#3744=FACE_OUTER_BOUND('',#5802,.T.) ;
#3745=FACE_OUTER_BOUND('',#5803,.T.) ;
#3746=FACE_OUTER_BOUND('',#5804,.T.) ;
#3747=FACE_OUTER_BOUND('',#5805,.T.) ;
#3748=FACE_OUTER_BOUND('',#5806,.T.) ;
#3749=FACE_OUTER_BOUND('',#5807,.T.) ;
#3750=FACE_OUTER_BOUND('',#5808,.T.) ;
#3751=FACE_OUTER_BOUND('',#5809,.T.) ;
#3752=FACE_OUTER_BOUND('',#5810,.T.) ;
#3753=FACE_OUTER_BOUND('',#5811,.T.) ;
#3754=FACE_OUTER_BOUND('',#5812,.T.) ;
#3755=FACE_OUTER_BOUND('',#5813,.T.) ;
#3756=FACE_OUTER_BOUND('',#5814,.T.) ;
#3757=FACE_OUTER_BOUND('',#5815,.T.) ;
#3758=FACE_OUTER_BOUND('',#5816,.T.) ;
#3759=FACE_OUTER_BOUND('',#5817,.T.) ;
#3760=FACE_OUTER_BOUND('',#5818,.T.) ;
#3761=FACE_OUTER_BOUND('',#5819,.T.) ;
#3762=FACE_OUTER_BOUND('',#5820,.T.) ;
#3763=FACE_OUTER_BOUND('',#5821,.T.) ;
#3764=FACE_OUTER_BOUND('',#5822,.T.) ;
#3765=FACE_OUTER_BOUND('',#5823,.T.) ;
#3766=FACE_OUTER_BOUND('',#5824,.T.) ;
#3767=FACE_OUTER_BOUND('',#5825,.T.) ;
#3768=FACE_OUTER_BOUND('',#5826,.T.) ;
#3769=FACE_OUTER_BOUND('',#5827,.T.) ;
#3770=FACE_OUTER_BOUND('',#5828,.T.) ;
#3771=FACE_OUTER_BOUND('',#5829,.T.) ;
#3772=FACE_OUTER_BOUND('',#5830,.T.) ;
#3773=FACE_OUTER_BOUND('',#5831,.T.) ;
#3774=FACE_OUTER_BOUND('',#5832,.T.) ;
#3775=FACE_OUTER_BOUND('',#5833,.T.) ;
#3776=FACE_OUTER_BOUND('',#5834,.T.) ;
#3777=FACE_OUTER_BOUND('',#5835,.T.) ;
#3778=FACE_OUTER_BOUND('',#5836,.T.) ;
#3779=FACE_OUTER_BOUND('',#5837,.T.) ;
#3780=FACE_OUTER_BOUND('',#5838,.T.) ;
#3781=FACE_OUTER_BOUND('',#5839,.T.) ;
#3782=FACE_OUTER_BOUND('',#5840,.T.) ;
#3783=FACE_OUTER_BOUND('',#5841,.T.) ;
#3784=FACE_OUTER_BOUND('',#5842,.T.) ;
#3785=FACE_OUTER_BOUND('',#5843,.T.) ;
#3786=FACE_OUTER_BOUND('',#5844,.T.) ;
#3787=FACE_OUTER_BOUND('',#5845,.T.) ;
#3788=FACE_OUTER_BOUND('',#5846,.T.) ;
#3789=FACE_OUTER_BOUND('',#5847,.T.) ;
#3790=FACE_OUTER_BOUND('',#5848,.T.) ;
#3791=FACE_OUTER_BOUND('',#5849,.T.) ;
#3792=FACE_OUTER_BOUND('',#5850,.T.) ;
#3793=FACE_OUTER_BOUND('',#5851,.T.) ;
#3794=FACE_OUTER_BOUND('',#5852,.T.) ;
#3795=FACE_OUTER_BOUND('',#5853,.T.) ;
#3796=FACE_OUTER_BOUND('',#5854,.T.) ;
#3797=FACE_OUTER_BOUND('',#5855,.T.) ;
#3798=FACE_OUTER_BOUND('',#5856,.T.) ;
#3799=FACE_OUTER_BOUND('',#5857,.T.) ;
#3800=FACE_OUTER_BOUND('',#5858,.T.) ;
#3801=FACE_OUTER_BOUND('',#5859,.T.) ;
#3802=FACE_OUTER_BOUND('',#5860,.T.) ;
#3803=FACE_OUTER_BOUND('',#5861,.T.) ;
#3804=FACE_OUTER_BOUND('',#5862,.T.) ;
#3805=FACE_OUTER_BOUND('',#5863,.T.) ;
#3806=FACE_OUTER_BOUND('',#5864,.T.) ;
#3807=FACE_OUTER_BOUND('',#5865,.T.) ;
#3808=FACE_OUTER_BOUND('',#5866,.T.) ;
#3809=FACE_OUTER_BOUND('',#5867,.T.) ;
#3810=FACE_OUTER_BOUND('',#5868,.T.) ;
#3811=FACE_OUTER_BOUND('',#5869,.T.) ;
#3812=FACE_OUTER_BOUND('',#5870,.T.) ;
#3813=FACE_OUTER_BOUND('',#5871,.T.) ;
#3814=FACE_OUTER_BOUND('',#5872,.T.) ;
#3815=FACE_OUTER_BOUND('',#5873,.T.) ;
#3816=FACE_OUTER_BOUND('',#5874,.T.) ;
#3817=FACE_OUTER_BOUND('',#5875,.T.) ;
#3818=FACE_OUTER_BOUND('',#5876,.T.) ;
#3819=FACE_OUTER_BOUND('',#5877,.T.) ;
#3820=FACE_OUTER_BOUND('',#5878,.T.) ;
#3821=FACE_OUTER_BOUND('',#5879,.T.) ;
#3822=FACE_OUTER_BOUND('',#5880,.T.) ;
#3823=FACE_OUTER_BOUND('',#5881,.T.) ;
#3824=FACE_OUTER_BOUND('',#5882,.T.) ;
#3825=FACE_OUTER_BOUND('',#5883,.T.) ;
#3826=FACE_OUTER_BOUND('',#5884,.T.) ;
#3827=FACE_OUTER_BOUND('',#5885,.T.) ;
#3828=FACE_OUTER_BOUND('',#5886,.T.) ;
#3829=FACE_OUTER_BOUND('',#5887,.T.) ;
#3830=FACE_OUTER_BOUND('',#5888,.T.) ;
#3831=FACE_OUTER_BOUND('',#5889,.T.) ;
#3832=FACE_OUTER_BOUND('',#5890,.T.) ;
#3833=FACE_OUTER_BOUND('',#5891,.T.) ;
#3834=FACE_OUTER_BOUND('',#5892,.T.) ;
#3835=FACE_OUTER_BOUND('',#5893,.T.) ;
#3836=FACE_OUTER_BOUND('',#5894,.T.) ;
#3837=FACE_OUTER_BOUND('',#5895,.T.) ;
#3838=FACE_OUTER_BOUND('',#5896,.T.) ;
#3839=FACE_OUTER_BOUND('',#5897,.T.) ;
#3840=FACE_OUTER_BOUND('',#5898,.T.) ;
#3841=FACE_OUTER_BOUND('',#5899,.T.) ;
#3842=FACE_OUTER_BOUND('',#5900,.T.) ;
#3843=FACE_OUTER_BOUND('',#5901,.T.) ;
#3844=FACE_OUTER_BOUND('',#5902,.T.) ;
#3845=FACE_OUTER_BOUND('',#5903,.T.) ;
#3846=FACE_OUTER_BOUND('',#5904,.T.) ;
#3847=FACE_OUTER_BOUND('',#5905,.T.) ;
#3848=FACE_OUTER_BOUND('',#5906,.T.) ;
#3849=FACE_OUTER_BOUND('',#5907,.T.) ;
#3850=FACE_OUTER_BOUND('',#5908,.T.) ;
#3851=FACE_OUTER_BOUND('',#5909,.T.) ;
#3852=FACE_OUTER_BOUND('',#5910,.T.) ;
#5681=EDGE_LOOP('',(#27364,#27365,#27366,#27367)) ;
#5682=EDGE_LOOP('',(#27368,#27369,#27370,#27371)) ;
#5683=EDGE_LOOP('',(#27372,#27373,#27374,#27375)) ;
#5684=EDGE_LOOP('',(#27376,#27377,#27378,#27379)) ;
#5685=EDGE_LOOP('',(#27380,#27381,#27382,#27383)) ;
#5686=EDGE_LOOP('',(#27384,#27385,#27386,#27387)) ;
#5687=EDGE_LOOP('',(#27388,#27389,#27390,#27391)) ;
#5688=EDGE_LOOP('',(#27392,#27393,#27394,#27395,#27396)) ;
#5689=EDGE_LOOP('',(#27397,#27398,#27399,#27400)) ;
#5690=EDGE_LOOP('',(#27401,#27402,#27403,#27404)) ;
#5691=EDGE_LOOP('',(#27405,#27406,#27407,#27408)) ;
#5692=EDGE_LOOP('',(#27409,#27410,#27411,#27412)) ;
#5693=EDGE_LOOP('',(#27413,#27414,#27415,#27416)) ;
#5694=EDGE_LOOP('',(#27417,#27418,#27419,#27420)) ;
#5695=EDGE_LOOP('',(#27421,#27422,#27423,#27424)) ;
#5696=EDGE_LOOP('',(#27425,#27426,#27427,#27428,#27429)) ;
#5697=EDGE_LOOP('',(#27430,#27431,#27432)) ;
#5698=EDGE_LOOP('',(#27433,#27434,#27435)) ;
#5699=EDGE_LOOP('',(#27436,#27437,#27438,#27439)) ;
#5700=EDGE_LOOP('',(#27440,#27441,#27442,#27443)) ;
#5701=EDGE_LOOP('',(#27444,#27445,#27446,#27447)) ;
#5702=EDGE_LOOP('',(#27448,#27449,#27450)) ;
#5703=EDGE_LOOP('',(#27451,#27452,#27453,#27454)) ;
#5704=EDGE_LOOP('',(#27455,#27456,#27457,#27458)) ;
#5705=EDGE_LOOP('',(#27459,#27460,#27461)) ;
#5706=EDGE_LOOP('',(#27462,#27463,#27464,#27465,#27466,#27467,#27468,#27469,
#27470,#27471,#27472,#27473,#27474,#27475,#27476,#27477)) ;
#5707=EDGE_LOOP('',(#27478,#27479,#27480,#27481,#27482,#27483,#27484,#27485)) ;
#5708=EDGE_LOOP('',(#27486,#27487,#27488)) ;
#5709=EDGE_LOOP('',(#27489,#27490,#27491,#27492)) ;
#5710=EDGE_LOOP('',(#27493,#27494,#27495,#27496)) ;
#5711=EDGE_LOOP('',(#27497,#27498,#27499,#27500)) ;
#5712=EDGE_LOOP('',(#27501,#27502,#27503)) ;
#5713=EDGE_LOOP('',(#27504,#27505,#27506,#27507)) ;
#5714=EDGE_LOOP('',(#27508,#27509,#27510,#27511)) ;
#5715=EDGE_LOOP('',(#27512,#27513,#27514,#27515,#27516,#27517)) ;
#5716=EDGE_LOOP('',(#27518,#27519,#27520,#27521,#27522,#27523,#27524,#27525,
#27526)) ;
#5717=EDGE_LOOP('',(#27527,#27528,#27529)) ;
#5718=EDGE_LOOP('',(#27530,#27531,#27532,#27533)) ;
#5719=EDGE_LOOP('',(#27534,#27535,#27536,#27537)) ;
#5720=EDGE_LOOP('',(#27538,#27539,#27540,#27541)) ;
#5721=EDGE_LOOP('',(#27542,#27543,#27544)) ;
#5722=EDGE_LOOP('',(#27545,#27546,#27547,#27548)) ;
#5723=EDGE_LOOP('',(#27549,#27550,#27551,#27552)) ;
#5724=EDGE_LOOP('',(#27553,#27554,#27555)) ;
#5725=EDGE_LOOP('',(#27556,#27557,#27558,#27559,#27560,#27561,#27562,#27563)) ;
#5726=EDGE_LOOP('',(#27564,#27565,#27566)) ;
#5727=EDGE_LOOP('',(#27567,#27568,#27569,#27570)) ;
#5728=EDGE_LOOP('',(#27571,#27572,#27573,#27574)) ;
#5729=EDGE_LOOP('',(#27575,#27576,#27577,#27578)) ;
#5730=EDGE_LOOP('',(#27579,#27580,#27581)) ;
#5731=EDGE_LOOP('',(#27582,#27583,#27584,#27585)) ;
#5732=EDGE_LOOP('',(#27586,#27587,#27588,#27589)) ;
#5733=EDGE_LOOP('',(#27590,#27591,#27592,#27593,#27594,#27595)) ;
#5734=EDGE_LOOP('',(#27596,#27597,#27598,#27599,#27600,#27601,#27602,#27603,
#27604)) ;
#5735=EDGE_LOOP('',(#27605,#27606,#27607)) ;
#5736=EDGE_LOOP('',(#27608,#27609,#27610,#27611)) ;
#5737=EDGE_LOOP('',(#27612,#27613,#27614)) ;
#5738=EDGE_LOOP('',(#27615,#27616,#27617,#27618)) ;
#5739=EDGE_LOOP('',(#27619,#27620,#27621,#27622,#27623)) ;
#5740=EDGE_LOOP('',(#27624,#27625,#27626,#27627)) ;
#5741=EDGE_LOOP('',(#27628,#27629,#27630)) ;
#5742=EDGE_LOOP('',(#27631,#27632,#27633,#27634)) ;
#5743=EDGE_LOOP('',(#27635,#27636,#27637,#27638)) ;
#5744=EDGE_LOOP('',(#27639,#27640,#27641)) ;
#5745=EDGE_LOOP('',(#27642,#27643,#27644)) ;
#5746=EDGE_LOOP('',(#27645,#27646,#27647,#27648)) ;
#5747=EDGE_LOOP('',(#27649,#27650,#27651,#27652)) ;
#5748=EDGE_LOOP('',(#27653,#27654,#27655)) ;
#5749=EDGE_LOOP('',(#27656,#27657,#27658,#27659)) ;
#5750=EDGE_LOOP('',(#27660,#27661,#27662,#27663,#27664)) ;
#5751=EDGE_LOOP('',(#27665,#27666,#27667,#27668)) ;
#5752=EDGE_LOOP('',(#27669,#27670,#27671)) ;
#5753=EDGE_LOOP('',(#27672,#27673,#27674,#27675)) ;
#5754=EDGE_LOOP('',(#27676,#27677,#27678)) ;
#5755=EDGE_LOOP('',(#27679,#27680,#27681,#27682,#27683,#27684)) ;
#5756=EDGE_LOOP('',(#27685,#27686,#27687,#27688)) ;
#5757=EDGE_LOOP('',(#27689,#27690,#27691)) ;
#5758=EDGE_LOOP('',(#27692,#27693,#27694,#27695)) ;
#5759=EDGE_LOOP('',(#27696,#27697,#27698,#27699)) ;
#5760=EDGE_LOOP('',(#27700,#27701,#27702)) ;
#5761=EDGE_LOOP('',(#27703,#27704,#27705,#27706,#27707,#27708)) ;
#5762=EDGE_LOOP('',(#27709,#27710,#27711,#27712)) ;
#5763=EDGE_LOOP('',(#27713,#27714,#27715,#27716)) ;
#5764=EDGE_LOOP('',(#27717,#27718,#27719,#27720)) ;
#5765=EDGE_LOOP('',(#27721,#27722,#27723)) ;
#5766=EDGE_LOOP('',(#27724,#27725,#27726,#27727)) ;
#5767=EDGE_LOOP('',(#27728,#27729,#27730,#27731)) ;
#5768=EDGE_LOOP('',(#27732,#27733,#27734)) ;
#5769=EDGE_LOOP('',(#27735,#27736,#27737,#27738)) ;
#5770=EDGE_LOOP('',(#27739,#27740,#27741,#27742,#27743)) ;
#5771=EDGE_LOOP('',(#27744,#27745,#27746,#27747)) ;
#5772=EDGE_LOOP('',(#27748,#27749,#27750)) ;
#5773=EDGE_LOOP('',(#27751,#27752,#27753,#27754)) ;
#5774=EDGE_LOOP('',(#27755,#27756,#27757)) ;
#5775=EDGE_LOOP('',(#27758,#27759,#27760,#27761,#27762,#27763)) ;
#5776=EDGE_LOOP('',(#27764,#27765,#27766,#27767)) ;
#5777=EDGE_LOOP('',(#27768,#27769,#27770)) ;
#5778=EDGE_LOOP('',(#27771,#27772,#27773,#27774)) ;
#5779=EDGE_LOOP('',(#27775,#27776,#27777)) ;
#5780=EDGE_LOOP('',(#27778,#27779,#27780,#27781,#27782)) ;
#5781=EDGE_LOOP('',(#27783,#27784,#27785,#27786)) ;
#5782=EDGE_LOOP('',(#27787,#27788,#27789,#27790,#27791,#27792,#27793,#27794)) ;
#5783=EDGE_LOOP('',(#27795,#27796,#27797,#27798,#27799)) ;
#5784=EDGE_LOOP('',(#27800,#27801,#27802,#27803,#27804,#27805,#27806,#27807,
#27808,#27809)) ;
#5785=EDGE_LOOP('',(#27810,#27811,#27812,#27813,#27814,#27815,#27816,#27817,
#27818,#27819,#27820,#27821,#27822,#27823,#27824,#27825,#27826,#27827,#27828,
#27829,#27830,#27831,#27832,#27833,#27834)) ;
#5786=EDGE_LOOP('',(#27835)) ;
#5787=EDGE_LOOP('',(#27836,#27837,#27838)) ;
#5788=EDGE_LOOP('',(#27839,#27840,#27841,#27842,#27843,#27844,#27845,#27846,
#27847)) ;
#5789=EDGE_LOOP('',(#27848,#27849,#27850,#27851)) ;
#5790=EDGE_LOOP('',(#27852,#27853,#27854,#27855)) ;
#5791=EDGE_LOOP('',(#27856,#27857,#27858)) ;
#5792=EDGE_LOOP('',(#27859,#27860,#27861,#27862)) ;
#5793=EDGE_LOOP('',(#27863,#27864,#27865,#27866,#27867,#27868,#27869,#27870)) ;
#5794=EDGE_LOOP('',(#27871,#27872,#27873,#27874,#27875,#27876,#27877,#27878)) ;
#5795=EDGE_LOOP('',(#27879,#27880,#27881)) ;
#5796=EDGE_LOOP('',(#27882,#27883,#27884,#27885)) ;
#5797=EDGE_LOOP('',(#27886,#27887,#27888,#27889)) ;
#5798=EDGE_LOOP('',(#27890,#27891,#27892,#27893,#27894)) ;
#5799=EDGE_LOOP('',(#27895,#27896,#27897,#27898,#27899,#27900)) ;
#5800=EDGE_LOOP('',(#27901,#27902,#27903,#27904)) ;
#5801=EDGE_LOOP('',(#27905,#27906,#27907,#27908)) ;
#5802=EDGE_LOOP('',(#27909,#27910,#27911,#27912,#27913,#27914,#27915,#27916)) ;
#5803=EDGE_LOOP('',(#27917,#27918,#27919)) ;
#5804=EDGE_LOOP('',(#27920,#27921,#27922,#27923)) ;
#5805=EDGE_LOOP('',(#27924,#27925,#27926,#27927)) ;
#5806=EDGE_LOOP('',(#27928,#27929,#27930,#27931)) ;
#5807=EDGE_LOOP('',(#27932,#27933,#27934)) ;
#5808=EDGE_LOOP('',(#27935,#27936,#27937)) ;
#5809=EDGE_LOOP('',(#27938,#27939,#27940,#27941)) ;
#5810=EDGE_LOOP('',(#27942,#27943,#27944,#27945)) ;
#5811=EDGE_LOOP('',(#27946,#27947,#27948,#27949,#27950,#27951)) ;
#5812=EDGE_LOOP('',(#27952,#27953,#27954)) ;
#5813=EDGE_LOOP('',(#27955,#27956,#27957,#27958)) ;
#5814=EDGE_LOOP('',(#27959,#27960,#27961,#27962)) ;
#5815=EDGE_LOOP('',(#27963,#27964,#27965)) ;
#5816=EDGE_LOOP('',(#27966,#27967,#27968,#27969)) ;
#5817=EDGE_LOOP('',(#27970,#27971,#27972,#27973)) ;
#5818=EDGE_LOOP('',(#27974,#27975,#27976)) ;
#5819=EDGE_LOOP('',(#27977,#27978,#27979,#27980)) ;
#5820=EDGE_LOOP('',(#27981,#27982,#27983)) ;
#5821=EDGE_LOOP('',(#27984,#27985,#27986)) ;
#5822=EDGE_LOOP('',(#27987,#27988,#27989,#27990)) ;
#5823=EDGE_LOOP('',(#27991,#27992,#27993,#27994)) ;
#5824=EDGE_LOOP('',(#27995,#27996,#27997,#27998,#27999,#28000,#28001,#28002,
#28003)) ;
#5825=EDGE_LOOP('',(#28004,#28005,#28006,#28007,#28008,#28009)) ;
#5826=EDGE_LOOP('',(#28010,#28011,#28012,#28013)) ;
#5827=EDGE_LOOP('',(#28014,#28015,#28016)) ;
#5828=EDGE_LOOP('',(#28017,#28018,#28019,#28020)) ;
#5829=EDGE_LOOP('',(#28021,#28022,#28023,#28024)) ;
#5830=EDGE_LOOP('',(#28025,#28026,#28027)) ;
#5831=EDGE_LOOP('',(#28028,#28029,#28030,#28031)) ;
#5832=EDGE_LOOP('',(#28032,#28033,#28034,#28035)) ;
#5833=EDGE_LOOP('',(#28036,#28037,#28038)) ;
#5834=EDGE_LOOP('',(#28039,#28040,#28041)) ;
#5835=EDGE_LOOP('',(#28042,#28043,#28044,#28045,#28046,#28047)) ;
#5836=EDGE_LOOP('',(#28048,#28049,#28050,#28051,#28052,#28053,#28054,#28055,
#28056)) ;
#5837=EDGE_LOOP('',(#28057,#28058,#28059,#28060)) ;
#5838=EDGE_LOOP('',(#28061,#28062,#28063,#28064)) ;
#5839=EDGE_LOOP('',(#28065,#28066,#28067)) ;
#5840=EDGE_LOOP('',(#28068,#28069,#28070,#28071)) ;
#5841=EDGE_LOOP('',(#28072,#28073,#28074,#28075,#28076,#28077,#28078,#28079)) ;
#5842=EDGE_LOOP('',(#28080,#28081,#28082,#28083,#28084,#28085,#28086,#28087)) ;
#5843=EDGE_LOOP('',(#28088,#28089,#28090)) ;
#5844=EDGE_LOOP('',(#28091,#28092,#28093,#28094)) ;
#5845=EDGE_LOOP('',(#28095,#28096,#28097,#28098)) ;
#5846=EDGE_LOOP('',(#28099,#28100,#28101,#28102,#28103)) ;
#5847=EDGE_LOOP('',(#28104,#28105,#28106,#28107,#28108,#28109)) ;
#5848=EDGE_LOOP('',(#28110,#28111,#28112,#28113)) ;
#5849=EDGE_LOOP('',(#28114,#28115,#28116,#28117)) ;
#5850=EDGE_LOOP('',(#28118,#28119,#28120,#28121,#28122,#28123,#28124,#28125)) ;
#5851=EDGE_LOOP('',(#28126,#28127,#28128,#28129)) ;
#5852=EDGE_LOOP('',(#28130,#28131,#28132)) ;
#5853=EDGE_LOOP('',(#28133,#28134,#28135,#28136)) ;
#5854=EDGE_LOOP('',(#28137,#28138,#28139,#28140)) ;
#5855=EDGE_LOOP('',(#28141,#28142,#28143)) ;
#5856=EDGE_LOOP('',(#28144,#28145,#28146)) ;
#5857=EDGE_LOOP('',(#28147,#28148,#28149,#28150)) ;
#5858=EDGE_LOOP('',(#28151,#28152,#28153,#28154)) ;
#5859=EDGE_LOOP('',(#28155,#28156,#28157,#28158)) ;
#5860=EDGE_LOOP('',(#28159,#28160,#28161,#28162,#28163,#28164)) ;
#5861=EDGE_LOOP('',(#28165,#28166,#28167)) ;
#5862=EDGE_LOOP('',(#28168,#28169,#28170,#28171)) ;
#5863=EDGE_LOOP('',(#28172,#28173,#28174)) ;
#5864=EDGE_LOOP('',(#28175,#28176,#28177,#28178)) ;
#5865=EDGE_LOOP('',(#28179,#28180,#28181,#28182,#28183,#28184)) ;
#5866=EDGE_LOOP('',(#28185,#28186,#28187,#28188)) ;
#5867=EDGE_LOOP('',(#28189,#28190,#28191,#28192)) ;
#5868=EDGE_LOOP('',(#28193,#28194,#28195)) ;
#5869=EDGE_LOOP('',(#28196,#28197,#28198,#28199)) ;
#5870=EDGE_LOOP('',(#28200,#28201,#28202)) ;
#5871=EDGE_LOOP('',(#28203,#28204,#28205)) ;
#5872=EDGE_LOOP('',(#28206,#28207,#28208,#28209)) ;
#5873=EDGE_LOOP('',(#28210,#28211,#28212,#28213)) ;
#5874=EDGE_LOOP('',(#28214,#28215,#28216,#28217,#28218,#28219,#28220,#28221,
#28222)) ;
#5875=EDGE_LOOP('',(#28223,#28224,#28225,#28226)) ;
#5876=EDGE_LOOP('',(#28227,#28228,#28229)) ;
#5877=EDGE_LOOP('',(#28230,#28231,#28232,#28233)) ;
#5878=EDGE_LOOP('',(#28234,#28235,#28236,#28237)) ;
#5879=EDGE_LOOP('',(#28238,#28239,#28240)) ;
#5880=EDGE_LOOP('',(#28241,#28242,#28243,#28244)) ;
#5881=EDGE_LOOP('',(#28245,#28246,#28247,#28248)) ;
#5882=EDGE_LOOP('',(#28249,#28250,#28251,#28252)) ;
#5883=EDGE_LOOP('',(#28253,#28254,#28255,#28256)) ;
#5884=EDGE_LOOP('',(#28257,#28258,#28259,#28260)) ;
#5885=EDGE_LOOP('',(#28261,#28262,#28263,#28264,#28265,#28266)) ;
#5886=EDGE_LOOP('',(#28267,#28268,#28269,#28270,#28271,#28272)) ;
#5887=EDGE_LOOP('',(#28273,#28274,#28275,#28276,#28277,#28278,#28279,#28280,
#28281,#28282,#28283,#28284,#28285,#28286,#28287,#28288,#28289,#28290,#28291,
#28292)) ;
#5888=EDGE_LOOP('',(#28293,#28294,#28295,#28296)) ;
#5889=EDGE_LOOP('',(#28297,#28298,#28299,#28300)) ;
#5890=EDGE_LOOP('',(#28301,#28302,#28303,#28304)) ;
#5891=EDGE_LOOP('',(#28305,#28306,#28307,#28308,#28309,#28310)) ;
#5892=EDGE_LOOP('',(#28311,#28312,#28313,#28314,#28315,#28316)) ;
#5893=EDGE_LOOP('',(#28317,#28318,#28319,#28320)) ;
#5894=EDGE_LOOP('',(#28321,#28322,#28323,#28324,#28325,#28326,#28327,#28328)) ;
#5895=EDGE_LOOP('',(#28329,#28330,#28331,#28332)) ;
#5896=EDGE_LOOP('',(#28333,#28334,#28335,#28336)) ;
#5897=EDGE_LOOP('',(#28337,#28338,#28339,#28340)) ;
#5898=EDGE_LOOP('',(#28341,#28342,#28343,#28344)) ;
#5899=EDGE_LOOP('',(#28345,#28346,#28347,#28348)) ;
#5900=EDGE_LOOP('',(#28349,#28350,#28351,#28352)) ;
#5901=EDGE_LOOP('',(#28353,#28354,#28355,#28356)) ;
#5902=EDGE_LOOP('',(#28357,#28358,#28359,#28360,#28361,#28362)) ;
#5903=EDGE_LOOP('',(#28363,#28364,#28365,#28366,#28367,#28368,#28369,#28370)) ;
#5904=EDGE_LOOP('',(#28371,#28372,#28373,#28374)) ;
#5905=EDGE_LOOP('',(#28375,#28376,#28377,#28378,#28379)) ;
#5906=EDGE_LOOP('',(#28380,#28381,#28382,#28383,#28384,#28385,#28386,#28387,
#28388)) ;
#5907=EDGE_LOOP('',(#28389,#28390,#28391,#28392)) ;
#5908=EDGE_LOOP('',(#28393,#28394,#28395,#28396,#28397,#28398)) ;
#5909=EDGE_LOOP('',(#28399)) ;
#5910=EDGE_LOOP('',(#28400,#28401,#28402,#28403,#28404,#28405,#28406,#28407,
#28408,#28409,#28410,#28411,#28412,#28413,#28414,#28415,#28416,#28417,#28418,
#28419,#28420,#28421)) ;
#8061=LINE('',#73265,#10380) ;
#8062=LINE('',#73336,#10381) ;
#8063=LINE('',#73412,#10382) ;
#8064=LINE('',#73488,#10383) ;
#8065=LINE('',#73564,#10384) ;
#8066=LINE('',#73640,#10385) ;
#8067=LINE('',#73716,#10386) ;
#8068=LINE('',#73792,#10387) ;
#8069=LINE('',#73868,#10388) ;
#8070=LINE('',#73919,#10389) ;
#8071=LINE('',#73995,#10390) ;
#8072=LINE('',#74071,#10391) ;
#8073=LINE('',#74147,#10392) ;
#8074=LINE('',#74223,#10393) ;
#8075=LINE('',#74299,#10394) ;
#8076=LINE('',#74652,#10395) ;
#8077=LINE('',#74684,#10396) ;
#8078=LINE('',#74754,#10397) ;
#8079=LINE('',#75015,#10398) ;
#8080=LINE('',#75038,#10399) ;
#8081=LINE('',#75090,#10400) ;
#8082=LINE('',#75113,#10401) ;
#8083=LINE('',#75116,#10402) ;
#8084=LINE('',#75119,#10403) ;
#8085=LINE('',#75121,#10404) ;
#8086=LINE('',#75308,#10405) ;
#8087=LINE('',#75393,#10406) ;
#8088=LINE('',#75461,#10407) ;
#8089=LINE('',#75680,#10408) ;
#8090=LINE('',#75703,#10409) ;
#8091=LINE('',#75755,#10410) ;
#8092=LINE('',#75778,#10411) ;
#8093=LINE('',#75781,#10412) ;
#8094=LINE('',#75784,#10413) ;
#8095=LINE('',#75786,#10414) ;
#8096=LINE('',#75814,#10415) ;
#8097=LINE('',#75817,#10416) ;
#8098=LINE('',#75835,#10417) ;
#8099=LINE('',#75844,#10418) ;
#8100=LINE('',#76057,#10419) ;
#8101=LINE('',#76058,#10420) ;
#8102=LINE('',#76061,#10421) ;
#8103=LINE('',#76084,#10422) ;
#8104=LINE('',#76090,#10423) ;
#8105=LINE('',#76092,#10424) ;
#8106=LINE('',#76096,#10425) ;
#8107=LINE('',#76100,#10426) ;
#8108=LINE('',#76242,#10427) ;
#8109=LINE('',#76245,#10428) ;
#8110=LINE('',#76343,#10429) ;
#8111=LINE('',#76344,#10430) ;
#8112=LINE('',#76347,#10431) ;
#8113=LINE('',#76370,#10432) ;
#8114=LINE('',#76376,#10433) ;
#8115=LINE('',#76378,#10434) ;
#8116=LINE('',#76382,#10435) ;
#8117=LINE('',#76386,#10436) ;
#8118=LINE('',#76409,#10437) ;
#8119=LINE('',#76412,#10438) ;
#8120=LINE('',#76421,#10439) ;
#8121=LINE('',#76424,#10440) ;
#8122=LINE('',#77333,#10441) ;
#8123=LINE('',#77335,#10442) ;
#8124=LINE('',#77387,#10443) ;
#8125=LINE('',#77390,#10444) ;
#8126=LINE('',#77397,#10445) ;
#8127=LINE('',#77399,#10446) ;
#8128=LINE('',#77400,#10447) ;
#8129=LINE('',#77403,#10448) ;
#8130=LINE('',#77451,#10449) ;
#8131=LINE('',#77452,#10450) ;
#8132=LINE('',#77520,#10451) ;
#8133=LINE('',#77523,#10452) ;
#8134=LINE('',#77526,#10453) ;
#8135=LINE('',#77527,#10454) ;
#8136=LINE('',#77530,#10455) ;
#8137=LINE('',#77534,#10456) ;
#8138=LINE('',#77535,#10457) ;
#8139=LINE('',#77537,#10458) ;
#8140=LINE('',#77538,#10459) ;
#8141=LINE('',#77562,#10460) ;
#8142=LINE('',#77563,#10461) ;
#8143=LINE('',#77597,#10462) ;
#8144=LINE('',#77606,#10463) ;
#8145=LINE('',#77608,#10464) ;
#8146=LINE('',#77611,#10465) ;
#8147=LINE('',#77612,#10466) ;
#8148=LINE('',#77668,#10467) ;
#8149=LINE('',#77678,#10468) ;
#8150=LINE('',#77708,#10469) ;
#8151=LINE('',#77710,#10470) ;
#8152=LINE('',#77714,#10471) ;
#8153=LINE('',#77716,#10472) ;
#8154=LINE('',#77717,#10473) ;
#8155=LINE('',#77744,#10474) ;
#8156=LINE('',#77746,#10475) ;
#8157=LINE('',#77781,#10476) ;
#8158=LINE('',#77783,#10477) ;
#8159=LINE('',#77819,#10478) ;
#8160=LINE('',#77821,#10479) ;
#8161=LINE('',#77873,#10480) ;
#8162=LINE('',#77876,#10481) ;
#8163=LINE('',#77883,#10482) ;
#8164=LINE('',#77885,#10483) ;
#8165=LINE('',#77886,#10484) ;
#8166=LINE('',#77889,#10485) ;
#8167=LINE('',#77937,#10486) ;
#8168=LINE('',#77938,#10487) ;
#8169=LINE('',#78006,#10488) ;
#8170=LINE('',#78009,#10489) ;
#8171=LINE('',#78012,#10490) ;
#8172=LINE('',#78013,#10491) ;
#8173=LINE('',#78016,#10492) ;
#8174=LINE('',#78019,#10493) ;
#8175=LINE('',#78021,#10494) ;
#8176=LINE('',#78022,#10495) ;
#8177=LINE('',#78028,#10496) ;
#8178=LINE('',#78031,#10497) ;
#8179=LINE('',#78084,#10498) ;
#8180=LINE('',#78092,#10499) ;
#8181=LINE('',#78093,#10500) ;
#8182=LINE('',#78096,#10501) ;
#8183=LINE('',#78098,#10502) ;
#8184=LINE('',#78101,#10503) ;
#8185=LINE('',#78102,#10504) ;
#8186=LINE('',#78158,#10505) ;
#8187=LINE('',#78168,#10506) ;
#8188=LINE('',#78198,#10507) ;
#8189=LINE('',#78206,#10508) ;
#8190=LINE('',#78208,#10509) ;
#8191=LINE('',#78209,#10510) ;
#8192=LINE('',#78236,#10511) ;
#8193=LINE('',#78238,#10512) ;
#8194=LINE('',#78291,#10513) ;
#8195=LINE('',#78429,#10514) ;
#8196=LINE('',#78458,#10515) ;
#10380=VECTOR('',#43761,1.2370442518096) ;
#10381=VECTOR('',#43764,1.2370442518096) ;
#10382=VECTOR('',#43767,1.2370442518096) ;
#10383=VECTOR('',#43770,1.2370442518096) ;
#10384=VECTOR('',#43773,1.2370442518096) ;
#10385=VECTOR('',#43776,1.2370442518096) ;
#10386=VECTOR('',#43779,1.2370442518096) ;
#10387=VECTOR('',#43782,1.2370442518096) ;
#10388=VECTOR('',#43787,1.7526) ;
#10389=VECTOR('',#43792,1.7526) ;
#10390=VECTOR('',#43795,1.7526) ;
#10391=VECTOR('',#43798,1.7526) ;
#10392=VECTOR('',#43801,1.7526) ;
#10393=VECTOR('',#43804,1.7526) ;
#10394=VECTOR('',#43807,1.7526) ;
#10395=VECTOR('',#43830,10.) ;
#10396=VECTOR('',#43833,10.) ;
#10397=VECTOR('',#43834,10.) ;
#10398=VECTOR('',#43879,10.) ;
#10399=VECTOR('',#43882,10.) ;
#10400=VECTOR('',#43885,10.) ;
#10401=VECTOR('',#43888,10.) ;
#10402=VECTOR('',#43891,10.) ;
#10403=VECTOR('',#43894,10.) ;
#10404=VECTOR('',#43895,10.) ;
#10405=VECTOR('',#43912,10.) ;
#10406=VECTOR('',#43915,10.) ;
#10407=VECTOR('',#43916,10.) ;
#10408=VECTOR('',#43937,10.) ;
#10409=VECTOR('',#43940,10.) ;
#10410=VECTOR('',#43943,10.) ;
#10411=VECTOR('',#43946,10.) ;
#10412=VECTOR('',#43949,10.) ;
#10413=VECTOR('',#43952,10.) ;
#10414=VECTOR('',#43953,10.) ;
#10415=VECTOR('',#43966,10.) ;
#10416=VECTOR('',#43969,10.) ;
#10417=VECTOR('',#43984,10.) ;
#10418=VECTOR('',#43989,10.) ;
#10419=VECTOR('',#44030,10.) ;
#10420=VECTOR('',#44031,10.) ;
#10421=VECTOR('',#44034,10.) ;
#10422=VECTOR('',#44043,10.) ;
#10423=VECTOR('',#44052,10.) ;
#10424=VECTOR('',#44053,10.) ;
#10425=VECTOR('',#44056,10.) ;
#10426=VECTOR('',#44061,10.) ;
#10427=VECTOR('',#44100,10.) ;
#10428=VECTOR('',#44103,10.) ;
#10429=VECTOR('',#44126,10.) ;
#10430=VECTOR('',#44127,10.) ;
#10431=VECTOR('',#44130,10.) ;
#10432=VECTOR('',#44139,10.) ;
#10433=VECTOR('',#44148,10.) ;
#10434=VECTOR('',#44149,10.) ;
#10435=VECTOR('',#44152,10.) ;
#10436=VECTOR('',#44157,10.) ;
#10437=VECTOR('',#44166,10.) ;
#10438=VECTOR('',#44169,10.) ;
#10439=VECTOR('',#44182,10.) ;
#10440=VECTOR('',#44185,10.) ;
#10441=VECTOR('',#44208,10.) ;
#10442=VECTOR('',#44209,10.) ;
#10443=VECTOR('',#44222,10.) ;
#10444=VECTOR('',#44225,10.) ;
#10445=VECTOR('',#44234,10.) ;
#10446=VECTOR('',#44235,10.) ;
#10447=VECTOR('',#44236,10.) ;
#10448=VECTOR('',#44239,10.) ;
#10449=VECTOR('',#44258,10.) ;
#10450=VECTOR('',#44259,10.) ;
#10451=VECTOR('',#44268,10.) ;
#10452=VECTOR('',#44271,10.) ;
#10453=VECTOR('',#44274,10.) ;
#10454=VECTOR('',#44275,10.) ;
#10455=VECTOR('',#44278,10.) ;
#10456=VECTOR('',#44283,10.) ;
#10457=VECTOR('',#44284,10.) ;
#10458=VECTOR('',#44285,10.) ;
#10459=VECTOR('',#44286,9.99999999999999) ;
#10460=VECTOR('',#44295,10.) ;
#10461=VECTOR('',#44296,10.) ;
#10462=VECTOR('',#44309,10.) ;
#10463=VECTOR('',#44322,10.) ;
#10464=VECTOR('',#44325,10.) ;
#10465=VECTOR('',#44328,10.) ;
#10466=VECTOR('',#44329,10.) ;
#10467=VECTOR('',#44354,10.) ;
#10468=VECTOR('',#44367,10.) ;
#10469=VECTOR('',#44388,10.) ;
#10470=VECTOR('',#44391,10.) ;
#10471=VECTOR('',#44396,9.99999999999999) ;
#10472=VECTOR('',#44397,10.) ;
#10473=VECTOR('',#44398,9.99999999999999) ;
#10474=VECTOR('',#44417,10.) ;
#10475=VECTOR('',#44420,9.99999999999999) ;
#10476=VECTOR('',#44423,10.) ;
#10477=VECTOR('',#44424,10.) ;
#10478=VECTOR('',#44435,10.) ;
#10479=VECTOR('',#44436,10.) ;
#10480=VECTOR('',#44449,10.) ;
#10481=VECTOR('',#44452,9.99999999999999) ;
#10482=VECTOR('',#44461,10.) ;
#10483=VECTOR('',#44462,10.) ;
#10484=VECTOR('',#44463,10.) ;
#10485=VECTOR('',#44466,10.) ;
#10486=VECTOR('',#44485,10.) ;
#10487=VECTOR('',#44486,10.) ;
#10488=VECTOR('',#44495,10.) ;
#10489=VECTOR('',#44498,10.) ;
#10490=VECTOR('',#44501,10.) ;
#10491=VECTOR('',#44502,10.) ;
#10492=VECTOR('',#44505,10.) ;
#10493=VECTOR('',#44510,10.) ;
#10494=VECTOR('',#44511,10.) ;
#10495=VECTOR('',#44512,10.) ;
#10496=VECTOR('',#44517,10.) ;
#10497=VECTOR('',#44520,10.) ;
#10498=VECTOR('',#44537,10.) ;
#10499=VECTOR('',#44550,10.) ;
#10500=VECTOR('',#44551,10.) ;
#10501=VECTOR('',#44554,10.) ;
#10502=VECTOR('',#44557,10.) ;
#10503=VECTOR('',#44560,10.) ;
#10504=VECTOR('',#44561,10.) ;
#10505=VECTOR('',#44588,10.) ;
#10506=VECTOR('',#44601,10.) ;
#10507=VECTOR('',#44622,10.) ;
#10508=VECTOR('',#44625,10.) ;
#10509=VECTOR('',#44626,10.) ;
#10510=VECTOR('',#44627,10.) ;
#10511=VECTOR('',#44646,10.) ;
#10512=VECTOR('',#44649,10.) ;
#10513=VECTOR('',#44694,10.) ;
#10514=VECTOR('',#44725,10.) ;
#10515=VECTOR('',#44738,1.7526) ;
#12195=CIRCLE('',#35484,1.23704425180986) ;
#12196=CIRCLE('',#35486,1.7526) ;
#12197=CIRCLE('',#35494,1.7526) ;
#12198=CIRCLE('',#35496,1.23704425180986) ;
#12199=CIRCLE('',#35497,0.1) ;
#12200=CIRCLE('',#35498,0.0999999999999999) ;
#12201=CIRCLE('',#35499,0.1) ;
#12202=CIRCLE('',#35500,0.1) ;
#12203=CIRCLE('',#35503,0.0999999999999989) ;
#12204=CIRCLE('',#35504,0.0999999999999997) ;
#12205=CIRCLE('',#35505,0.0999999999999999) ;
#12206=CIRCLE('',#35508,3.429) ;
#12207=CIRCLE('',#35510,3.35640733905173) ;
#12208=CIRCLE('',#35512,3.429) ;
#12209=CIRCLE('',#35513,3.35640733905173) ;
#12210=CIRCLE('',#35515,3.429) ;
#12211=CIRCLE('',#35516,0.443484) ;
#12212=CIRCLE('',#35517,2.985516) ;
#12213=CIRCLE('',#35519,3.2727760605723) ;
#12214=CIRCLE('',#35521,0.1) ;
#12215=CIRCLE('',#35522,0.0999999999999997) ;
#12216=CIRCLE('',#35523,0.0999999999999997) ;
#12217=CIRCLE('',#35524,0.1) ;
#12218=CIRCLE('',#35525,0.1) ;
#12219=CIRCLE('',#35527,0.100000000000001) ;
#12220=CIRCLE('',#35528,0.0999999999999995) ;
#12221=CIRCLE('',#35530,0.1) ;
#12222=CIRCLE('',#35532,5.21754264299203) ;
#12223=CIRCLE('',#35533,0.0999999999999999) ;
#12224=CIRCLE('',#35534,0.1) ;
#12225=CIRCLE('',#35535,0.1) ;
#12226=CIRCLE('',#35536,0.1) ;
#12227=CIRCLE('',#35539,0.100000000000001) ;
#12228=CIRCLE('',#35540,0.1) ;
#12229=CIRCLE('',#35541,0.0999999999999999) ;
#12230=CIRCLE('',#35543,3.2727760605723) ;
#12231=CIRCLE('',#35545,0.100000000000001) ;
#12232=CIRCLE('',#35546,0.1) ;
#12233=CIRCLE('',#35547,0.1) ;
#12234=CIRCLE('',#35548,0.1) ;
#12235=CIRCLE('',#35549,0.1) ;
#12236=CIRCLE('',#35551,0.100000000000001) ;
#12237=CIRCLE('',#35552,0.0999999999999988) ;
#12238=CIRCLE('',#35554,0.1) ;
#12239=CIRCLE('',#35556,5.21754264299203) ;
#12240=CIRCLE('',#35558,0.1) ;
#12241=CIRCLE('',#35562,0.1) ;
#12242=CIRCLE('',#35564,0.1) ;
#12243=CIRCLE('',#35565,0.1) ;
#12244=CIRCLE('',#35567,5.28650897109211) ;
#12245=CIRCLE('',#35568,5.38647567822556) ;
#12246=CIRCLE('',#35572,0.1) ;
#12247=CIRCLE('',#35573,0.1) ;
#12248=CIRCLE('',#35574,0.1) ;
#12249=CIRCLE('',#35576,0.1) ;
#12250=CIRCLE('',#35578,0.1) ;
#12251=CIRCLE('',#35580,0.0999999999999999) ;
#12252=CIRCLE('',#35581,0.1) ;
#12253=CIRCLE('',#35582,0.1) ;
#12254=CIRCLE('',#35583,0.1) ;
#12255=CIRCLE('',#35584,0.0999999999999999) ;
#12256=CIRCLE('',#35588,5.28650897109211) ;
#12257=CIRCLE('',#35589,0.1) ;
#12258=CIRCLE('',#35590,5.38647567822556) ;
#12259=CIRCLE('',#35594,0.0999999999999998) ;
#12260=CIRCLE('',#35597,0.0999999999999998) ;
#12261=CIRCLE('',#35599,0.1) ;
#12262=CIRCLE('',#35602,5.25939963812285) ;
#12263=CIRCLE('',#35606,0.0999999999999999) ;
#12264=CIRCLE('',#35607,0.1) ;
#12265=CIRCLE('',#35608,0.1) ;
#12266=CIRCLE('',#35609,0.1) ;
#12267=CIRCLE('',#35611,0.0999999999999999) ;
#12268=CIRCLE('',#35614,2.21840405576151) ;
#12269=CIRCLE('',#35616,2.35877270918314) ;
#12270=CIRCLE('',#35618,1.83996264656598) ;
#12271=CIRCLE('',#35620,1.74337006393707) ;
#12272=CIRCLE('',#35621,0.1) ;
#12273=CIRCLE('',#35625,0.1) ;
#12274=CIRCLE('',#35626,0.1) ;
#12275=CIRCLE('',#35627,0.1) ;
#12276=CIRCLE('',#35628,0.1) ;
#12277=CIRCLE('',#35631,5.28650897109211) ;
#12278=CIRCLE('',#35632,0.1) ;
#12279=CIRCLE('',#35633,5.38647567822556) ;
#12280=CIRCLE('',#35637,0.0999999999999997) ;
#12281=CIRCLE('',#35640,0.1) ;
#12282=CIRCLE('',#35642,0.1) ;
#12283=CIRCLE('',#35645,5.25939963812284) ;
#12284=CIRCLE('',#35648,0.0999999999999998) ;
#12285=CIRCLE('',#35651,0.1) ;
#12286=CIRCLE('',#35653,0.1) ;
#12287=CIRCLE('',#35654,0.1) ;
#12288=CIRCLE('',#35656,5.28650897109211) ;
#12289=CIRCLE('',#35660,1.81678704225081) ;
#12290=CIRCLE('',#35662,1.8526) ;
#12291=CIRCLE('',#35664,1.82930603365754) ;
#12292=CIRCLE('',#35666,0.1) ;
#12293=CIRCLE('',#35673,0.1) ;
#12294=CIRCLE('',#35676,0.1) ;
#12295=CIRCLE('',#35678,0.1) ;
#12296=CIRCLE('',#35679,0.1) ;
#12297=CIRCLE('',#35682,0.1) ;
#12298=CIRCLE('',#35684,1.89730211487829) ;
#12299=CIRCLE('',#35685,1.99389469750719) ;
#12300=CIRCLE('',#35687,0.1) ;
#12301=CIRCLE('',#35688,0.1) ;
#12302=CIRCLE('',#35689,0.1) ;
#12303=CIRCLE('',#35690,0.0999999999999999) ;
#12304=CIRCLE('',#35692,0.1) ;
#12305=CIRCLE('',#35695,0.1) ;
#12306=CIRCLE('',#35700,0.0999999999999998) ;
#12307=CIRCLE('',#35703,0.1) ;
#12308=CIRCLE('',#35704,0.0999999999382708) ;
#12309=CIRCLE('',#35706,0.1) ;
#12310=CIRCLE('',#35709,0.100000000000001) ;
#12311=CIRCLE('',#35711,0.1) ;
#12312=CIRCLE('',#35712,0.1) ;
#12313=CIRCLE('',#35714,0.1) ;
#12314=CIRCLE('',#35720,0.0999999999999999) ;
#12315=CIRCLE('',#35721,0.1) ;
#12316=CIRCLE('',#35724,0.1) ;
#12317=CIRCLE('',#35725,0.1) ;
#12318=CIRCLE('',#35726,0.1) ;
#12319=CIRCLE('',#35729,0.100000000000001) ;
#12320=CIRCLE('',#35731,0.1) ;
#12321=CIRCLE('',#35732,0.1) ;
#12322=CIRCLE('',#35734,0.1) ;
#12323=CIRCLE('',#35735,0.1) ;
#12324=CIRCLE('',#35738,0.1) ;
#12325=CIRCLE('',#35740,5.35885371380814) ;
#12326=CIRCLE('',#35742,5.21754264299203) ;
#12327=CIRCLE('',#35743,0.0999999999999998) ;
#12328=CIRCLE('',#35744,5.31620521222257) ;
#12329=CIRCLE('',#35750,0.0999999999999999) ;
#12330=CIRCLE('',#35751,0.1) ;
#12331=CIRCLE('',#35754,0.1) ;
#12332=CIRCLE('',#35761,0.1) ;
#12333=CIRCLE('',#35768,0.1) ;
#12334=CIRCLE('',#35771,0.1) ;
#12335=CIRCLE('',#35773,0.1) ;
#12336=CIRCLE('',#35774,0.1) ;
#12337=CIRCLE('',#35777,0.1) ;
#12338=CIRCLE('',#35779,1.89730211487828) ;
#12339=CIRCLE('',#35780,1.99389469750719) ;
#12340=CIRCLE('',#35782,0.1) ;
#12341=CIRCLE('',#35783,0.1) ;
#12342=CIRCLE('',#35784,0.1) ;
#12343=CIRCLE('',#35785,0.0999999999999999) ;
#12344=CIRCLE('',#35787,0.1) ;
#12345=CIRCLE('',#35790,0.0999999999999999) ;
#12346=CIRCLE('',#35796,0.1) ;
#12347=CIRCLE('',#35797,0.0999999999999999) ;
#12348=CIRCLE('',#35800,0.0999999999386781) ;
#12349=CIRCLE('',#35802,0.1) ;
#12350=CIRCLE('',#35805,0.1) ;
#12351=CIRCLE('',#35807,0.1) ;
#12352=CIRCLE('',#35808,0.1) ;
#12353=CIRCLE('',#35810,0.1) ;
#12354=CIRCLE('',#35817,0.0999999999999999) ;
#12355=CIRCLE('',#35818,0.1) ;
#12356=CIRCLE('',#35820,0.0999999999999999) ;
#12357=CIRCLE('',#35823,5.25939963812284) ;
#12358=CIRCLE('',#35824,0.1) ;
#12359=CIRCLE('',#35825,0.1) ;
#12360=CIRCLE('',#35827,0.1) ;
#12361=CIRCLE('',#35829,0.1) ;
#12362=CIRCLE('',#35830,0.1) ;
#12363=CIRCLE('',#35832,0.1) ;
#12364=CIRCLE('',#35833,0.1) ;
#12365=CIRCLE('',#35836,0.1) ;
#12366=CIRCLE('',#35838,5.35885371380814) ;
#12367=CIRCLE('',#35840,5.21754264299203) ;
#12368=CIRCLE('',#35841,0.1) ;
#12369=CIRCLE('',#35842,5.31620521222257) ;
#12370=CIRCLE('',#35846,0.1) ;
#12371=CIRCLE('',#35847,0.1) ;
#12372=CIRCLE('',#35850,0.1) ;
#12373=CIRCLE('',#35856,1.74337006393707) ;
#12374=CIRCLE('',#35857,1.83996264656598) ;
#12375=CIRCLE('',#35859,1.74337006393707) ;
#12376=CIRCLE('',#35860,1.83996264656598) ;
#12377=CIRCLE('',#35862,1.74337006393707) ;
#12378=CIRCLE('',#35863,1.83996264656598) ;
#12379=CIRCLE('',#35865,5.25939963812284) ;
#12380=CIRCLE('',#35869,5.31620521222257) ;
#12381=CIRCLE('',#35870,0.100000000000004) ;
#12382=CIRCLE('',#35872,5.35885371380814) ;
#12383=CIRCLE('',#35874,2.21840405576151) ;
#12384=CIRCLE('',#35875,2.35877270918314) ;
#12385=CIRCLE('',#35877,0.1) ;
#12386=CIRCLE('',#35879,3.25327858632053) ;
#12387=CIRCLE('',#35881,3.429) ;
#12388=CIRCLE('',#35883,0.1) ;
#12389=CIRCLE('',#35885,5.31620521222257) ;
#12390=CIRCLE('',#35887,5.35885371380814) ;
#12391=CIRCLE('',#35889,5.38647567822556) ;
#12392=CIRCLE('',#35890,0.1) ;
#12393=CIRCLE('',#35893,3.25327858632053) ;
#12394=CIRCLE('',#35895,3.429) ;
#12395=CIRCLE('',#35898,1.1572875) ;
#14820=VERTEX_POINT('',#73263) ;
#14821=VERTEX_POINT('',#73264) ;
#14822=VERTEX_POINT('',#73266) ;
#14823=VERTEX_POINT('',#73297) ;
#14824=VERTEX_POINT('',#73334) ;
#14825=VERTEX_POINT('',#73335) ;
#14826=VERTEX_POINT('',#73410) ;
#14827=VERTEX_POINT('',#73411) ;
#14828=VERTEX_POINT('',#73486) ;
#14829=VERTEX_POINT('',#73487) ;
#14830=VERTEX_POINT('',#73562) ;
#14831=VERTEX_POINT('',#73563) ;
#14832=VERTEX_POINT('',#73638) ;
#14833=VERTEX_POINT('',#73639) ;
#14834=VERTEX_POINT('',#73714) ;
#14835=VERTEX_POINT('',#73715) ;
#14836=VERTEX_POINT('',#73790) ;
#14837=VERTEX_POINT('',#73791) ;
#14838=VERTEX_POINT('',#73793) ;
#14839=VERTEX_POINT('',#73866) ;
#14840=VERTEX_POINT('',#73867) ;
#14841=VERTEX_POINT('',#73869) ;
#14842=VERTEX_POINT('',#73894) ;
#14843=VERTEX_POINT('',#73917) ;
#14844=VERTEX_POINT('',#73918) ;
#14845=VERTEX_POINT('',#73993) ;
#14846=VERTEX_POINT('',#73994) ;
#14847=VERTEX_POINT('',#74069) ;
#14848=VERTEX_POINT('',#74070) ;
#14849=VERTEX_POINT('',#74145) ;
#14850=VERTEX_POINT('',#74146) ;
#14851=VERTEX_POINT('',#74221) ;
#14852=VERTEX_POINT('',#74222) ;
#14853=VERTEX_POINT('',#74297) ;
#14854=VERTEX_POINT('',#74298) ;
#14855=VERTEX_POINT('',#74373) ;
#14856=VERTEX_POINT('',#74398) ;
#14857=VERTEX_POINT('',#74400) ;
#14858=VERTEX_POINT('',#74432) ;
#14859=VERTEX_POINT('',#74462) ;
#14860=VERTEX_POINT('',#74463) ;
#14861=VERTEX_POINT('',#74465) ;
#14862=VERTEX_POINT('',#74498) ;
#14863=VERTEX_POINT('',#74503) ;
#14864=VERTEX_POINT('',#74538) ;
#14865=VERTEX_POINT('',#74539) ;
#14866=VERTEX_POINT('',#74571) ;
#14867=VERTEX_POINT('',#74572) ;
#14868=VERTEX_POINT('',#74648) ;
#14869=VERTEX_POINT('',#74649) ;
#14870=VERTEX_POINT('',#74651) ;
#14871=VERTEX_POINT('',#74681) ;
#14872=VERTEX_POINT('',#74682) ;
#14873=VERTEX_POINT('',#74771) ;
#14874=VERTEX_POINT('',#74775) ;
#14875=VERTEX_POINT('',#74776) ;
#14876=VERTEX_POINT('',#74778) ;
#14877=VERTEX_POINT('',#74785) ;
#14878=VERTEX_POINT('',#74787) ;
#14879=VERTEX_POINT('',#74789) ;
#14880=VERTEX_POINT('',#74791) ;
#14881=VERTEX_POINT('',#74799) ;
#14882=VERTEX_POINT('',#74801) ;
#14883=VERTEX_POINT('',#74803) ;
#14884=VERTEX_POINT('',#74811) ;
#14885=VERTEX_POINT('',#74815) ;
#14886=VERTEX_POINT('',#74817) ;
#14887=VERTEX_POINT('',#74819) ;
#14888=VERTEX_POINT('',#74850) ;
#14889=VERTEX_POINT('',#74878) ;
#14890=VERTEX_POINT('',#74915) ;
#14891=VERTEX_POINT('',#74942) ;
#14892=VERTEX_POINT('',#74990) ;
#14893=VERTEX_POINT('',#74991) ;
#14894=VERTEX_POINT('',#75014) ;
#14895=VERTEX_POINT('',#75037) ;
#14896=VERTEX_POINT('',#75039) ;
#14897=VERTEX_POINT('',#75112) ;
#14898=VERTEX_POINT('',#75114) ;
#14899=VERTEX_POINT('',#75118) ;
#14900=VERTEX_POINT('',#75120) ;
#14901=VERTEX_POINT('',#75122) ;
#14902=VERTEX_POINT('',#75153) ;
#14903=VERTEX_POINT('',#75181) ;
#14904=VERTEX_POINT('',#75186) ;
#14905=VERTEX_POINT('',#75221) ;
#14906=VERTEX_POINT('',#75222) ;
#14907=VERTEX_POINT('',#75254) ;
#14908=VERTEX_POINT('',#75255) ;
#14909=VERTEX_POINT('',#75304) ;
#14910=VERTEX_POINT('',#75305) ;
#14911=VERTEX_POINT('',#75307) ;
#14912=VERTEX_POINT('',#75390) ;
#14913=VERTEX_POINT('',#75391) ;
#14914=VERTEX_POINT('',#75480) ;
#14915=VERTEX_POINT('',#75482) ;
#14916=VERTEX_POINT('',#75484) ;
#14917=VERTEX_POINT('',#75515) ;
#14918=VERTEX_POINT('',#75543) ;
#14919=VERTEX_POINT('',#75580) ;
#14920=VERTEX_POINT('',#75607) ;
#14921=VERTEX_POINT('',#75655) ;
#14922=VERTEX_POINT('',#75656) ;
#14923=VERTEX_POINT('',#75679) ;
#14924=VERTEX_POINT('',#75702) ;
#14925=VERTEX_POINT('',#75704) ;
#14926=VERTEX_POINT('',#75777) ;
#14927=VERTEX_POINT('',#75779) ;
#14928=VERTEX_POINT('',#75783) ;
#14929=VERTEX_POINT('',#75785) ;
#14930=VERTEX_POINT('',#75787) ;
#14931=VERTEX_POINT('',#75806) ;
#14932=VERTEX_POINT('',#75807) ;
#14933=VERTEX_POINT('',#75809) ;
#14934=VERTEX_POINT('',#75813) ;
#14935=VERTEX_POINT('',#75815) ;
#14936=VERTEX_POINT('',#75819) ;
#14937=VERTEX_POINT('',#75823) ;
#14938=VERTEX_POINT('',#75825) ;
#14939=VERTEX_POINT('',#75834) ;
#14940=VERTEX_POINT('',#75836) ;
#14941=VERTEX_POINT('',#75843) ;
#14942=VERTEX_POINT('',#75876) ;
#14943=VERTEX_POINT('',#75904) ;
#14944=VERTEX_POINT('',#75927) ;
#14945=VERTEX_POINT('',#75940) ;
#14946=VERTEX_POINT('',#75941) ;
#14947=VERTEX_POINT('',#75943) ;
#14948=VERTEX_POINT('',#75966) ;
#14949=VERTEX_POINT('',#75967) ;
#14950=VERTEX_POINT('',#76001) ;
#14951=VERTEX_POINT('',#76002) ;
#14952=VERTEX_POINT('',#76036) ;
#14953=VERTEX_POINT('',#76050) ;
#14954=VERTEX_POINT('',#76052) ;
#14955=VERTEX_POINT('',#76056) ;
#14956=VERTEX_POINT('',#76060) ;
#14957=VERTEX_POINT('',#76079) ;
#14958=VERTEX_POINT('',#76083) ;
#14959=VERTEX_POINT('',#76089) ;
#14960=VERTEX_POINT('',#76091) ;
#14961=VERTEX_POINT('',#76093) ;
#14962=VERTEX_POINT('',#76095) ;
#14963=VERTEX_POINT('',#76099) ;
#14964=VERTEX_POINT('',#76103) ;
#14965=VERTEX_POINT('',#76104) ;
#14966=VERTEX_POINT('',#76106) ;
#14967=VERTEX_POINT('',#76129) ;
#14968=VERTEX_POINT('',#76130) ;
#14969=VERTEX_POINT('',#76164) ;
#14970=VERTEX_POINT('',#76166) ;
#14971=VERTEX_POINT('',#76199) ;
#14972=VERTEX_POINT('',#76213) ;
#14973=VERTEX_POINT('',#76215) ;
#14974=VERTEX_POINT('',#76217) ;
#14975=VERTEX_POINT('',#76226) ;
#14976=VERTEX_POINT('',#76237) ;
#14977=VERTEX_POINT('',#76241) ;
#14978=VERTEX_POINT('',#76243) ;
#14979=VERTEX_POINT('',#76247) ;
#14980=VERTEX_POINT('',#76270) ;
#14981=VERTEX_POINT('',#76296) ;
#14982=VERTEX_POINT('',#76336) ;
#14983=VERTEX_POINT('',#76338) ;
#14984=VERTEX_POINT('',#76342) ;
#14985=VERTEX_POINT('',#76346) ;
#14986=VERTEX_POINT('',#76365) ;
#14987=VERTEX_POINT('',#76369) ;
#14988=VERTEX_POINT('',#76375) ;
#14989=VERTEX_POINT('',#76377) ;
#14990=VERTEX_POINT('',#76379) ;
#14991=VERTEX_POINT('',#76381) ;
#14992=VERTEX_POINT('',#76385) ;
#14993=VERTEX_POINT('',#76404) ;
#14994=VERTEX_POINT('',#76408) ;
#14995=VERTEX_POINT('',#76410) ;
#14996=VERTEX_POINT('',#76414) ;
#14997=VERTEX_POINT('',#76420) ;
#14998=VERTEX_POINT('',#76422) ;
#14999=VERTEX_POINT('',#76465) ;
#15000=VERTEX_POINT('',#76466) ;
#15001=VERTEX_POINT('',#76475) ;
#15002=VERTEX_POINT('',#76486) ;
#15003=VERTEX_POINT('',#76494) ;
#15004=VERTEX_POINT('',#76496) ;
#15005=VERTEX_POINT('',#76498) ;
#15006=VERTEX_POINT('',#76517) ;
#15007=VERTEX_POINT('',#76563) ;
#15008=VERTEX_POINT('',#76681) ;
#15009=VERTEX_POINT('',#76686) ;
#15010=VERTEX_POINT('',#76693) ;
#15011=VERTEX_POINT('',#77323) ;
#15012=VERTEX_POINT('',#77324) ;
#15013=VERTEX_POINT('',#77326) ;
#15014=VERTEX_POINT('',#77328) ;
#15015=VERTEX_POINT('',#77330) ;
#15016=VERTEX_POINT('',#77332) ;
#15017=VERTEX_POINT('',#77334) ;
#15018=VERTEX_POINT('',#77336) ;
#15019=VERTEX_POINT('',#77338) ;
#15020=VERTEX_POINT('',#77361) ;
#15021=VERTEX_POINT('',#77362) ;
#15022=VERTEX_POINT('',#77386) ;
#15023=VERTEX_POINT('',#77388) ;
#15024=VERTEX_POINT('',#77392) ;
#15025=VERTEX_POINT('',#77396) ;
#15026=VERTEX_POINT('',#77398) ;
#15027=VERTEX_POINT('',#77402) ;
#15028=VERTEX_POINT('',#77406) ;
#15029=VERTEX_POINT('',#77408) ;
#15030=VERTEX_POINT('',#77413) ;
#15031=VERTEX_POINT('',#77422) ;
#15032=VERTEX_POINT('',#77423) ;
#15033=VERTEX_POINT('',#77425) ;
#15034=VERTEX_POINT('',#77448) ;
#15035=VERTEX_POINT('',#77449) ;
#15036=VERTEX_POINT('',#77473) ;
#15037=VERTEX_POINT('',#77507) ;
#15038=VERTEX_POINT('',#77519) ;
#15039=VERTEX_POINT('',#77521) ;
#15040=VERTEX_POINT('',#77525) ;
#15041=VERTEX_POINT('',#77529) ;
#15042=VERTEX_POINT('',#77533) ;
#15043=VERTEX_POINT('',#77536) ;
#15044=VERTEX_POINT('',#77555) ;
#15045=VERTEX_POINT('',#77559) ;
#15046=VERTEX_POINT('',#77560) ;
#15047=VERTEX_POINT('',#77590) ;
#15048=VERTEX_POINT('',#77595) ;
#15049=VERTEX_POINT('',#77599) ;
#15050=VERTEX_POINT('',#77605) ;
#15051=VERTEX_POINT('',#77610) ;
#15052=VERTEX_POINT('',#77661) ;
#15053=VERTEX_POINT('',#77666) ;
#15054=VERTEX_POINT('',#77670) ;
#15055=VERTEX_POINT('',#77674) ;
#15056=VERTEX_POINT('',#77676) ;
#15057=VERTEX_POINT('',#77701) ;
#15058=VERTEX_POINT('',#77703) ;
#15059=VERTEX_POINT('',#77707) ;
#15060=VERTEX_POINT('',#77713) ;
#15061=VERTEX_POINT('',#77715) ;
#15062=VERTEX_POINT('',#77740) ;
#15063=VERTEX_POINT('',#77780) ;
#15064=VERTEX_POINT('',#77782) ;
#15065=VERTEX_POINT('',#77809) ;
#15066=VERTEX_POINT('',#77810) ;
#15067=VERTEX_POINT('',#77812) ;
#15068=VERTEX_POINT('',#77814) ;
#15069=VERTEX_POINT('',#77816) ;
#15070=VERTEX_POINT('',#77818) ;
#15071=VERTEX_POINT('',#77820) ;
#15072=VERTEX_POINT('',#77822) ;
#15073=VERTEX_POINT('',#77824) ;
#15074=VERTEX_POINT('',#77847) ;
#15075=VERTEX_POINT('',#77848) ;
#15076=VERTEX_POINT('',#77872) ;
#15077=VERTEX_POINT('',#77874) ;
#15078=VERTEX_POINT('',#77878) ;
#15079=VERTEX_POINT('',#77882) ;
#15080=VERTEX_POINT('',#77884) ;
#15081=VERTEX_POINT('',#77888) ;
#15082=VERTEX_POINT('',#77892) ;
#15083=VERTEX_POINT('',#77894) ;
#15084=VERTEX_POINT('',#77899) ;
#15085=VERTEX_POINT('',#77908) ;
#15086=VERTEX_POINT('',#77909) ;
#15087=VERTEX_POINT('',#77911) ;
#15088=VERTEX_POINT('',#77934) ;
#15089=VERTEX_POINT('',#77935) ;
#15090=VERTEX_POINT('',#77959) ;
#15091=VERTEX_POINT('',#77993) ;
#15092=VERTEX_POINT('',#78005) ;
#15093=VERTEX_POINT('',#78007) ;
#15094=VERTEX_POINT('',#78011) ;
#15095=VERTEX_POINT('',#78015) ;
#15096=VERTEX_POINT('',#78020) ;
#15097=VERTEX_POINT('',#78024) ;
#15098=VERTEX_POINT('',#78025) ;
#15099=VERTEX_POINT('',#78027) ;
#15100=VERTEX_POINT('',#78029) ;
#15101=VERTEX_POINT('',#78048) ;
#15102=VERTEX_POINT('',#78077) ;
#15103=VERTEX_POINT('',#78082) ;
#15104=VERTEX_POINT('',#78086) ;
#15105=VERTEX_POINT('',#78095) ;
#15106=VERTEX_POINT('',#78100) ;
#15107=VERTEX_POINT('',#78156) ;
#15108=VERTEX_POINT('',#78160) ;
#15109=VERTEX_POINT('',#78164) ;
#15110=VERTEX_POINT('',#78166) ;
#15111=VERTEX_POINT('',#78191) ;
#15112=VERTEX_POINT('',#78193) ;
#15113=VERTEX_POINT('',#78197) ;
#15114=VERTEX_POINT('',#78205) ;
#15115=VERTEX_POINT('',#78207) ;
#15116=VERTEX_POINT('',#78232) ;
#15117=VERTEX_POINT('',#78253) ;
#15118=VERTEX_POINT('',#78290) ;
#15119=VERTEX_POINT('',#78356) ;
#15120=VERTEX_POINT('',#78410) ;
#15121=VERTEX_POINT('',#78436) ;
#15122=VERTEX_POINT('',#78457) ;
#19088=EDGE_CURVE('',#14820,#14821,#8061,.T.) ;
#19089=EDGE_CURVE('',#14820,#14822,#1465,.T.) ;
#19090=EDGE_CURVE('',#14822,#14823,#1466,.T.) ;
#19091=EDGE_CURVE('',#14821,#14823,#804,.T.) ;
#19092=EDGE_CURVE('',#14824,#14825,#8062,.T.) ;
#19093=EDGE_CURVE('',#14824,#14820,#1467,.T.) ;
#19094=EDGE_CURVE('',#14825,#14821,#1468,.F.) ;
#19095=EDGE_CURVE('',#14826,#14827,#8063,.T.) ;
#19096=EDGE_CURVE('',#14826,#14824,#1469,.T.) ;
#19097=EDGE_CURVE('',#14827,#14825,#1470,.F.) ;
#19098=EDGE_CURVE('',#14828,#14829,#8064,.T.) ;
#19099=EDGE_CURVE('',#14828,#14826,#1471,.T.) ;
#19100=EDGE_CURVE('',#14829,#14827,#1472,.F.) ;
#19101=EDGE_CURVE('',#14830,#14831,#8065,.T.) ;
#19102=EDGE_CURVE('',#14830,#14828,#1473,.T.) ;
#19103=EDGE_CURVE('',#14831,#14829,#1474,.F.) ;
#19104=EDGE_CURVE('',#14832,#14833,#8066,.T.) ;
#19105=EDGE_CURVE('',#14832,#14830,#1475,.T.) ;
#19106=EDGE_CURVE('',#14833,#14831,#1476,.F.) ;
#19107=EDGE_CURVE('',#14834,#14835,#8067,.T.) ;
#19108=EDGE_CURVE('',#14834,#14832,#1477,.T.) ;
#19109=EDGE_CURVE('',#14835,#14833,#1478,.F.) ;
#19110=EDGE_CURVE('',#14836,#14837,#8068,.T.) ;
#19111=EDGE_CURVE('',#14838,#14836,#12195,.T.) ;
#19112=EDGE_CURVE('',#14838,#14834,#1479,.T.) ;
#19113=EDGE_CURVE('',#14837,#14835,#1480,.F.) ;
#19114=EDGE_CURVE('',#14839,#14840,#8069,.T.) ;
#19115=EDGE_CURVE('',#14841,#14839,#1481,.F.) ;
#19116=EDGE_CURVE('',#14841,#14842,#12196,.T.) ;
#19117=EDGE_CURVE('',#14842,#14840,#1482,.T.) ;
#19118=EDGE_CURVE('',#14843,#14844,#8070,.T.) ;
#19119=EDGE_CURVE('',#14839,#14843,#1483,.F.) ;
#19120=EDGE_CURVE('',#14840,#14844,#1484,.T.) ;
#19121=EDGE_CURVE('',#14845,#14846,#8071,.T.) ;
#19122=EDGE_CURVE('',#14843,#14845,#1485,.F.) ;
#19123=EDGE_CURVE('',#14844,#14846,#1486,.T.) ;
#19124=EDGE_CURVE('',#14847,#14848,#8072,.T.) ;
#19125=EDGE_CURVE('',#14845,#14847,#1487,.F.) ;
#19126=EDGE_CURVE('',#14846,#14848,#1488,.T.) ;
#19127=EDGE_CURVE('',#14849,#14850,#8073,.T.) ;
#19128=EDGE_CURVE('',#14847,#14849,#1489,.F.) ;
#19129=EDGE_CURVE('',#14848,#14850,#1490,.T.) ;
#19130=EDGE_CURVE('',#14851,#14852,#8074,.T.) ;
#19131=EDGE_CURVE('',#14849,#14851,#1491,.F.) ;
#19132=EDGE_CURVE('',#14850,#14852,#1492,.T.) ;
#19133=EDGE_CURVE('',#14853,#14854,#8075,.T.) ;
#19134=EDGE_CURVE('',#14851,#14853,#1493,.F.) ;
#19135=EDGE_CURVE('',#14852,#14854,#1494,.T.) ;
#19136=EDGE_CURVE('',#14854,#14855,#1495,.T.) ;
#19137=EDGE_CURVE('',#14856,#14855,#12197,.T.) ;
#19138=EDGE_CURVE('',#14857,#14856,#1496,.T.) ;
#19139=EDGE_CURVE('',#14853,#14857,#1497,.F.) ;
#19140=EDGE_CURVE('',#14858,#14837,#1498,.F.) ;
#19141=EDGE_CURVE('',#14836,#14858,#12198,.T.) ;
#19142=EDGE_CURVE('',#14859,#14860,#12199,.T.) ;
#19143=EDGE_CURVE('',#14860,#14861,#1499,.T.) ;
#19144=EDGE_CURVE('',#14861,#14859,#1500,.T.) ;
#19145=EDGE_CURVE('',#14859,#14862,#1501,.T.) ;
#19146=EDGE_CURVE('',#14862,#14863,#12200,.T.) ;
#19147=EDGE_CURVE('',#14863,#14860,#1502,.T.) ;
#19148=EDGE_CURVE('',#14864,#14865,#12201,.T.) ;
#19149=EDGE_CURVE('',#14865,#14863,#1503,.T.) ;
#19150=EDGE_CURVE('',#14862,#14864,#1504,.T.) ;
#19151=EDGE_CURVE('',#14866,#14867,#12202,.T.) ;
#19152=EDGE_CURVE('',#14867,#14865,#150,.T.) ;
#19153=EDGE_CURVE('',#14864,#14866,#151,.T.) ;
#19154=EDGE_CURVE('',#14868,#14869,#12203,.T.) ;
#19155=EDGE_CURVE('',#14869,#14870,#8076,.T.) ;
#19156=EDGE_CURVE('',#14870,#14868,#1505,.T.) ;
#19157=EDGE_CURVE('',#14871,#14872,#12204,.T.) ;
#19158=EDGE_CURVE('',#14872,#14869,#8077,.T.) ;
#19159=EDGE_CURVE('',#14868,#14871,#1506,.T.) ;
#19160=EDGE_CURVE('',#14871,#14867,#1507,.T.) ;
#19161=EDGE_CURVE('',#14866,#14872,#8078,.T.) ;
#19162=EDGE_CURVE('',#14873,#14863,#12205,.T.) ;
#19163=EDGE_CURVE('',#14873,#14860,#152,.T.) ;
#19164=EDGE_CURVE('',#14874,#14875,#12206,.T.) ;
#19165=EDGE_CURVE('',#14876,#14874,#1508,.T.) ;
#19166=EDGE_CURVE('',#14877,#14876,#153,.T.) ;
#19167=EDGE_CURVE('',#14878,#14877,#12207,.T.) ;
#19168=EDGE_CURVE('',#14879,#14878,#154,.T.) ;
#19169=EDGE_CURVE('',#14880,#14879,#1509,.T.) ;
#19170=EDGE_CURVE('',#14861,#14880,#12208,.T.) ;
#19171=EDGE_CURVE('',#14881,#14873,#12209,.T.) ;
#19172=EDGE_CURVE('',#14882,#14881,#155,.T.) ;
#19173=EDGE_CURVE('',#14883,#14882,#1510,.T.) ;
#19174=EDGE_CURVE('',#14875,#14883,#12210,.T.) ;
#19175=EDGE_CURVE('',#14875,#14884,#12211,.T.) ;
#19176=EDGE_CURVE('',#14884,#14884,#12212,.T.) ;
#19177=EDGE_CURVE('',#14867,#14885,#12213,.T.) ;
#19178=EDGE_CURVE('',#14886,#14885,#156,.T.) ;
#19179=EDGE_CURVE('',#14887,#14886,#1511,.T.) ;
#19180=EDGE_CURVE('',#14881,#14887,#12214,.T.) ;
#19181=EDGE_CURVE('',#14882,#14888,#12215,.T.) ;
#19182=EDGE_CURVE('',#14888,#14883,#1512,.T.) ;
#19183=EDGE_CURVE('',#14887,#14889,#12216,.T.) ;
#19184=EDGE_CURVE('',#14889,#14888,#1513,.T.) ;
#19185=EDGE_CURVE('',#14882,#14887,#1514,.T.) ;
#19186=EDGE_CURVE('',#14886,#14890,#12217,.T.) ;
#19187=EDGE_CURVE('',#14890,#14889,#1515,.T.) ;
#19188=EDGE_CURVE('',#14885,#14891,#12218,.T.) ;
#19189=EDGE_CURVE('',#14891,#14890,#157,.T.) ;
#19190=EDGE_CURVE('',#14892,#14893,#1516,.T.) ;
#19191=EDGE_CURVE('',#14893,#14894,#8079,.T.) ;
#19192=EDGE_CURVE('',#14894,#14892,#12219,.T.) ;
#19193=EDGE_CURVE('',#14894,#14895,#8080,.T.) ;
#19194=EDGE_CURVE('',#14895,#14896,#12220,.T.) ;
#19195=EDGE_CURVE('',#14896,#14892,#1517,.T.) ;
#19196=EDGE_CURVE('',#14895,#14891,#8081,.T.) ;
#19197=EDGE_CURVE('',#14885,#14896,#1518,.T.) ;
#19198=EDGE_CURVE('',#14890,#14897,#8082,.T.) ;
#19199=EDGE_CURVE('',#14897,#14898,#12221,.T.) ;
#19200=EDGE_CURVE('',#14898,#14883,#8083,.T.) ;
#19201=EDGE_CURVE('',#14899,#14893,#8084,.T.) ;
#19202=EDGE_CURVE('',#14900,#14899,#8085,.T.) ;
#19203=EDGE_CURVE('',#14901,#14900,#12222,.T.) ;
#19204=EDGE_CURVE('',#14897,#14901,#1519,.T.) ;
#19205=EDGE_CURVE('',#14902,#14876,#12223,.T.) ;
#19206=EDGE_CURVE('',#14874,#14902,#1520,.T.) ;
#19207=EDGE_CURVE('',#14902,#14903,#1521,.T.) ;
#19208=EDGE_CURVE('',#14903,#14904,#12224,.T.) ;
#19209=EDGE_CURVE('',#14904,#14876,#1522,.T.) ;
#19210=EDGE_CURVE('',#14905,#14906,#12225,.T.) ;
#19211=EDGE_CURVE('',#14906,#14904,#1523,.T.) ;
#19212=EDGE_CURVE('',#14903,#14905,#1524,.T.) ;
#19213=EDGE_CURVE('',#14907,#14908,#12226,.T.) ;
#19214=EDGE_CURVE('',#14908,#14906,#158,.T.) ;
#19215=EDGE_CURVE('',#14905,#14907,#159,.T.) ;
#19216=EDGE_CURVE('',#14909,#14910,#12227,.T.) ;
#19217=EDGE_CURVE('',#14910,#14911,#8086,.T.) ;
#19218=EDGE_CURVE('',#14911,#14909,#1525,.T.) ;
#19219=EDGE_CURVE('',#14912,#14913,#12228,.T.) ;
#19220=EDGE_CURVE('',#14913,#14910,#8087,.T.) ;
#19221=EDGE_CURVE('',#14909,#14912,#1526,.T.) ;
#19222=EDGE_CURVE('',#14912,#14908,#1527,.T.) ;
#19223=EDGE_CURVE('',#14907,#14913,#8088,.T.) ;
#19224=EDGE_CURVE('',#14877,#14904,#12229,.T.) ;
#19225=EDGE_CURVE('',#14908,#14914,#12230,.T.) ;
#19226=EDGE_CURVE('',#14915,#14914,#160,.T.) ;
#19227=EDGE_CURVE('',#14916,#14915,#1528,.T.) ;
#19228=EDGE_CURVE('',#14878,#14916,#12231,.T.) ;
#19229=EDGE_CURVE('',#14879,#14917,#12232,.T.) ;
#19230=EDGE_CURVE('',#14917,#14880,#1529,.T.) ;
#19231=EDGE_CURVE('',#14916,#14918,#12233,.T.) ;
#19232=EDGE_CURVE('',#14918,#14917,#1530,.T.) ;
#19233=EDGE_CURVE('',#14879,#14916,#1531,.T.) ;
#19234=EDGE_CURVE('',#14915,#14919,#12234,.T.) ;
#19235=EDGE_CURVE('',#14919,#14918,#1532,.T.) ;
#19236=EDGE_CURVE('',#14914,#14920,#12235,.T.) ;
#19237=EDGE_CURVE('',#14920,#14919,#161,.T.) ;
#19238=EDGE_CURVE('',#14921,#14922,#1533,.T.) ;
#19239=EDGE_CURVE('',#14922,#14923,#8089,.T.) ;
#19240=EDGE_CURVE('',#14923,#14921,#12236,.T.) ;
#19241=EDGE_CURVE('',#14923,#14924,#8090,.T.) ;
#19242=EDGE_CURVE('',#14924,#14925,#12237,.T.) ;
#19243=EDGE_CURVE('',#14925,#14921,#1534,.T.) ;
#19244=EDGE_CURVE('',#14924,#14920,#8091,.T.) ;
#19245=EDGE_CURVE('',#14914,#14925,#1535,.T.) ;
#19246=EDGE_CURVE('',#14919,#14926,#8092,.T.) ;
#19247=EDGE_CURVE('',#14927,#14926,#12238,.T.) ;
#19248=EDGE_CURVE('',#14927,#14880,#8093,.T.) ;
#19249=EDGE_CURVE('',#14928,#14922,#8094,.T.) ;
#19250=EDGE_CURVE('',#14929,#14928,#8095,.T.) ;
#19251=EDGE_CURVE('',#14930,#14929,#12239,.T.) ;
#19252=EDGE_CURVE('',#14926,#14930,#162,.T.) ;
#19253=EDGE_CURVE('',#14931,#14932,#12240,.T.) ;
#19254=EDGE_CURVE('',#14932,#14933,#163,.T.) ;
#19255=EDGE_CURVE('',#14933,#14931,#164,.T.) ;
#19256=EDGE_CURVE('',#14931,#14934,#8096,.T.) ;
#19257=EDGE_CURVE('',#14934,#14935,#12241,.T.) ;
#19258=EDGE_CURVE('',#14935,#14932,#8097,.T.) ;
#19259=EDGE_CURVE('',#14934,#14936,#12242,.T.) ;
#19260=EDGE_CURVE('',#14936,#14935,#12243,.T.) ;
#19261=EDGE_CURVE('',#14934,#14937,#12244,.T.) ;
#19262=EDGE_CURVE('',#14938,#14937,#1536,.T.) ;
#19263=EDGE_CURVE('',#14938,#14936,#12245,.T.) ;
#19264=EDGE_CURVE('',#14939,#14931,#8098,.T.) ;
#19265=EDGE_CURVE('',#14940,#14939,#1537,.T.) ;
#19266=EDGE_CURVE('',#14937,#14940,#165,.T.) ;
#19267=EDGE_CURVE('',#14933,#14941,#8099,.T.) ;
#19268=EDGE_CURVE('',#14939,#14941,#12246,.T.) ;
#19269=EDGE_CURVE('',#14942,#14938,#1538,.T.) ;
#19270=EDGE_CURVE('',#14937,#14942,#12247,.T.) ;
#19271=EDGE_CURVE('',#14940,#14943,#12248,.T.) ;
#19272=EDGE_CURVE('',#14943,#14942,#166,.T.) ;
#19273=EDGE_CURVE('',#14939,#14944,#12249,.T.) ;
#19274=EDGE_CURVE('',#14944,#14943,#1539,.T.) ;
#19275=EDGE_CURVE('',#14941,#14944,#12250,.T.) ;
#19276=EDGE_CURVE('',#14945,#14946,#12251,.T.) ;
#19277=EDGE_CURVE('',#14946,#14947,#12252,.T.) ;
#19278=EDGE_CURVE('',#14947,#14945,#12253,.T.) ;
#19279=EDGE_CURVE('',#14948,#14949,#12254,.T.) ;
#19280=EDGE_CURVE('',#14949,#14946,#1540,.T.) ;
#19281=EDGE_CURVE('',#14945,#14948,#1541,.T.) ;
#19282=EDGE_CURVE('',#14950,#14951,#12255,.T.) ;
#19283=EDGE_CURVE('',#14951,#14949,#167,.T.) ;
#19284=EDGE_CURVE('',#14948,#14950,#168,.T.) ;
#19285=EDGE_CURVE('',#14950,#14952,#1542,.T.) ;
#19286=EDGE_CURVE('',#14952,#14951,#1543,.T.) ;
#19287=EDGE_CURVE('',#14950,#14953,#12256,.T.) ;
#19288=EDGE_CURVE('',#14954,#14953,#12257,.T.) ;
#19289=EDGE_CURVE('',#14954,#14952,#12258,.T.) ;
#19290=EDGE_CURVE('',#14955,#14945,#8100,.T.) ;
#19291=EDGE_CURVE('',#14953,#14955,#8101,.T.) ;
#19292=EDGE_CURVE('',#14947,#14956,#8102,.T.) ;
#19293=EDGE_CURVE('',#14955,#14956,#169,.T.) ;
#19294=EDGE_CURVE('',#14957,#14955,#12259,.T.) ;
#19295=EDGE_CURVE('',#14956,#14957,#170,.T.) ;
#19296=EDGE_CURVE('',#14957,#14958,#8103,.T.) ;
#19297=EDGE_CURVE('',#14958,#14953,#12260,.T.) ;
#19298=EDGE_CURVE('',#14958,#14954,#12261,.T.) ;
#19299=EDGE_CURVE('',#14959,#14957,#8104,.T.) ;
#19300=EDGE_CURVE('',#14960,#14959,#8105,.T.) ;
#19301=EDGE_CURVE('',#14961,#14960,#171,.T.) ;
#19302=EDGE_CURVE('',#14962,#14961,#8106,.T.) ;
#19303=EDGE_CURVE('',#14958,#14962,#12262,.T.) ;
#19304=EDGE_CURVE('',#14956,#14963,#8107,.T.) ;
#19305=EDGE_CURVE('',#14959,#14963,#172,.T.) ;
#19306=EDGE_CURVE('',#14964,#14965,#12263,.T.) ;
#19307=EDGE_CURVE('',#14965,#14966,#12264,.T.) ;
#19308=EDGE_CURVE('',#14966,#14964,#12265,.T.) ;
#19309=EDGE_CURVE('',#14967,#14968,#12266,.T.) ;
#19310=EDGE_CURVE('',#14968,#14965,#1544,.T.) ;
#19311=EDGE_CURVE('',#14964,#14967,#1545,.T.) ;
#19312=EDGE_CURVE('',#14967,#14969,#173,.T.) ;
#19313=EDGE_CURVE('',#14969,#14970,#12267,.T.) ;
#19314=EDGE_CURVE('',#14970,#14968,#174,.T.) ;
#19315=EDGE_CURVE('',#14969,#14971,#1546,.T.) ;
#19316=EDGE_CURVE('',#14971,#14970,#1547,.T.) ;
#19317=EDGE_CURVE('',#14967,#14972,#12268,.T.) ;
#19318=EDGE_CURVE('',#14973,#14972,#175,.T.) ;
#19319=EDGE_CURVE('',#14974,#14973,#1548,.T.) ;
#19320=EDGE_CURVE('',#14974,#14971,#12269,.T.) ;
#19321=EDGE_CURVE('',#14975,#14964,#12270,.T.) ;
#19322=EDGE_CURVE('',#14972,#14975,#1549,.T.) ;
#19323=EDGE_CURVE('',#14966,#14976,#12271,.T.) ;
#19324=EDGE_CURVE('',#14975,#14976,#12272,.T.) ;
#19325=EDGE_CURVE('',#14965,#14977,#8108,.T.) ;
#19326=EDGE_CURVE('',#14978,#14977,#176,.T.) ;
#19327=EDGE_CURVE('',#14978,#14966,#8109,.T.) ;
#19328=EDGE_CURVE('',#14979,#14975,#12273,.T.) ;
#19329=EDGE_CURVE('',#14976,#14979,#12274,.T.) ;
#19330=EDGE_CURVE('',#14980,#14972,#12275,.T.) ;
#19331=EDGE_CURVE('',#14979,#14980,#1550,.T.) ;
#19332=EDGE_CURVE('',#14981,#14973,#12276,.T.) ;
#19333=EDGE_CURVE('',#14980,#14981,#177,.T.) ;
#19334=EDGE_CURVE('',#14981,#14974,#1551,.T.) ;
#19335=EDGE_CURVE('',#14981,#14982,#12277,.T.) ;
#19336=EDGE_CURVE('',#14983,#14982,#12278,.T.) ;
#19337=EDGE_CURVE('',#14983,#14974,#12279,.T.) ;
#19338=EDGE_CURVE('',#14984,#14979,#8110,.T.) ;
#19339=EDGE_CURVE('',#14982,#14984,#8111,.T.) ;
#19340=EDGE_CURVE('',#14976,#14985,#8112,.T.) ;
#19341=EDGE_CURVE('',#14984,#14985,#178,.T.) ;
#19342=EDGE_CURVE('',#14986,#14984,#12280,.T.) ;
#19343=EDGE_CURVE('',#14985,#14986,#179,.T.) ;
#19344=EDGE_CURVE('',#14986,#14987,#8113,.T.) ;
#19345=EDGE_CURVE('',#14987,#14982,#12281,.T.) ;
#19346=EDGE_CURVE('',#14987,#14983,#12282,.T.) ;
#19347=EDGE_CURVE('',#14988,#14986,#8114,.T.) ;
#19348=EDGE_CURVE('',#14989,#14988,#8115,.T.) ;
#19349=EDGE_CURVE('',#14990,#14989,#180,.T.) ;
#19350=EDGE_CURVE('',#14991,#14990,#8116,.T.) ;
#19351=EDGE_CURVE('',#14987,#14991,#12283,.T.) ;
#19352=EDGE_CURVE('',#14985,#14992,#8117,.T.) ;
#19353=EDGE_CURVE('',#14988,#14992,#181,.T.) ;
#19354=EDGE_CURVE('',#14977,#14993,#12284,.T.) ;
#19355=EDGE_CURVE('',#14993,#14978,#182,.T.) ;
#19356=EDGE_CURVE('',#14977,#14994,#8118,.T.) ;
#19357=EDGE_CURVE('',#14994,#14995,#12285,.T.) ;
#19358=EDGE_CURVE('',#14995,#14993,#8119,.T.) ;
#19359=EDGE_CURVE('',#14994,#14996,#12286,.T.) ;
#19360=EDGE_CURVE('',#14996,#14995,#12287,.T.) ;
#19361=EDGE_CURVE('',#14994,#14970,#12288,.T.) ;
#19362=EDGE_CURVE('',#14993,#14997,#8120,.T.) ;
#19363=EDGE_CURVE('',#14998,#14997,#183,.T.) ;
#19364=EDGE_CURVE('',#14998,#14978,#8121,.T.) ;
#19365=EDGE_CURVE('',#14999,#15000,#1552,.T.) ;
#19366=EDGE_CURVE('',#14999,#15001,#1553,.T.) ;
#19367=EDGE_CURVE('',#15001,#15002,#1554,.T.) ;
#19368=EDGE_CURVE('',#15002,#15003,#184,.T.) ;
#19369=EDGE_CURVE('',#15003,#15004,#12289,.T.) ;
#19370=EDGE_CURVE('',#15004,#15005,#1555,.T.) ;
#19371=EDGE_CURVE('',#15005,#15006,#1556,.T.) ;
#19372=EDGE_CURVE('',#15006,#15000,#1557,.T.) ;
#19373=EDGE_CURVE('',#14855,#15002,#1558,.T.) ;
#19374=EDGE_CURVE('',#15001,#15007,#12290,.T.) ;
#19375=EDGE_CURVE('',#15007,#14856,#1559,.T.) ;
#19376=EDGE_CURVE('',#14823,#15000,#1560,.T.) ;
#19377=EDGE_CURVE('',#14822,#15008,#1561,.T.) ;
#19378=EDGE_CURVE('',#15008,#15009,#1562,.T.) ;
#19379=EDGE_CURVE('',#15009,#15010,#185,.T.) ;
#19380=EDGE_CURVE('',#15010,#14857,#12291,.T.) ;
#19381=EDGE_CURVE('',#15007,#14999,#1563,.T.) ;
#19382=EDGE_CURVE('',#14858,#14842,#1564,.T.) ;
#19383=EDGE_CURVE('',#15011,#15012,#12292,.T.) ;
#19384=EDGE_CURVE('',#15012,#15013,#186,.T.) ;
#19385=EDGE_CURVE('',#15013,#15014,#187,.T.) ;
#19386=EDGE_CURVE('',#15014,#15015,#188,.T.) ;
#19387=EDGE_CURVE('',#15015,#15016,#8122,.T.) ;
#19388=EDGE_CURVE('',#15016,#15017,#8123,.T.) ;
#19389=EDGE_CURVE('',#15017,#15018,#189,.T.) ;
#19390=EDGE_CURVE('',#15018,#15019,#190,.T.) ;
#19391=EDGE_CURVE('',#15019,#15011,#191,.T.) ;
#19392=EDGE_CURVE('',#15020,#15021,#12293,.T.) ;
#19393=EDGE_CURVE('',#15021,#15012,#192,.T.) ;
#19394=EDGE_CURVE('',#15011,#15020,#193,.T.) ;
#19395=EDGE_CURVE('',#15020,#15022,#8124,.T.) ;
#19396=EDGE_CURVE('',#15022,#15023,#12294,.T.) ;
#19397=EDGE_CURVE('',#15023,#15021,#8125,.T.) ;
#19398=EDGE_CURVE('',#15022,#15024,#12295,.T.) ;
#19399=EDGE_CURVE('',#15024,#15023,#12296,.T.) ;
#19400=EDGE_CURVE('',#15025,#15020,#8126,.T.) ;
#19401=EDGE_CURVE('',#15026,#15025,#8127,.T.) ;
#19402=EDGE_CURVE('',#15022,#15026,#8128,.T.) ;
#19403=EDGE_CURVE('',#15016,#15027,#8129,.T.) ;
#19404=EDGE_CURVE('',#15027,#15025,#12297,.F.) ;
#19405=EDGE_CURVE('',#15012,#15028,#12298,.T.) ;
#19406=EDGE_CURVE('',#15029,#15028,#1565,.T.) ;
#19407=EDGE_CURVE('',#15030,#15029,#1566,.T.) ;
#19408=EDGE_CURVE('',#15030,#15016,#12299,.T.) ;
#19409=EDGE_CURVE('',#15031,#15032,#12300,.T.) ;
#19410=EDGE_CURVE('',#15032,#15033,#12301,.T.) ;
#19411=EDGE_CURVE('',#15033,#15031,#12302,.T.) ;
#19412=EDGE_CURVE('',#15034,#15035,#12303,.T.) ;
#19413=EDGE_CURVE('',#15035,#15032,#8130,.T.) ;
#19414=EDGE_CURVE('',#15031,#15034,#8131,.T.) ;
#19415=EDGE_CURVE('',#15034,#15036,#194,.T.) ;
#19416=EDGE_CURVE('',#15036,#15028,#12304,.T.) ;
#19417=EDGE_CURVE('',#15028,#15035,#195,.T.) ;
#19418=EDGE_CURVE('',#15036,#15037,#1567,.T.) ;
#19419=EDGE_CURVE('',#15037,#15030,#1568,.T.) ;
#19420=EDGE_CURVE('',#15034,#15038,#8132,.T.) ;
#19421=EDGE_CURVE('',#15038,#15039,#12305,.F.) ;
#19422=EDGE_CURVE('',#15039,#15030,#8133,.T.) ;
#19423=EDGE_CURVE('',#15040,#15031,#8134,.T.) ;
#19424=EDGE_CURVE('',#15038,#15040,#8135,.T.) ;
#19425=EDGE_CURVE('',#15033,#15041,#8136,.T.) ;
#19426=EDGE_CURVE('',#15040,#15041,#196,.T.) ;
#19427=EDGE_CURVE('',#15042,#15039,#8137,.T.) ;
#19428=EDGE_CURVE('',#14885,#15042,#8138,.T.) ;
#19429=EDGE_CURVE('',#15043,#14867,#8139,.T.) ;
#19430=EDGE_CURVE('',#15027,#15043,#8140,.T.) ;
#19431=EDGE_CURVE('',#14997,#15044,#12306,.T.) ;
#19432=EDGE_CURVE('',#15044,#14998,#197,.T.) ;
#19433=EDGE_CURVE('',#15045,#15046,#12307,.T.) ;
#19434=EDGE_CURVE('',#15046,#15044,#8141,.T.) ;
#19435=EDGE_CURVE('',#14997,#15045,#8142,.T.) ;
#19436=EDGE_CURVE('',#15042,#15045,#12308,.T.) ;
#19437=EDGE_CURVE('',#15045,#15047,#198,.T.) ;
#19438=EDGE_CURVE('',#15047,#14899,#12309,.T.) ;
#19439=EDGE_CURVE('',#14899,#15042,#199,.T.) ;
#19440=EDGE_CURVE('',#15048,#14900,#12310,.T.) ;
#19441=EDGE_CURVE('',#15047,#15048,#8143,.T.) ;
#19442=EDGE_CURVE('',#15048,#15049,#12311,.T.) ;
#19443=EDGE_CURVE('',#15049,#14900,#12312,.T.) ;
#19444=EDGE_CURVE('',#15042,#15046,#12313,.T.) ;
#19445=EDGE_CURVE('',#15044,#15050,#8144,.T.) ;
#19446=EDGE_CURVE('',#15041,#15050,#200,.T.) ;
#19447=EDGE_CURVE('',#15041,#14998,#8145,.T.) ;
#19448=EDGE_CURVE('',#15051,#15046,#8146,.T.) ;
#19449=EDGE_CURVE('',#15050,#15051,#8147,.T.) ;
#19450=EDGE_CURVE('',#15051,#15038,#12314,.F.) ;
#19451=EDGE_CURVE('',#15039,#15051,#12315,.F.) ;
#19452=EDGE_CURVE('',#15040,#15050,#12316,.T.) ;
#19453=EDGE_CURVE('',#15052,#14961,#12317,.T.) ;
#19454=EDGE_CURVE('',#14960,#15043,#12318,.T.) ;
#19455=EDGE_CURVE('',#15043,#15052,#201,.T.) ;
#19456=EDGE_CURVE('',#15053,#14962,#12319,.T.) ;
#19457=EDGE_CURVE('',#15052,#15053,#8148,.T.) ;
#19458=EDGE_CURVE('',#15053,#15054,#12320,.T.) ;
#19459=EDGE_CURVE('',#15054,#14962,#12321,.T.) ;
#19460=EDGE_CURVE('',#15055,#14960,#12322,.T.) ;
#19461=EDGE_CURVE('',#14959,#15056,#12323,.T.) ;
#19462=EDGE_CURVE('',#15056,#15055,#8149,.T.) ;
#19463=EDGE_CURVE('',#14963,#15056,#202,.T.) ;
#19464=EDGE_CURVE('',#15055,#15043,#12324,.T.) ;
#19465=EDGE_CURVE('',#15054,#14954,#12325,.T.) ;
#19466=EDGE_CURVE('',#15053,#15057,#12326,.T.) ;
#19467=EDGE_CURVE('',#15058,#15057,#12327,.T.) ;
#19468=EDGE_CURVE('',#15058,#15054,#12328,.T.) ;
#19469=EDGE_CURVE('',#15059,#14864,#8150,.T.) ;
#19470=EDGE_CURVE('',#15057,#15059,#203,.T.) ;
#19471=EDGE_CURVE('',#14870,#15052,#8151,.T.) ;
#19472=EDGE_CURVE('',#15060,#15056,#8152,.T.) ;
#19473=EDGE_CURVE('',#15061,#15060,#8153,.T.) ;
#19474=EDGE_CURVE('',#15055,#15061,#8154,.T.) ;
#19475=EDGE_CURVE('',#15025,#15061,#12329,.F.) ;
#19476=EDGE_CURVE('',#15061,#15027,#12330,.F.) ;
#19477=EDGE_CURVE('',#15060,#15026,#12331,.T.) ;
#19478=EDGE_CURVE('',#15060,#15062,#204,.T.) ;
#19479=EDGE_CURVE('',#15062,#15026,#205,.T.) ;
#19480=EDGE_CURVE('',#15062,#15024,#8155,.T.) ;
#19481=EDGE_CURVE('',#14963,#15062,#8156,.T.) ;
#19482=EDGE_CURVE('',#15063,#14908,#8157,.T.) ;
#19483=EDGE_CURVE('',#14911,#15064,#8158,.T.) ;
#19484=EDGE_CURVE('',#15063,#15064,#206,.T.) ;
#19485=EDGE_CURVE('',#15065,#15066,#12332,.T.) ;
#19486=EDGE_CURVE('',#15066,#15067,#207,.T.) ;
#19487=EDGE_CURVE('',#15067,#15068,#208,.T.) ;
#19488=EDGE_CURVE('',#15068,#15069,#209,.T.) ;
#19489=EDGE_CURVE('',#15069,#15070,#8159,.T.) ;
#19490=EDGE_CURVE('',#15070,#15071,#8160,.T.) ;
#19491=EDGE_CURVE('',#15071,#15072,#210,.T.) ;
#19492=EDGE_CURVE('',#15072,#15073,#211,.T.) ;
#19493=EDGE_CURVE('',#15073,#15065,#212,.T.) ;
#19494=EDGE_CURVE('',#15074,#15075,#12333,.T.) ;
#19495=EDGE_CURVE('',#15075,#15066,#213,.T.) ;
#19496=EDGE_CURVE('',#15065,#15074,#214,.T.) ;
#19497=EDGE_CURVE('',#15074,#15076,#8161,.T.) ;
#19498=EDGE_CURVE('',#15076,#15077,#12334,.T.) ;
#19499=EDGE_CURVE('',#15077,#15075,#8162,.T.) ;
#19500=EDGE_CURVE('',#15076,#15078,#12335,.T.) ;
#19501=EDGE_CURVE('',#15078,#15077,#12336,.T.) ;
#19502=EDGE_CURVE('',#15079,#15074,#8163,.T.) ;
#19503=EDGE_CURVE('',#15080,#15079,#8164,.T.) ;
#19504=EDGE_CURVE('',#15076,#15080,#8165,.T.) ;
#19505=EDGE_CURVE('',#15070,#15081,#8166,.T.) ;
#19506=EDGE_CURVE('',#15081,#15079,#12337,.F.) ;
#19507=EDGE_CURVE('',#15066,#15082,#12338,.T.) ;
#19508=EDGE_CURVE('',#15083,#15082,#1569,.T.) ;
#19509=EDGE_CURVE('',#15084,#15083,#1570,.T.) ;
#19510=EDGE_CURVE('',#15084,#15070,#12339,.T.) ;
#19511=EDGE_CURVE('',#15085,#15086,#12340,.T.) ;
#19512=EDGE_CURVE('',#15086,#15087,#12341,.T.) ;
#19513=EDGE_CURVE('',#15087,#15085,#12342,.T.) ;
#19514=EDGE_CURVE('',#15088,#15089,#12343,.T.) ;
#19515=EDGE_CURVE('',#15089,#15086,#8167,.T.) ;
#19516=EDGE_CURVE('',#15085,#15088,#8168,.T.) ;
#19517=EDGE_CURVE('',#15088,#15090,#215,.T.) ;
#19518=EDGE_CURVE('',#15090,#15082,#12344,.T.) ;
#19519=EDGE_CURVE('',#15082,#15089,#216,.T.) ;
#19520=EDGE_CURVE('',#15090,#15091,#1571,.T.) ;
#19521=EDGE_CURVE('',#15091,#15084,#1572,.T.) ;
#19522=EDGE_CURVE('',#15088,#15092,#8169,.T.) ;
#19523=EDGE_CURVE('',#15092,#15093,#12345,.F.) ;
#19524=EDGE_CURVE('',#15093,#15084,#8170,.T.) ;
#19525=EDGE_CURVE('',#15094,#15085,#8171,.T.) ;
#19526=EDGE_CURVE('',#15092,#15094,#8172,.T.) ;
#19527=EDGE_CURVE('',#15087,#15095,#8173,.T.) ;
#19528=EDGE_CURVE('',#15094,#15095,#217,.T.) ;
#19529=EDGE_CURVE('',#15081,#15063,#8174,.T.) ;
#19530=EDGE_CURVE('',#15096,#15093,#8175,.T.) ;
#19531=EDGE_CURVE('',#14914,#15096,#8176,.T.) ;
#19532=EDGE_CURVE('',#15097,#15098,#12346,.T.) ;
#19533=EDGE_CURVE('',#15098,#15099,#8177,.T.) ;
#19534=EDGE_CURVE('',#15099,#15100,#12347,.T.) ;
#19535=EDGE_CURVE('',#15100,#15097,#8178,.T.) ;
#19536=EDGE_CURVE('',#15099,#15101,#218,.T.) ;
#19537=EDGE_CURVE('',#15101,#15100,#219,.T.) ;
#19538=EDGE_CURVE('',#15096,#15097,#12348,.T.) ;
#19539=EDGE_CURVE('',#15097,#15102,#220,.T.) ;
#19540=EDGE_CURVE('',#15102,#14928,#12349,.T.) ;
#19541=EDGE_CURVE('',#14928,#15096,#221,.T.) ;
#19542=EDGE_CURVE('',#15103,#14929,#12350,.T.) ;
#19543=EDGE_CURVE('',#15102,#15103,#8179,.T.) ;
#19544=EDGE_CURVE('',#15103,#15104,#12351,.T.) ;
#19545=EDGE_CURVE('',#15104,#14929,#12352,.T.) ;
#19546=EDGE_CURVE('',#15096,#15098,#12353,.T.) ;
#19547=EDGE_CURVE('',#14932,#15100,#8180,.T.) ;
#19548=EDGE_CURVE('',#15101,#14933,#8181,.T.) ;
#19549=EDGE_CURVE('',#15099,#15105,#8182,.T.) ;
#19550=EDGE_CURVE('',#15095,#15105,#222,.T.) ;
#19551=EDGE_CURVE('',#15095,#15101,#8183,.T.) ;
#19552=EDGE_CURVE('',#15106,#15098,#8184,.T.) ;
#19553=EDGE_CURVE('',#15105,#15106,#8185,.T.) ;
#19554=EDGE_CURVE('',#15106,#15092,#12354,.F.) ;
#19555=EDGE_CURVE('',#15093,#15106,#12355,.F.) ;
#19556=EDGE_CURVE('',#15105,#15094,#12356,.T.) ;
#19557=EDGE_CURVE('',#15103,#14935,#12357,.T.) ;
#19558=EDGE_CURVE('',#15064,#14990,#12358,.T.) ;
#19559=EDGE_CURVE('',#14989,#15063,#12359,.T.) ;
#19560=EDGE_CURVE('',#15107,#14991,#12360,.T.) ;
#19561=EDGE_CURVE('',#15064,#15107,#8186,.T.) ;
#19562=EDGE_CURVE('',#15107,#15108,#12361,.T.) ;
#19563=EDGE_CURVE('',#15108,#14991,#12362,.T.) ;
#19564=EDGE_CURVE('',#15109,#14989,#12363,.T.) ;
#19565=EDGE_CURVE('',#14988,#15110,#12364,.T.) ;
#19566=EDGE_CURVE('',#15110,#15109,#8187,.T.) ;
#19567=EDGE_CURVE('',#14992,#15110,#223,.T.) ;
#19568=EDGE_CURVE('',#15109,#15063,#12365,.T.) ;
#19569=EDGE_CURVE('',#15108,#14983,#12366,.T.) ;
#19570=EDGE_CURVE('',#15107,#15111,#12367,.T.) ;
#19571=EDGE_CURVE('',#15111,#15112,#12368,.T.) ;
#19572=EDGE_CURVE('',#15112,#15108,#12369,.T.) ;
#19573=EDGE_CURVE('',#15113,#14905,#8188,.T.) ;
#19574=EDGE_CURVE('',#15111,#15113,#1573,.T.) ;
#19575=EDGE_CURVE('',#15114,#15110,#8189,.T.) ;
#19576=EDGE_CURVE('',#15115,#15114,#8190,.T.) ;
#19577=EDGE_CURVE('',#15109,#15115,#8191,.T.) ;
#19578=EDGE_CURVE('',#15079,#15115,#12370,.F.) ;
#19579=EDGE_CURVE('',#15115,#15081,#12371,.F.) ;
#19580=EDGE_CURVE('',#15114,#15080,#12372,.T.) ;
#19581=EDGE_CURVE('',#15114,#15116,#224,.T.) ;
#19582=EDGE_CURVE('',#15116,#15080,#225,.T.) ;
#19583=EDGE_CURVE('',#15116,#15078,#8192,.T.) ;
#19584=EDGE_CURVE('',#14992,#15116,#8193,.T.) ;
#19585=EDGE_CURVE('',#15024,#15033,#12373,.T.) ;
#19586=EDGE_CURVE('',#15032,#15023,#12374,.T.) ;
#19587=EDGE_CURVE('',#14941,#14947,#12375,.T.) ;
#19588=EDGE_CURVE('',#14946,#14944,#12376,.T.) ;
#19589=EDGE_CURVE('',#15078,#15087,#12377,.T.) ;
#19590=EDGE_CURVE('',#15086,#15077,#12378,.T.) ;
#19591=EDGE_CURVE('',#15048,#14995,#12379,.T.) ;
#19592=EDGE_CURVE('',#15104,#15117,#12380,.T.) ;
#19593=EDGE_CURVE('',#15117,#14930,#12381,.T.) ;
#19594=EDGE_CURVE('',#15117,#14927,#1574,.T.) ;
#19595=EDGE_CURVE('',#14936,#15104,#12382,.T.) ;
#19596=EDGE_CURVE('',#14943,#14949,#12383,.T.) ;
#19597=EDGE_CURVE('',#14952,#14938,#12384,.T.) ;
#19598=EDGE_CURVE('',#14861,#15118,#8194,.T.) ;
#19599=EDGE_CURVE('',#15118,#15059,#12385,.T.) ;
#19600=EDGE_CURVE('',#15118,#15058,#1575,.T.) ;
#19601=EDGE_CURVE('',#15058,#15117,#12386,.T.) ;
#19602=EDGE_CURVE('',#15118,#14927,#12387,.T.) ;
#19603=EDGE_CURVE('',#14901,#15119,#12388,.T.) ;
#19604=EDGE_CURVE('',#15119,#14898,#1576,.T.) ;
#19605=EDGE_CURVE('',#15049,#15119,#12389,.T.) ;
#19606=EDGE_CURVE('',#14996,#15049,#12390,.T.) ;
#19607=EDGE_CURVE('',#14971,#14996,#12391,.T.) ;
#19608=EDGE_CURVE('',#15113,#15120,#12392,.T.) ;
#19609=EDGE_CURVE('',#15120,#15112,#1577,.T.) ;
#19610=EDGE_CURVE('',#14874,#15120,#8195,.T.) ;
#19611=EDGE_CURVE('',#15112,#15119,#12393,.T.) ;
#19612=EDGE_CURVE('',#15120,#14898,#12394,.T.) ;
#19613=EDGE_CURVE('',#14841,#15121,#1578,.F.) ;
#19614=EDGE_CURVE('',#15121,#15122,#8196,.T.) ;
#19615=EDGE_CURVE('',#15122,#15122,#12395,.T.) ;
#19616=EDGE_CURVE('',#15121,#14838,#1579,.F.) ;
#27364=ORIENTED_EDGE('',*,*,#19088,.F.) ;
#27365=ORIENTED_EDGE('',*,*,#19089,.T.) ;
#27366=ORIENTED_EDGE('',*,*,#19090,.T.) ;
#27367=ORIENTED_EDGE('',*,*,#19091,.F.) ;
#27368=ORIENTED_EDGE('',*,*,#19092,.F.) ;
#27369=ORIENTED_EDGE('',*,*,#19093,.T.) ;
#27370=ORIENTED_EDGE('',*,*,#19088,.T.) ;
#27371=ORIENTED_EDGE('',*,*,#19094,.F.) ;
#27372=ORIENTED_EDGE('',*,*,#19095,.F.) ;
#27373=ORIENTED_EDGE('',*,*,#19096,.T.) ;
#27374=ORIENTED_EDGE('',*,*,#19092,.T.) ;
#27375=ORIENTED_EDGE('',*,*,#19097,.F.) ;
#27376=ORIENTED_EDGE('',*,*,#19098,.F.) ;
#27377=ORIENTED_EDGE('',*,*,#19099,.T.) ;
#27378=ORIENTED_EDGE('',*,*,#19095,.T.) ;
#27379=ORIENTED_EDGE('',*,*,#19100,.F.) ;
#27380=ORIENTED_EDGE('',*,*,#19101,.F.) ;
#27381=ORIENTED_EDGE('',*,*,#19102,.T.) ;
#27382=ORIENTED_EDGE('',*,*,#19098,.T.) ;
#27383=ORIENTED_EDGE('',*,*,#19103,.F.) ;
#27384=ORIENTED_EDGE('',*,*,#19104,.F.) ;
#27385=ORIENTED_EDGE('',*,*,#19105,.T.) ;
#27386=ORIENTED_EDGE('',*,*,#19101,.T.) ;
#27387=ORIENTED_EDGE('',*,*,#19106,.F.) ;
#27388=ORIENTED_EDGE('',*,*,#19107,.F.) ;
#27389=ORIENTED_EDGE('',*,*,#19108,.T.) ;
#27390=ORIENTED_EDGE('',*,*,#19104,.T.) ;
#27391=ORIENTED_EDGE('',*,*,#19109,.F.) ;
#27392=ORIENTED_EDGE('',*,*,#19110,.F.) ;
#27393=ORIENTED_EDGE('',*,*,#19111,.F.) ;
#27394=ORIENTED_EDGE('',*,*,#19112,.T.) ;
#27395=ORIENTED_EDGE('',*,*,#19107,.T.) ;
#27396=ORIENTED_EDGE('',*,*,#19113,.F.) ;
#27397=ORIENTED_EDGE('',*,*,#19114,.F.) ;
#27398=ORIENTED_EDGE('',*,*,#19115,.F.) ;
#27399=ORIENTED_EDGE('',*,*,#19116,.T.) ;
#27400=ORIENTED_EDGE('',*,*,#19117,.T.) ;
#27401=ORIENTED_EDGE('',*,*,#19118,.F.) ;
#27402=ORIENTED_EDGE('',*,*,#19119,.F.) ;
#27403=ORIENTED_EDGE('',*,*,#19114,.T.) ;
#27404=ORIENTED_EDGE('',*,*,#19120,.T.) ;
#27405=ORIENTED_EDGE('',*,*,#19121,.F.) ;
#27406=ORIENTED_EDGE('',*,*,#19122,.F.) ;
#27407=ORIENTED_EDGE('',*,*,#19118,.T.) ;
#27408=ORIENTED_EDGE('',*,*,#19123,.T.) ;
#27409=ORIENTED_EDGE('',*,*,#19124,.F.) ;
#27410=ORIENTED_EDGE('',*,*,#19125,.F.) ;
#27411=ORIENTED_EDGE('',*,*,#19121,.T.) ;
#27412=ORIENTED_EDGE('',*,*,#19126,.T.) ;
#27413=ORIENTED_EDGE('',*,*,#19127,.F.) ;
#27414=ORIENTED_EDGE('',*,*,#19128,.F.) ;
#27415=ORIENTED_EDGE('',*,*,#19124,.T.) ;
#27416=ORIENTED_EDGE('',*,*,#19129,.T.) ;
#27417=ORIENTED_EDGE('',*,*,#19130,.F.) ;
#27418=ORIENTED_EDGE('',*,*,#19131,.F.) ;
#27419=ORIENTED_EDGE('',*,*,#19127,.T.) ;
#27420=ORIENTED_EDGE('',*,*,#19132,.T.) ;
#27421=ORIENTED_EDGE('',*,*,#19133,.F.) ;
#27422=ORIENTED_EDGE('',*,*,#19134,.F.) ;
#27423=ORIENTED_EDGE('',*,*,#19130,.T.) ;
#27424=ORIENTED_EDGE('',*,*,#19135,.T.) ;
#27425=ORIENTED_EDGE('',*,*,#19133,.T.) ;
#27426=ORIENTED_EDGE('',*,*,#19136,.T.) ;
#27427=ORIENTED_EDGE('',*,*,#19137,.F.) ;
#27428=ORIENTED_EDGE('',*,*,#19138,.F.) ;
#27429=ORIENTED_EDGE('',*,*,#19139,.F.) ;
#27430=ORIENTED_EDGE('',*,*,#19110,.T.) ;
#27431=ORIENTED_EDGE('',*,*,#19140,.F.) ;
#27432=ORIENTED_EDGE('',*,*,#19141,.F.) ;
#27433=ORIENTED_EDGE('',*,*,#19142,.T.) ;
#27434=ORIENTED_EDGE('',*,*,#19143,.T.) ;
#27435=ORIENTED_EDGE('',*,*,#19144,.T.) ;
#27436=ORIENTED_EDGE('',*,*,#19142,.F.) ;
#27437=ORIENTED_EDGE('',*,*,#19145,.T.) ;
#27438=ORIENTED_EDGE('',*,*,#19146,.T.) ;
#27439=ORIENTED_EDGE('',*,*,#19147,.T.) ;
#27440=ORIENTED_EDGE('',*,*,#19148,.T.) ;
#27441=ORIENTED_EDGE('',*,*,#19149,.T.) ;
#27442=ORIENTED_EDGE('',*,*,#19146,.F.) ;
#27443=ORIENTED_EDGE('',*,*,#19150,.T.) ;
#27444=ORIENTED_EDGE('',*,*,#19151,.T.) ;
#27445=ORIENTED_EDGE('',*,*,#19152,.T.) ;
#27446=ORIENTED_EDGE('',*,*,#19148,.F.) ;
#27447=ORIENTED_EDGE('',*,*,#19153,.T.) ;
#27448=ORIENTED_EDGE('',*,*,#19154,.T.) ;
#27449=ORIENTED_EDGE('',*,*,#19155,.T.) ;
#27450=ORIENTED_EDGE('',*,*,#19156,.T.) ;
#27451=ORIENTED_EDGE('',*,*,#19157,.T.) ;
#27452=ORIENTED_EDGE('',*,*,#19158,.T.) ;
#27453=ORIENTED_EDGE('',*,*,#19154,.F.) ;
#27454=ORIENTED_EDGE('',*,*,#19159,.T.) ;
#27455=ORIENTED_EDGE('',*,*,#19157,.F.) ;
#27456=ORIENTED_EDGE('',*,*,#19160,.T.) ;
#27457=ORIENTED_EDGE('',*,*,#19151,.F.) ;
#27458=ORIENTED_EDGE('',*,*,#19161,.T.) ;
#27459=ORIENTED_EDGE('',*,*,#19147,.F.) ;
#27460=ORIENTED_EDGE('',*,*,#19162,.F.) ;
#27461=ORIENTED_EDGE('',*,*,#19163,.T.) ;
#27462=ORIENTED_EDGE('',*,*,#19164,.F.) ;
#27463=ORIENTED_EDGE('',*,*,#19165,.F.) ;
#27464=ORIENTED_EDGE('',*,*,#19166,.F.) ;
#27465=ORIENTED_EDGE('',*,*,#19167,.F.) ;
#27466=ORIENTED_EDGE('',*,*,#19168,.F.) ;
#27467=ORIENTED_EDGE('',*,*,#19169,.F.) ;
#27468=ORIENTED_EDGE('',*,*,#19170,.F.) ;
#27469=ORIENTED_EDGE('',*,*,#19143,.F.) ;
#27470=ORIENTED_EDGE('',*,*,#19163,.F.) ;
#27471=ORIENTED_EDGE('',*,*,#19171,.F.) ;
#27472=ORIENTED_EDGE('',*,*,#19172,.F.) ;
#27473=ORIENTED_EDGE('',*,*,#19173,.F.) ;
#27474=ORIENTED_EDGE('',*,*,#19174,.F.) ;
#27475=ORIENTED_EDGE('',*,*,#19175,.T.) ;
#27476=ORIENTED_EDGE('',*,*,#19176,.T.) ;
#27477=ORIENTED_EDGE('',*,*,#19175,.F.) ;
#27478=ORIENTED_EDGE('',*,*,#19149,.F.) ;
#27479=ORIENTED_EDGE('',*,*,#19152,.F.) ;
#27480=ORIENTED_EDGE('',*,*,#19177,.T.) ;
#27481=ORIENTED_EDGE('',*,*,#19178,.F.) ;
#27482=ORIENTED_EDGE('',*,*,#19179,.F.) ;
#27483=ORIENTED_EDGE('',*,*,#19180,.F.) ;
#27484=ORIENTED_EDGE('',*,*,#19171,.T.) ;
#27485=ORIENTED_EDGE('',*,*,#19162,.T.) ;
#27486=ORIENTED_EDGE('',*,*,#19181,.T.) ;
#27487=ORIENTED_EDGE('',*,*,#19182,.T.) ;
#27488=ORIENTED_EDGE('',*,*,#19173,.T.) ;
#27489=ORIENTED_EDGE('',*,*,#19183,.T.) ;
#27490=ORIENTED_EDGE('',*,*,#19184,.T.) ;
#27491=ORIENTED_EDGE('',*,*,#19181,.F.) ;
#27492=ORIENTED_EDGE('',*,*,#19185,.T.) ;
#27493=ORIENTED_EDGE('',*,*,#19186,.T.) ;
#27494=ORIENTED_EDGE('',*,*,#19187,.T.) ;
#27495=ORIENTED_EDGE('',*,*,#19183,.F.) ;
#27496=ORIENTED_EDGE('',*,*,#19179,.T.) ;
#27497=ORIENTED_EDGE('',*,*,#19188,.T.) ;
#27498=ORIENTED_EDGE('',*,*,#19189,.T.) ;
#27499=ORIENTED_EDGE('',*,*,#19186,.F.) ;
#27500=ORIENTED_EDGE('',*,*,#19178,.T.) ;
#27501=ORIENTED_EDGE('',*,*,#19190,.T.) ;
#27502=ORIENTED_EDGE('',*,*,#19191,.T.) ;
#27503=ORIENTED_EDGE('',*,*,#19192,.T.) ;
#27504=ORIENTED_EDGE('',*,*,#19192,.F.) ;
#27505=ORIENTED_EDGE('',*,*,#19193,.T.) ;
#27506=ORIENTED_EDGE('',*,*,#19194,.T.) ;
#27507=ORIENTED_EDGE('',*,*,#19195,.T.) ;
#27508=ORIENTED_EDGE('',*,*,#19194,.F.) ;
#27509=ORIENTED_EDGE('',*,*,#19196,.T.) ;
#27510=ORIENTED_EDGE('',*,*,#19188,.F.) ;
#27511=ORIENTED_EDGE('',*,*,#19197,.T.) ;
#27512=ORIENTED_EDGE('',*,*,#19182,.F.) ;
#27513=ORIENTED_EDGE('',*,*,#19184,.F.) ;
#27514=ORIENTED_EDGE('',*,*,#19187,.F.) ;
#27515=ORIENTED_EDGE('',*,*,#19198,.T.) ;
#27516=ORIENTED_EDGE('',*,*,#19199,.T.) ;
#27517=ORIENTED_EDGE('',*,*,#19200,.T.) ;
#27518=ORIENTED_EDGE('',*,*,#19189,.F.) ;
#27519=ORIENTED_EDGE('',*,*,#19196,.F.) ;
#27520=ORIENTED_EDGE('',*,*,#19193,.F.) ;
#27521=ORIENTED_EDGE('',*,*,#19191,.F.) ;
#27522=ORIENTED_EDGE('',*,*,#19201,.F.) ;
#27523=ORIENTED_EDGE('',*,*,#19202,.F.) ;
#27524=ORIENTED_EDGE('',*,*,#19203,.F.) ;
#27525=ORIENTED_EDGE('',*,*,#19204,.F.) ;
#27526=ORIENTED_EDGE('',*,*,#19198,.F.) ;
#27527=ORIENTED_EDGE('',*,*,#19205,.T.) ;
#27528=ORIENTED_EDGE('',*,*,#19165,.T.) ;
#27529=ORIENTED_EDGE('',*,*,#19206,.T.) ;
#27530=ORIENTED_EDGE('',*,*,#19205,.F.) ;
#27531=ORIENTED_EDGE('',*,*,#19207,.T.) ;
#27532=ORIENTED_EDGE('',*,*,#19208,.T.) ;
#27533=ORIENTED_EDGE('',*,*,#19209,.T.) ;
#27534=ORIENTED_EDGE('',*,*,#19210,.T.) ;
#27535=ORIENTED_EDGE('',*,*,#19211,.T.) ;
#27536=ORIENTED_EDGE('',*,*,#19208,.F.) ;
#27537=ORIENTED_EDGE('',*,*,#19212,.T.) ;
#27538=ORIENTED_EDGE('',*,*,#19213,.T.) ;
#27539=ORIENTED_EDGE('',*,*,#19214,.T.) ;
#27540=ORIENTED_EDGE('',*,*,#19210,.F.) ;
#27541=ORIENTED_EDGE('',*,*,#19215,.T.) ;
#27542=ORIENTED_EDGE('',*,*,#19216,.T.) ;
#27543=ORIENTED_EDGE('',*,*,#19217,.T.) ;
#27544=ORIENTED_EDGE('',*,*,#19218,.T.) ;
#27545=ORIENTED_EDGE('',*,*,#19219,.T.) ;
#27546=ORIENTED_EDGE('',*,*,#19220,.T.) ;
#27547=ORIENTED_EDGE('',*,*,#19216,.F.) ;
#27548=ORIENTED_EDGE('',*,*,#19221,.T.) ;
#27549=ORIENTED_EDGE('',*,*,#19219,.F.) ;
#27550=ORIENTED_EDGE('',*,*,#19222,.T.) ;
#27551=ORIENTED_EDGE('',*,*,#19213,.F.) ;
#27552=ORIENTED_EDGE('',*,*,#19223,.T.) ;
#27553=ORIENTED_EDGE('',*,*,#19209,.F.) ;
#27554=ORIENTED_EDGE('',*,*,#19224,.F.) ;
#27555=ORIENTED_EDGE('',*,*,#19166,.T.) ;
#27556=ORIENTED_EDGE('',*,*,#19211,.F.) ;
#27557=ORIENTED_EDGE('',*,*,#19214,.F.) ;
#27558=ORIENTED_EDGE('',*,*,#19225,.T.) ;
#27559=ORIENTED_EDGE('',*,*,#19226,.F.) ;
#27560=ORIENTED_EDGE('',*,*,#19227,.F.) ;
#27561=ORIENTED_EDGE('',*,*,#19228,.F.) ;
#27562=ORIENTED_EDGE('',*,*,#19167,.T.) ;
#27563=ORIENTED_EDGE('',*,*,#19224,.T.) ;
#27564=ORIENTED_EDGE('',*,*,#19229,.T.) ;
#27565=ORIENTED_EDGE('',*,*,#19230,.T.) ;
#27566=ORIENTED_EDGE('',*,*,#19169,.T.) ;
#27567=ORIENTED_EDGE('',*,*,#19231,.T.) ;
#27568=ORIENTED_EDGE('',*,*,#19232,.T.) ;
#27569=ORIENTED_EDGE('',*,*,#19229,.F.) ;
#27570=ORIENTED_EDGE('',*,*,#19233,.T.) ;
#27571=ORIENTED_EDGE('',*,*,#19234,.T.) ;
#27572=ORIENTED_EDGE('',*,*,#19235,.T.) ;
#27573=ORIENTED_EDGE('',*,*,#19231,.F.) ;
#27574=ORIENTED_EDGE('',*,*,#19227,.T.) ;
#27575=ORIENTED_EDGE('',*,*,#19236,.T.) ;
#27576=ORIENTED_EDGE('',*,*,#19237,.T.) ;
#27577=ORIENTED_EDGE('',*,*,#19234,.F.) ;
#27578=ORIENTED_EDGE('',*,*,#19226,.T.) ;
#27579=ORIENTED_EDGE('',*,*,#19238,.T.) ;
#27580=ORIENTED_EDGE('',*,*,#19239,.T.) ;
#27581=ORIENTED_EDGE('',*,*,#19240,.T.) ;
#27582=ORIENTED_EDGE('',*,*,#19240,.F.) ;
#27583=ORIENTED_EDGE('',*,*,#19241,.T.) ;
#27584=ORIENTED_EDGE('',*,*,#19242,.T.) ;
#27585=ORIENTED_EDGE('',*,*,#19243,.T.) ;
#27586=ORIENTED_EDGE('',*,*,#19242,.F.) ;
#27587=ORIENTED_EDGE('',*,*,#19244,.T.) ;
#27588=ORIENTED_EDGE('',*,*,#19236,.F.) ;
#27589=ORIENTED_EDGE('',*,*,#19245,.T.) ;
#27590=ORIENTED_EDGE('',*,*,#19230,.F.) ;
#27591=ORIENTED_EDGE('',*,*,#19232,.F.) ;
#27592=ORIENTED_EDGE('',*,*,#19235,.F.) ;
#27593=ORIENTED_EDGE('',*,*,#19246,.T.) ;
#27594=ORIENTED_EDGE('',*,*,#19247,.F.) ;
#27595=ORIENTED_EDGE('',*,*,#19248,.T.) ;
#27596=ORIENTED_EDGE('',*,*,#19237,.F.) ;
#27597=ORIENTED_EDGE('',*,*,#19244,.F.) ;
#27598=ORIENTED_EDGE('',*,*,#19241,.F.) ;
#27599=ORIENTED_EDGE('',*,*,#19239,.F.) ;
#27600=ORIENTED_EDGE('',*,*,#19249,.F.) ;
#27601=ORIENTED_EDGE('',*,*,#19250,.F.) ;
#27602=ORIENTED_EDGE('',*,*,#19251,.F.) ;
#27603=ORIENTED_EDGE('',*,*,#19252,.F.) ;
#27604=ORIENTED_EDGE('',*,*,#19246,.F.) ;
#27605=ORIENTED_EDGE('',*,*,#19253,.T.) ;
#27606=ORIENTED_EDGE('',*,*,#19254,.T.) ;
#27607=ORIENTED_EDGE('',*,*,#19255,.T.) ;
#27608=ORIENTED_EDGE('',*,*,#19253,.F.) ;
#27609=ORIENTED_EDGE('',*,*,#19256,.T.) ;
#27610=ORIENTED_EDGE('',*,*,#19257,.T.) ;
#27611=ORIENTED_EDGE('',*,*,#19258,.T.) ;
#27612=ORIENTED_EDGE('',*,*,#19257,.F.) ;
#27613=ORIENTED_EDGE('',*,*,#19259,.T.) ;
#27614=ORIENTED_EDGE('',*,*,#19260,.T.) ;
#27615=ORIENTED_EDGE('',*,*,#19259,.F.) ;
#27616=ORIENTED_EDGE('',*,*,#19261,.T.) ;
#27617=ORIENTED_EDGE('',*,*,#19262,.F.) ;
#27618=ORIENTED_EDGE('',*,*,#19263,.T.) ;
#27619=ORIENTED_EDGE('',*,*,#19256,.F.) ;
#27620=ORIENTED_EDGE('',*,*,#19264,.F.) ;
#27621=ORIENTED_EDGE('',*,*,#19265,.F.) ;
#27622=ORIENTED_EDGE('',*,*,#19266,.F.) ;
#27623=ORIENTED_EDGE('',*,*,#19261,.F.) ;
#27624=ORIENTED_EDGE('',*,*,#19255,.F.) ;
#27625=ORIENTED_EDGE('',*,*,#19267,.T.) ;
#27626=ORIENTED_EDGE('',*,*,#19268,.F.) ;
#27627=ORIENTED_EDGE('',*,*,#19264,.T.) ;
#27628=ORIENTED_EDGE('',*,*,#19269,.T.) ;
#27629=ORIENTED_EDGE('',*,*,#19262,.T.) ;
#27630=ORIENTED_EDGE('',*,*,#19270,.T.) ;
#27631=ORIENTED_EDGE('',*,*,#19271,.T.) ;
#27632=ORIENTED_EDGE('',*,*,#19272,.T.) ;
#27633=ORIENTED_EDGE('',*,*,#19270,.F.) ;
#27634=ORIENTED_EDGE('',*,*,#19266,.T.) ;
#27635=ORIENTED_EDGE('',*,*,#19271,.F.) ;
#27636=ORIENTED_EDGE('',*,*,#19265,.T.) ;
#27637=ORIENTED_EDGE('',*,*,#19273,.T.) ;
#27638=ORIENTED_EDGE('',*,*,#19274,.T.) ;
#27639=ORIENTED_EDGE('',*,*,#19273,.F.) ;
#27640=ORIENTED_EDGE('',*,*,#19268,.T.) ;
#27641=ORIENTED_EDGE('',*,*,#19275,.T.) ;
#27642=ORIENTED_EDGE('',*,*,#19276,.T.) ;
#27643=ORIENTED_EDGE('',*,*,#19277,.T.) ;
#27644=ORIENTED_EDGE('',*,*,#19278,.T.) ;
#27645=ORIENTED_EDGE('',*,*,#19279,.T.) ;
#27646=ORIENTED_EDGE('',*,*,#19280,.T.) ;
#27647=ORIENTED_EDGE('',*,*,#19276,.F.) ;
#27648=ORIENTED_EDGE('',*,*,#19281,.T.) ;
#27649=ORIENTED_EDGE('',*,*,#19282,.T.) ;
#27650=ORIENTED_EDGE('',*,*,#19283,.T.) ;
#27651=ORIENTED_EDGE('',*,*,#19279,.F.) ;
#27652=ORIENTED_EDGE('',*,*,#19284,.T.) ;
#27653=ORIENTED_EDGE('',*,*,#19285,.T.) ;
#27654=ORIENTED_EDGE('',*,*,#19286,.T.) ;
#27655=ORIENTED_EDGE('',*,*,#19282,.F.) ;
#27656=ORIENTED_EDGE('',*,*,#19285,.F.) ;
#27657=ORIENTED_EDGE('',*,*,#19287,.T.) ;
#27658=ORIENTED_EDGE('',*,*,#19288,.F.) ;
#27659=ORIENTED_EDGE('',*,*,#19289,.T.) ;
#27660=ORIENTED_EDGE('',*,*,#19284,.F.) ;
#27661=ORIENTED_EDGE('',*,*,#19281,.F.) ;
#27662=ORIENTED_EDGE('',*,*,#19290,.F.) ;
#27663=ORIENTED_EDGE('',*,*,#19291,.F.) ;
#27664=ORIENTED_EDGE('',*,*,#19287,.F.) ;
#27665=ORIENTED_EDGE('',*,*,#19278,.F.) ;
#27666=ORIENTED_EDGE('',*,*,#19292,.T.) ;
#27667=ORIENTED_EDGE('',*,*,#19293,.F.) ;
#27668=ORIENTED_EDGE('',*,*,#19290,.T.) ;
#27669=ORIENTED_EDGE('',*,*,#19294,.T.) ;
#27670=ORIENTED_EDGE('',*,*,#19293,.T.) ;
#27671=ORIENTED_EDGE('',*,*,#19295,.T.) ;
#27672=ORIENTED_EDGE('',*,*,#19294,.F.) ;
#27673=ORIENTED_EDGE('',*,*,#19296,.T.) ;
#27674=ORIENTED_EDGE('',*,*,#19297,.T.) ;
#27675=ORIENTED_EDGE('',*,*,#19291,.T.) ;
#27676=ORIENTED_EDGE('',*,*,#19297,.F.) ;
#27677=ORIENTED_EDGE('',*,*,#19298,.T.) ;
#27678=ORIENTED_EDGE('',*,*,#19288,.T.) ;
#27679=ORIENTED_EDGE('',*,*,#19296,.F.) ;
#27680=ORIENTED_EDGE('',*,*,#19299,.F.) ;
#27681=ORIENTED_EDGE('',*,*,#19300,.F.) ;
#27682=ORIENTED_EDGE('',*,*,#19301,.F.) ;
#27683=ORIENTED_EDGE('',*,*,#19302,.F.) ;
#27684=ORIENTED_EDGE('',*,*,#19303,.F.) ;
#27685=ORIENTED_EDGE('',*,*,#19295,.F.) ;
#27686=ORIENTED_EDGE('',*,*,#19304,.T.) ;
#27687=ORIENTED_EDGE('',*,*,#19305,.F.) ;
#27688=ORIENTED_EDGE('',*,*,#19299,.T.) ;
#27689=ORIENTED_EDGE('',*,*,#19306,.T.) ;
#27690=ORIENTED_EDGE('',*,*,#19307,.T.) ;
#27691=ORIENTED_EDGE('',*,*,#19308,.T.) ;
#27692=ORIENTED_EDGE('',*,*,#19309,.T.) ;
#27693=ORIENTED_EDGE('',*,*,#19310,.T.) ;
#27694=ORIENTED_EDGE('',*,*,#19306,.F.) ;
#27695=ORIENTED_EDGE('',*,*,#19311,.T.) ;
#27696=ORIENTED_EDGE('',*,*,#19309,.F.) ;
#27697=ORIENTED_EDGE('',*,*,#19312,.T.) ;
#27698=ORIENTED_EDGE('',*,*,#19313,.T.) ;
#27699=ORIENTED_EDGE('',*,*,#19314,.T.) ;
#27700=ORIENTED_EDGE('',*,*,#19315,.T.) ;
#27701=ORIENTED_EDGE('',*,*,#19316,.T.) ;
#27702=ORIENTED_EDGE('',*,*,#19313,.F.) ;
#27703=ORIENTED_EDGE('',*,*,#19315,.F.) ;
#27704=ORIENTED_EDGE('',*,*,#19312,.F.) ;
#27705=ORIENTED_EDGE('',*,*,#19317,.T.) ;
#27706=ORIENTED_EDGE('',*,*,#19318,.F.) ;
#27707=ORIENTED_EDGE('',*,*,#19319,.F.) ;
#27708=ORIENTED_EDGE('',*,*,#19320,.T.) ;
#27709=ORIENTED_EDGE('',*,*,#19311,.F.) ;
#27710=ORIENTED_EDGE('',*,*,#19321,.F.) ;
#27711=ORIENTED_EDGE('',*,*,#19322,.F.) ;
#27712=ORIENTED_EDGE('',*,*,#19317,.F.) ;
#27713=ORIENTED_EDGE('',*,*,#19308,.F.) ;
#27714=ORIENTED_EDGE('',*,*,#19323,.T.) ;
#27715=ORIENTED_EDGE('',*,*,#19324,.F.) ;
#27716=ORIENTED_EDGE('',*,*,#19321,.T.) ;
#27717=ORIENTED_EDGE('',*,*,#19307,.F.) ;
#27718=ORIENTED_EDGE('',*,*,#19325,.T.) ;
#27719=ORIENTED_EDGE('',*,*,#19326,.F.) ;
#27720=ORIENTED_EDGE('',*,*,#19327,.T.) ;
#27721=ORIENTED_EDGE('',*,*,#19328,.T.) ;
#27722=ORIENTED_EDGE('',*,*,#19324,.T.) ;
#27723=ORIENTED_EDGE('',*,*,#19329,.T.) ;
#27724=ORIENTED_EDGE('',*,*,#19330,.T.) ;
#27725=ORIENTED_EDGE('',*,*,#19322,.T.) ;
#27726=ORIENTED_EDGE('',*,*,#19328,.F.) ;
#27727=ORIENTED_EDGE('',*,*,#19331,.T.) ;
#27728=ORIENTED_EDGE('',*,*,#19332,.T.) ;
#27729=ORIENTED_EDGE('',*,*,#19318,.T.) ;
#27730=ORIENTED_EDGE('',*,*,#19330,.F.) ;
#27731=ORIENTED_EDGE('',*,*,#19333,.T.) ;
#27732=ORIENTED_EDGE('',*,*,#19334,.T.) ;
#27733=ORIENTED_EDGE('',*,*,#19319,.T.) ;
#27734=ORIENTED_EDGE('',*,*,#19332,.F.) ;
#27735=ORIENTED_EDGE('',*,*,#19334,.F.) ;
#27736=ORIENTED_EDGE('',*,*,#19335,.T.) ;
#27737=ORIENTED_EDGE('',*,*,#19336,.F.) ;
#27738=ORIENTED_EDGE('',*,*,#19337,.T.) ;
#27739=ORIENTED_EDGE('',*,*,#19333,.F.) ;
#27740=ORIENTED_EDGE('',*,*,#19331,.F.) ;
#27741=ORIENTED_EDGE('',*,*,#19338,.F.) ;
#27742=ORIENTED_EDGE('',*,*,#19339,.F.) ;
#27743=ORIENTED_EDGE('',*,*,#19335,.F.) ;
#27744=ORIENTED_EDGE('',*,*,#19329,.F.) ;
#27745=ORIENTED_EDGE('',*,*,#19340,.T.) ;
#27746=ORIENTED_EDGE('',*,*,#19341,.F.) ;
#27747=ORIENTED_EDGE('',*,*,#19338,.T.) ;
#27748=ORIENTED_EDGE('',*,*,#19342,.T.) ;
#27749=ORIENTED_EDGE('',*,*,#19341,.T.) ;
#27750=ORIENTED_EDGE('',*,*,#19343,.T.) ;
#27751=ORIENTED_EDGE('',*,*,#19342,.F.) ;
#27752=ORIENTED_EDGE('',*,*,#19344,.T.) ;
#27753=ORIENTED_EDGE('',*,*,#19345,.T.) ;
#27754=ORIENTED_EDGE('',*,*,#19339,.T.) ;
#27755=ORIENTED_EDGE('',*,*,#19345,.F.) ;
#27756=ORIENTED_EDGE('',*,*,#19346,.T.) ;
#27757=ORIENTED_EDGE('',*,*,#19336,.T.) ;
#27758=ORIENTED_EDGE('',*,*,#19344,.F.) ;
#27759=ORIENTED_EDGE('',*,*,#19347,.F.) ;
#27760=ORIENTED_EDGE('',*,*,#19348,.F.) ;
#27761=ORIENTED_EDGE('',*,*,#19349,.F.) ;
#27762=ORIENTED_EDGE('',*,*,#19350,.F.) ;
#27763=ORIENTED_EDGE('',*,*,#19351,.F.) ;
#27764=ORIENTED_EDGE('',*,*,#19343,.F.) ;
#27765=ORIENTED_EDGE('',*,*,#19352,.T.) ;
#27766=ORIENTED_EDGE('',*,*,#19353,.F.) ;
#27767=ORIENTED_EDGE('',*,*,#19347,.T.) ;
#27768=ORIENTED_EDGE('',*,*,#19354,.T.) ;
#27769=ORIENTED_EDGE('',*,*,#19355,.T.) ;
#27770=ORIENTED_EDGE('',*,*,#19326,.T.) ;
#27771=ORIENTED_EDGE('',*,*,#19354,.F.) ;
#27772=ORIENTED_EDGE('',*,*,#19356,.T.) ;
#27773=ORIENTED_EDGE('',*,*,#19357,.T.) ;
#27774=ORIENTED_EDGE('',*,*,#19358,.T.) ;
#27775=ORIENTED_EDGE('',*,*,#19357,.F.) ;
#27776=ORIENTED_EDGE('',*,*,#19359,.T.) ;
#27777=ORIENTED_EDGE('',*,*,#19360,.T.) ;
#27778=ORIENTED_EDGE('',*,*,#19314,.F.) ;
#27779=ORIENTED_EDGE('',*,*,#19361,.F.) ;
#27780=ORIENTED_EDGE('',*,*,#19356,.F.) ;
#27781=ORIENTED_EDGE('',*,*,#19325,.F.) ;
#27782=ORIENTED_EDGE('',*,*,#19310,.F.) ;
#27783=ORIENTED_EDGE('',*,*,#19355,.F.) ;
#27784=ORIENTED_EDGE('',*,*,#19362,.T.) ;
#27785=ORIENTED_EDGE('',*,*,#19363,.F.) ;
#27786=ORIENTED_EDGE('',*,*,#19364,.T.) ;
#27787=ORIENTED_EDGE('',*,*,#19365,.F.) ;
#27788=ORIENTED_EDGE('',*,*,#19366,.T.) ;
#27789=ORIENTED_EDGE('',*,*,#19367,.T.) ;
#27790=ORIENTED_EDGE('',*,*,#19368,.T.) ;
#27791=ORIENTED_EDGE('',*,*,#19369,.T.) ;
#27792=ORIENTED_EDGE('',*,*,#19370,.T.) ;
#27793=ORIENTED_EDGE('',*,*,#19371,.T.) ;
#27794=ORIENTED_EDGE('',*,*,#19372,.T.) ;
#27795=ORIENTED_EDGE('',*,*,#19137,.T.) ;
#27796=ORIENTED_EDGE('',*,*,#19373,.T.) ;
#27797=ORIENTED_EDGE('',*,*,#19367,.F.) ;
#27798=ORIENTED_EDGE('',*,*,#19374,.T.) ;
#27799=ORIENTED_EDGE('',*,*,#19375,.T.) ;
#27800=ORIENTED_EDGE('',*,*,#19365,.T.) ;
#27801=ORIENTED_EDGE('',*,*,#19376,.F.) ;
#27802=ORIENTED_EDGE('',*,*,#19090,.F.) ;
#27803=ORIENTED_EDGE('',*,*,#19377,.T.) ;
#27804=ORIENTED_EDGE('',*,*,#19378,.T.) ;
#27805=ORIENTED_EDGE('',*,*,#19379,.T.) ;
#27806=ORIENTED_EDGE('',*,*,#19380,.T.) ;
#27807=ORIENTED_EDGE('',*,*,#19138,.T.) ;
#27808=ORIENTED_EDGE('',*,*,#19375,.F.) ;
#27809=ORIENTED_EDGE('',*,*,#19381,.T.) ;
#27810=ORIENTED_EDGE('',*,*,#19376,.T.) ;
#27811=ORIENTED_EDGE('',*,*,#19372,.F.) ;
#27812=ORIENTED_EDGE('',*,*,#19371,.F.) ;
#27813=ORIENTED_EDGE('',*,*,#19370,.F.) ;
#27814=ORIENTED_EDGE('',*,*,#19369,.F.) ;
#27815=ORIENTED_EDGE('',*,*,#19368,.F.) ;
#27816=ORIENTED_EDGE('',*,*,#19373,.F.) ;
#27817=ORIENTED_EDGE('',*,*,#19136,.F.) ;
#27818=ORIENTED_EDGE('',*,*,#19135,.F.) ;
#27819=ORIENTED_EDGE('',*,*,#19132,.F.) ;
#27820=ORIENTED_EDGE('',*,*,#19129,.F.) ;
#27821=ORIENTED_EDGE('',*,*,#19126,.F.) ;
#27822=ORIENTED_EDGE('',*,*,#19123,.F.) ;
#27823=ORIENTED_EDGE('',*,*,#19120,.F.) ;
#27824=ORIENTED_EDGE('',*,*,#19117,.F.) ;
#27825=ORIENTED_EDGE('',*,*,#19382,.F.) ;
#27826=ORIENTED_EDGE('',*,*,#19140,.T.) ;
#27827=ORIENTED_EDGE('',*,*,#19113,.T.) ;
#27828=ORIENTED_EDGE('',*,*,#19109,.T.) ;
#27829=ORIENTED_EDGE('',*,*,#19106,.T.) ;
#27830=ORIENTED_EDGE('',*,*,#19103,.T.) ;
#27831=ORIENTED_EDGE('',*,*,#19100,.T.) ;
#27832=ORIENTED_EDGE('',*,*,#19097,.T.) ;
#27833=ORIENTED_EDGE('',*,*,#19094,.T.) ;
#27834=ORIENTED_EDGE('',*,*,#19091,.T.) ;
#27835=ORIENTED_EDGE('',*,*,#19176,.F.) ;
#27836=ORIENTED_EDGE('',*,*,#19366,.F.) ;
#27837=ORIENTED_EDGE('',*,*,#19381,.F.) ;
#27838=ORIENTED_EDGE('',*,*,#19374,.F.) ;
#27839=ORIENTED_EDGE('',*,*,#19383,.T.) ;
#27840=ORIENTED_EDGE('',*,*,#19384,.T.) ;
#27841=ORIENTED_EDGE('',*,*,#19385,.T.) ;
#27842=ORIENTED_EDGE('',*,*,#19386,.T.) ;
#27843=ORIENTED_EDGE('',*,*,#19387,.T.) ;
#27844=ORIENTED_EDGE('',*,*,#19388,.T.) ;
#27845=ORIENTED_EDGE('',*,*,#19389,.T.) ;
#27846=ORIENTED_EDGE('',*,*,#19390,.T.) ;
#27847=ORIENTED_EDGE('',*,*,#19391,.T.) ;
#27848=ORIENTED_EDGE('',*,*,#19392,.T.) ;
#27849=ORIENTED_EDGE('',*,*,#19393,.T.) ;
#27850=ORIENTED_EDGE('',*,*,#19383,.F.) ;
#27851=ORIENTED_EDGE('',*,*,#19394,.T.) ;
#27852=ORIENTED_EDGE('',*,*,#19392,.F.) ;
#27853=ORIENTED_EDGE('',*,*,#19395,.T.) ;
#27854=ORIENTED_EDGE('',*,*,#19396,.T.) ;
#27855=ORIENTED_EDGE('',*,*,#19397,.T.) ;
#27856=ORIENTED_EDGE('',*,*,#19396,.F.) ;
#27857=ORIENTED_EDGE('',*,*,#19398,.T.) ;
#27858=ORIENTED_EDGE('',*,*,#19399,.T.) ;
#27859=ORIENTED_EDGE('',*,*,#19395,.F.) ;
#27860=ORIENTED_EDGE('',*,*,#19400,.F.) ;
#27861=ORIENTED_EDGE('',*,*,#19401,.F.) ;
#27862=ORIENTED_EDGE('',*,*,#19402,.F.) ;
#27863=ORIENTED_EDGE('',*,*,#19394,.F.) ;
#27864=ORIENTED_EDGE('',*,*,#19391,.F.) ;
#27865=ORIENTED_EDGE('',*,*,#19390,.F.) ;
#27866=ORIENTED_EDGE('',*,*,#19389,.F.) ;
#27867=ORIENTED_EDGE('',*,*,#19388,.F.) ;
#27868=ORIENTED_EDGE('',*,*,#19403,.T.) ;
#27869=ORIENTED_EDGE('',*,*,#19404,.T.) ;
#27870=ORIENTED_EDGE('',*,*,#19400,.T.) ;
#27871=ORIENTED_EDGE('',*,*,#19384,.F.) ;
#27872=ORIENTED_EDGE('',*,*,#19405,.T.) ;
#27873=ORIENTED_EDGE('',*,*,#19406,.F.) ;
#27874=ORIENTED_EDGE('',*,*,#19407,.F.) ;
#27875=ORIENTED_EDGE('',*,*,#19408,.T.) ;
#27876=ORIENTED_EDGE('',*,*,#19387,.F.) ;
#27877=ORIENTED_EDGE('',*,*,#19386,.F.) ;
#27878=ORIENTED_EDGE('',*,*,#19385,.F.) ;
#27879=ORIENTED_EDGE('',*,*,#19409,.T.) ;
#27880=ORIENTED_EDGE('',*,*,#19410,.T.) ;
#27881=ORIENTED_EDGE('',*,*,#19411,.T.) ;
#27882=ORIENTED_EDGE('',*,*,#19412,.T.) ;
#27883=ORIENTED_EDGE('',*,*,#19413,.T.) ;
#27884=ORIENTED_EDGE('',*,*,#19409,.F.) ;
#27885=ORIENTED_EDGE('',*,*,#19414,.T.) ;
#27886=ORIENTED_EDGE('',*,*,#19412,.F.) ;
#27887=ORIENTED_EDGE('',*,*,#19415,.T.) ;
#27888=ORIENTED_EDGE('',*,*,#19416,.T.) ;
#27889=ORIENTED_EDGE('',*,*,#19417,.T.) ;
#27890=ORIENTED_EDGE('',*,*,#19418,.T.) ;
#27891=ORIENTED_EDGE('',*,*,#19419,.T.) ;
#27892=ORIENTED_EDGE('',*,*,#19407,.T.) ;
#27893=ORIENTED_EDGE('',*,*,#19406,.T.) ;
#27894=ORIENTED_EDGE('',*,*,#19416,.F.) ;
#27895=ORIENTED_EDGE('',*,*,#19418,.F.) ;
#27896=ORIENTED_EDGE('',*,*,#19415,.F.) ;
#27897=ORIENTED_EDGE('',*,*,#19420,.T.) ;
#27898=ORIENTED_EDGE('',*,*,#19421,.T.) ;
#27899=ORIENTED_EDGE('',*,*,#19422,.T.) ;
#27900=ORIENTED_EDGE('',*,*,#19419,.F.) ;
#27901=ORIENTED_EDGE('',*,*,#19414,.F.) ;
#27902=ORIENTED_EDGE('',*,*,#19423,.F.) ;
#27903=ORIENTED_EDGE('',*,*,#19424,.F.) ;
#27904=ORIENTED_EDGE('',*,*,#19420,.F.) ;
#27905=ORIENTED_EDGE('',*,*,#19411,.F.) ;
#27906=ORIENTED_EDGE('',*,*,#19425,.T.) ;
#27907=ORIENTED_EDGE('',*,*,#19426,.F.) ;
#27908=ORIENTED_EDGE('',*,*,#19423,.T.) ;
#27909=ORIENTED_EDGE('',*,*,#19403,.F.) ;
#27910=ORIENTED_EDGE('',*,*,#19408,.F.) ;
#27911=ORIENTED_EDGE('',*,*,#19422,.F.) ;
#27912=ORIENTED_EDGE('',*,*,#19427,.F.) ;
#27913=ORIENTED_EDGE('',*,*,#19428,.F.) ;
#27914=ORIENTED_EDGE('',*,*,#19177,.F.) ;
#27915=ORIENTED_EDGE('',*,*,#19429,.F.) ;
#27916=ORIENTED_EDGE('',*,*,#19430,.F.) ;
#27917=ORIENTED_EDGE('',*,*,#19431,.T.) ;
#27918=ORIENTED_EDGE('',*,*,#19432,.T.) ;
#27919=ORIENTED_EDGE('',*,*,#19363,.T.) ;
#27920=ORIENTED_EDGE('',*,*,#19433,.T.) ;
#27921=ORIENTED_EDGE('',*,*,#19434,.T.) ;
#27922=ORIENTED_EDGE('',*,*,#19431,.F.) ;
#27923=ORIENTED_EDGE('',*,*,#19435,.T.) ;
#27924=ORIENTED_EDGE('',*,*,#19436,.T.) ;
#27925=ORIENTED_EDGE('',*,*,#19437,.T.) ;
#27926=ORIENTED_EDGE('',*,*,#19438,.T.) ;
#27927=ORIENTED_EDGE('',*,*,#19439,.T.) ;
#27928=ORIENTED_EDGE('',*,*,#19440,.T.) ;
#27929=ORIENTED_EDGE('',*,*,#19202,.T.) ;
#27930=ORIENTED_EDGE('',*,*,#19438,.F.) ;
#27931=ORIENTED_EDGE('',*,*,#19441,.T.) ;
#27932=ORIENTED_EDGE('',*,*,#19440,.F.) ;
#27933=ORIENTED_EDGE('',*,*,#19442,.T.) ;
#27934=ORIENTED_EDGE('',*,*,#19443,.T.) ;
#27935=ORIENTED_EDGE('',*,*,#19436,.F.) ;
#27936=ORIENTED_EDGE('',*,*,#19444,.T.) ;
#27937=ORIENTED_EDGE('',*,*,#19433,.F.) ;
#27938=ORIENTED_EDGE('',*,*,#19432,.F.) ;
#27939=ORIENTED_EDGE('',*,*,#19445,.T.) ;
#27940=ORIENTED_EDGE('',*,*,#19446,.F.) ;
#27941=ORIENTED_EDGE('',*,*,#19447,.T.) ;
#27942=ORIENTED_EDGE('',*,*,#19448,.F.) ;
#27943=ORIENTED_EDGE('',*,*,#19449,.F.) ;
#27944=ORIENTED_EDGE('',*,*,#19445,.F.) ;
#27945=ORIENTED_EDGE('',*,*,#19434,.F.) ;
#27946=ORIENTED_EDGE('',*,*,#19439,.F.) ;
#27947=ORIENTED_EDGE('',*,*,#19201,.T.) ;
#27948=ORIENTED_EDGE('',*,*,#19190,.F.) ;
#27949=ORIENTED_EDGE('',*,*,#19195,.F.) ;
#27950=ORIENTED_EDGE('',*,*,#19197,.F.) ;
#27951=ORIENTED_EDGE('',*,*,#19428,.T.) ;
#27952=ORIENTED_EDGE('',*,*,#19450,.F.) ;
#27953=ORIENTED_EDGE('',*,*,#19451,.F.) ;
#27954=ORIENTED_EDGE('',*,*,#19421,.F.) ;
#27955=ORIENTED_EDGE('',*,*,#19444,.F.) ;
#27956=ORIENTED_EDGE('',*,*,#19427,.T.) ;
#27957=ORIENTED_EDGE('',*,*,#19451,.T.) ;
#27958=ORIENTED_EDGE('',*,*,#19448,.T.) ;
#27959=ORIENTED_EDGE('',*,*,#19452,.T.) ;
#27960=ORIENTED_EDGE('',*,*,#19449,.T.) ;
#27961=ORIENTED_EDGE('',*,*,#19450,.T.) ;
#27962=ORIENTED_EDGE('',*,*,#19424,.T.) ;
#27963=ORIENTED_EDGE('',*,*,#19452,.F.) ;
#27964=ORIENTED_EDGE('',*,*,#19426,.T.) ;
#27965=ORIENTED_EDGE('',*,*,#19446,.T.) ;
#27966=ORIENTED_EDGE('',*,*,#19453,.T.) ;
#27967=ORIENTED_EDGE('',*,*,#19301,.T.) ;
#27968=ORIENTED_EDGE('',*,*,#19454,.T.) ;
#27969=ORIENTED_EDGE('',*,*,#19455,.T.) ;
#27970=ORIENTED_EDGE('',*,*,#19456,.T.) ;
#27971=ORIENTED_EDGE('',*,*,#19302,.T.) ;
#27972=ORIENTED_EDGE('',*,*,#19453,.F.) ;
#27973=ORIENTED_EDGE('',*,*,#19457,.T.) ;
#27974=ORIENTED_EDGE('',*,*,#19456,.F.) ;
#27975=ORIENTED_EDGE('',*,*,#19458,.T.) ;
#27976=ORIENTED_EDGE('',*,*,#19459,.T.) ;
#27977=ORIENTED_EDGE('',*,*,#19460,.T.) ;
#27978=ORIENTED_EDGE('',*,*,#19300,.T.) ;
#27979=ORIENTED_EDGE('',*,*,#19461,.T.) ;
#27980=ORIENTED_EDGE('',*,*,#19462,.T.) ;
#27981=ORIENTED_EDGE('',*,*,#19461,.F.) ;
#27982=ORIENTED_EDGE('',*,*,#19305,.T.) ;
#27983=ORIENTED_EDGE('',*,*,#19463,.T.) ;
#27984=ORIENTED_EDGE('',*,*,#19460,.F.) ;
#27985=ORIENTED_EDGE('',*,*,#19464,.T.) ;
#27986=ORIENTED_EDGE('',*,*,#19454,.F.) ;
#27987=ORIENTED_EDGE('',*,*,#19298,.F.) ;
#27988=ORIENTED_EDGE('',*,*,#19303,.T.) ;
#27989=ORIENTED_EDGE('',*,*,#19459,.F.) ;
#27990=ORIENTED_EDGE('',*,*,#19465,.T.) ;
#27991=ORIENTED_EDGE('',*,*,#19458,.F.) ;
#27992=ORIENTED_EDGE('',*,*,#19466,.T.) ;
#27993=ORIENTED_EDGE('',*,*,#19467,.F.) ;
#27994=ORIENTED_EDGE('',*,*,#19468,.T.) ;
#27995=ORIENTED_EDGE('',*,*,#19153,.F.) ;
#27996=ORIENTED_EDGE('',*,*,#19469,.F.) ;
#27997=ORIENTED_EDGE('',*,*,#19470,.F.) ;
#27998=ORIENTED_EDGE('',*,*,#19466,.F.) ;
#27999=ORIENTED_EDGE('',*,*,#19457,.F.) ;
#28000=ORIENTED_EDGE('',*,*,#19471,.F.) ;
#28001=ORIENTED_EDGE('',*,*,#19155,.F.) ;
#28002=ORIENTED_EDGE('',*,*,#19158,.F.) ;
#28003=ORIENTED_EDGE('',*,*,#19161,.F.) ;
#28004=ORIENTED_EDGE('',*,*,#19429,.T.) ;
#28005=ORIENTED_EDGE('',*,*,#19160,.F.) ;
#28006=ORIENTED_EDGE('',*,*,#19159,.F.) ;
#28007=ORIENTED_EDGE('',*,*,#19156,.F.) ;
#28008=ORIENTED_EDGE('',*,*,#19471,.T.) ;
#28009=ORIENTED_EDGE('',*,*,#19455,.F.) ;
#28010=ORIENTED_EDGE('',*,*,#19462,.F.) ;
#28011=ORIENTED_EDGE('',*,*,#19472,.F.) ;
#28012=ORIENTED_EDGE('',*,*,#19473,.F.) ;
#28013=ORIENTED_EDGE('',*,*,#19474,.F.) ;
#28014=ORIENTED_EDGE('',*,*,#19475,.F.) ;
#28015=ORIENTED_EDGE('',*,*,#19404,.F.) ;
#28016=ORIENTED_EDGE('',*,*,#19476,.F.) ;
#28017=ORIENTED_EDGE('',*,*,#19464,.F.) ;
#28018=ORIENTED_EDGE('',*,*,#19474,.T.) ;
#28019=ORIENTED_EDGE('',*,*,#19476,.T.) ;
#28020=ORIENTED_EDGE('',*,*,#19430,.T.) ;
#28021=ORIENTED_EDGE('',*,*,#19477,.T.) ;
#28022=ORIENTED_EDGE('',*,*,#19401,.T.) ;
#28023=ORIENTED_EDGE('',*,*,#19475,.T.) ;
#28024=ORIENTED_EDGE('',*,*,#19473,.T.) ;
#28025=ORIENTED_EDGE('',*,*,#19477,.F.) ;
#28026=ORIENTED_EDGE('',*,*,#19478,.T.) ;
#28027=ORIENTED_EDGE('',*,*,#19479,.T.) ;
#28028=ORIENTED_EDGE('',*,*,#19398,.F.) ;
#28029=ORIENTED_EDGE('',*,*,#19402,.T.) ;
#28030=ORIENTED_EDGE('',*,*,#19479,.F.) ;
#28031=ORIENTED_EDGE('',*,*,#19480,.T.) ;
#28032=ORIENTED_EDGE('',*,*,#19463,.F.) ;
#28033=ORIENTED_EDGE('',*,*,#19481,.T.) ;
#28034=ORIENTED_EDGE('',*,*,#19478,.F.) ;
#28035=ORIENTED_EDGE('',*,*,#19472,.T.) ;
#28036=ORIENTED_EDGE('',*,*,#19185,.F.) ;
#28037=ORIENTED_EDGE('',*,*,#19172,.T.) ;
#28038=ORIENTED_EDGE('',*,*,#19180,.T.) ;
#28039=ORIENTED_EDGE('',*,*,#19233,.F.) ;
#28040=ORIENTED_EDGE('',*,*,#19168,.T.) ;
#28041=ORIENTED_EDGE('',*,*,#19228,.T.) ;
#28042=ORIENTED_EDGE('',*,*,#19482,.T.) ;
#28043=ORIENTED_EDGE('',*,*,#19222,.F.) ;
#28044=ORIENTED_EDGE('',*,*,#19221,.F.) ;
#28045=ORIENTED_EDGE('',*,*,#19218,.F.) ;
#28046=ORIENTED_EDGE('',*,*,#19483,.T.) ;
#28047=ORIENTED_EDGE('',*,*,#19484,.F.) ;
#28048=ORIENTED_EDGE('',*,*,#19485,.T.) ;
#28049=ORIENTED_EDGE('',*,*,#19486,.T.) ;
#28050=ORIENTED_EDGE('',*,*,#19487,.T.) ;
#28051=ORIENTED_EDGE('',*,*,#19488,.T.) ;
#28052=ORIENTED_EDGE('',*,*,#19489,.T.) ;
#28053=ORIENTED_EDGE('',*,*,#19490,.T.) ;
#28054=ORIENTED_EDGE('',*,*,#19491,.T.) ;
#28055=ORIENTED_EDGE('',*,*,#19492,.T.) ;
#28056=ORIENTED_EDGE('',*,*,#19493,.T.) ;
#28057=ORIENTED_EDGE('',*,*,#19494,.T.) ;
#28058=ORIENTED_EDGE('',*,*,#19495,.T.) ;
#28059=ORIENTED_EDGE('',*,*,#19485,.F.) ;
#28060=ORIENTED_EDGE('',*,*,#19496,.T.) ;
#28061=ORIENTED_EDGE('',*,*,#19494,.F.) ;
#28062=ORIENTED_EDGE('',*,*,#19497,.T.) ;
#28063=ORIENTED_EDGE('',*,*,#19498,.T.) ;
#28064=ORIENTED_EDGE('',*,*,#19499,.T.) ;
#28065=ORIENTED_EDGE('',*,*,#19498,.F.) ;
#28066=ORIENTED_EDGE('',*,*,#19500,.T.) ;
#28067=ORIENTED_EDGE('',*,*,#19501,.T.) ;
#28068=ORIENTED_EDGE('',*,*,#19497,.F.) ;
#28069=ORIENTED_EDGE('',*,*,#19502,.F.) ;
#28070=ORIENTED_EDGE('',*,*,#19503,.F.) ;
#28071=ORIENTED_EDGE('',*,*,#19504,.F.) ;
#28072=ORIENTED_EDGE('',*,*,#19496,.F.) ;
#28073=ORIENTED_EDGE('',*,*,#19493,.F.) ;
#28074=ORIENTED_EDGE('',*,*,#19492,.F.) ;
#28075=ORIENTED_EDGE('',*,*,#19491,.F.) ;
#28076=ORIENTED_EDGE('',*,*,#19490,.F.) ;
#28077=ORIENTED_EDGE('',*,*,#19505,.T.) ;
#28078=ORIENTED_EDGE('',*,*,#19506,.T.) ;
#28079=ORIENTED_EDGE('',*,*,#19502,.T.) ;
#28080=ORIENTED_EDGE('',*,*,#19486,.F.) ;
#28081=ORIENTED_EDGE('',*,*,#19507,.T.) ;
#28082=ORIENTED_EDGE('',*,*,#19508,.F.) ;
#28083=ORIENTED_EDGE('',*,*,#19509,.F.) ;
#28084=ORIENTED_EDGE('',*,*,#19510,.T.) ;
#28085=ORIENTED_EDGE('',*,*,#19489,.F.) ;
#28086=ORIENTED_EDGE('',*,*,#19488,.F.) ;
#28087=ORIENTED_EDGE('',*,*,#19487,.F.) ;
#28088=ORIENTED_EDGE('',*,*,#19511,.T.) ;
#28089=ORIENTED_EDGE('',*,*,#19512,.T.) ;
#28090=ORIENTED_EDGE('',*,*,#19513,.T.) ;
#28091=ORIENTED_EDGE('',*,*,#19514,.T.) ;
#28092=ORIENTED_EDGE('',*,*,#19515,.T.) ;
#28093=ORIENTED_EDGE('',*,*,#19511,.F.) ;
#28094=ORIENTED_EDGE('',*,*,#19516,.T.) ;
#28095=ORIENTED_EDGE('',*,*,#19514,.F.) ;
#28096=ORIENTED_EDGE('',*,*,#19517,.T.) ;
#28097=ORIENTED_EDGE('',*,*,#19518,.T.) ;
#28098=ORIENTED_EDGE('',*,*,#19519,.T.) ;
#28099=ORIENTED_EDGE('',*,*,#19520,.T.) ;
#28100=ORIENTED_EDGE('',*,*,#19521,.T.) ;
#28101=ORIENTED_EDGE('',*,*,#19509,.T.) ;
#28102=ORIENTED_EDGE('',*,*,#19508,.T.) ;
#28103=ORIENTED_EDGE('',*,*,#19518,.F.) ;
#28104=ORIENTED_EDGE('',*,*,#19520,.F.) ;
#28105=ORIENTED_EDGE('',*,*,#19517,.F.) ;
#28106=ORIENTED_EDGE('',*,*,#19522,.T.) ;
#28107=ORIENTED_EDGE('',*,*,#19523,.T.) ;
#28108=ORIENTED_EDGE('',*,*,#19524,.T.) ;
#28109=ORIENTED_EDGE('',*,*,#19521,.F.) ;
#28110=ORIENTED_EDGE('',*,*,#19516,.F.) ;
#28111=ORIENTED_EDGE('',*,*,#19525,.F.) ;
#28112=ORIENTED_EDGE('',*,*,#19526,.F.) ;
#28113=ORIENTED_EDGE('',*,*,#19522,.F.) ;
#28114=ORIENTED_EDGE('',*,*,#19513,.F.) ;
#28115=ORIENTED_EDGE('',*,*,#19527,.T.) ;
#28116=ORIENTED_EDGE('',*,*,#19528,.F.) ;
#28117=ORIENTED_EDGE('',*,*,#19525,.T.) ;
#28118=ORIENTED_EDGE('',*,*,#19225,.F.) ;
#28119=ORIENTED_EDGE('',*,*,#19482,.F.) ;
#28120=ORIENTED_EDGE('',*,*,#19529,.F.) ;
#28121=ORIENTED_EDGE('',*,*,#19505,.F.) ;
#28122=ORIENTED_EDGE('',*,*,#19510,.F.) ;
#28123=ORIENTED_EDGE('',*,*,#19524,.F.) ;
#28124=ORIENTED_EDGE('',*,*,#19530,.F.) ;
#28125=ORIENTED_EDGE('',*,*,#19531,.F.) ;
#28126=ORIENTED_EDGE('',*,*,#19532,.T.) ;
#28127=ORIENTED_EDGE('',*,*,#19533,.T.) ;
#28128=ORIENTED_EDGE('',*,*,#19534,.T.) ;
#28129=ORIENTED_EDGE('',*,*,#19535,.T.) ;
#28130=ORIENTED_EDGE('',*,*,#19534,.F.) ;
#28131=ORIENTED_EDGE('',*,*,#19536,.T.) ;
#28132=ORIENTED_EDGE('',*,*,#19537,.T.) ;
#28133=ORIENTED_EDGE('',*,*,#19538,.T.) ;
#28134=ORIENTED_EDGE('',*,*,#19539,.T.) ;
#28135=ORIENTED_EDGE('',*,*,#19540,.T.) ;
#28136=ORIENTED_EDGE('',*,*,#19541,.T.) ;
#28137=ORIENTED_EDGE('',*,*,#19542,.T.) ;
#28138=ORIENTED_EDGE('',*,*,#19250,.T.) ;
#28139=ORIENTED_EDGE('',*,*,#19540,.F.) ;
#28140=ORIENTED_EDGE('',*,*,#19543,.T.) ;
#28141=ORIENTED_EDGE('',*,*,#19542,.F.) ;
#28142=ORIENTED_EDGE('',*,*,#19544,.T.) ;
#28143=ORIENTED_EDGE('',*,*,#19545,.T.) ;
#28144=ORIENTED_EDGE('',*,*,#19538,.F.) ;
#28145=ORIENTED_EDGE('',*,*,#19546,.T.) ;
#28146=ORIENTED_EDGE('',*,*,#19532,.F.) ;
#28147=ORIENTED_EDGE('',*,*,#19254,.F.) ;
#28148=ORIENTED_EDGE('',*,*,#19547,.T.) ;
#28149=ORIENTED_EDGE('',*,*,#19537,.F.) ;
#28150=ORIENTED_EDGE('',*,*,#19548,.T.) ;
#28151=ORIENTED_EDGE('',*,*,#19536,.F.) ;
#28152=ORIENTED_EDGE('',*,*,#19549,.T.) ;
#28153=ORIENTED_EDGE('',*,*,#19550,.F.) ;
#28154=ORIENTED_EDGE('',*,*,#19551,.T.) ;
#28155=ORIENTED_EDGE('',*,*,#19552,.F.) ;
#28156=ORIENTED_EDGE('',*,*,#19553,.F.) ;
#28157=ORIENTED_EDGE('',*,*,#19549,.F.) ;
#28158=ORIENTED_EDGE('',*,*,#19533,.F.) ;
#28159=ORIENTED_EDGE('',*,*,#19541,.F.) ;
#28160=ORIENTED_EDGE('',*,*,#19249,.T.) ;
#28161=ORIENTED_EDGE('',*,*,#19238,.F.) ;
#28162=ORIENTED_EDGE('',*,*,#19243,.F.) ;
#28163=ORIENTED_EDGE('',*,*,#19245,.F.) ;
#28164=ORIENTED_EDGE('',*,*,#19531,.T.) ;
#28165=ORIENTED_EDGE('',*,*,#19554,.F.) ;
#28166=ORIENTED_EDGE('',*,*,#19555,.F.) ;
#28167=ORIENTED_EDGE('',*,*,#19523,.F.) ;
#28168=ORIENTED_EDGE('',*,*,#19546,.F.) ;
#28169=ORIENTED_EDGE('',*,*,#19530,.T.) ;
#28170=ORIENTED_EDGE('',*,*,#19555,.T.) ;
#28171=ORIENTED_EDGE('',*,*,#19552,.T.) ;
#28172=ORIENTED_EDGE('',*,*,#19556,.T.) ;
#28173=ORIENTED_EDGE('',*,*,#19528,.T.) ;
#28174=ORIENTED_EDGE('',*,*,#19550,.T.) ;
#28175=ORIENTED_EDGE('',*,*,#19556,.F.) ;
#28176=ORIENTED_EDGE('',*,*,#19553,.T.) ;
#28177=ORIENTED_EDGE('',*,*,#19554,.T.) ;
#28178=ORIENTED_EDGE('',*,*,#19526,.T.) ;
#28179=ORIENTED_EDGE('',*,*,#19258,.F.) ;
#28180=ORIENTED_EDGE('',*,*,#19557,.F.) ;
#28181=ORIENTED_EDGE('',*,*,#19543,.F.) ;
#28182=ORIENTED_EDGE('',*,*,#19539,.F.) ;
#28183=ORIENTED_EDGE('',*,*,#19535,.F.) ;
#28184=ORIENTED_EDGE('',*,*,#19547,.F.) ;
#28185=ORIENTED_EDGE('',*,*,#19558,.T.) ;
#28186=ORIENTED_EDGE('',*,*,#19349,.T.) ;
#28187=ORIENTED_EDGE('',*,*,#19559,.T.) ;
#28188=ORIENTED_EDGE('',*,*,#19484,.T.) ;
#28189=ORIENTED_EDGE('',*,*,#19560,.T.) ;
#28190=ORIENTED_EDGE('',*,*,#19350,.T.) ;
#28191=ORIENTED_EDGE('',*,*,#19558,.F.) ;
#28192=ORIENTED_EDGE('',*,*,#19561,.T.) ;
#28193=ORIENTED_EDGE('',*,*,#19560,.F.) ;
#28194=ORIENTED_EDGE('',*,*,#19562,.T.) ;
#28195=ORIENTED_EDGE('',*,*,#19563,.T.) ;
#28196=ORIENTED_EDGE('',*,*,#19564,.T.) ;
#28197=ORIENTED_EDGE('',*,*,#19348,.T.) ;
#28198=ORIENTED_EDGE('',*,*,#19565,.T.) ;
#28199=ORIENTED_EDGE('',*,*,#19566,.T.) ;
#28200=ORIENTED_EDGE('',*,*,#19565,.F.) ;
#28201=ORIENTED_EDGE('',*,*,#19353,.T.) ;
#28202=ORIENTED_EDGE('',*,*,#19567,.T.) ;
#28203=ORIENTED_EDGE('',*,*,#19564,.F.) ;
#28204=ORIENTED_EDGE('',*,*,#19568,.T.) ;
#28205=ORIENTED_EDGE('',*,*,#19559,.F.) ;
#28206=ORIENTED_EDGE('',*,*,#19346,.F.) ;
#28207=ORIENTED_EDGE('',*,*,#19351,.T.) ;
#28208=ORIENTED_EDGE('',*,*,#19563,.F.) ;
#28209=ORIENTED_EDGE('',*,*,#19569,.T.) ;
#28210=ORIENTED_EDGE('',*,*,#19562,.F.) ;
#28211=ORIENTED_EDGE('',*,*,#19570,.T.) ;
#28212=ORIENTED_EDGE('',*,*,#19571,.T.) ;
#28213=ORIENTED_EDGE('',*,*,#19572,.T.) ;
#28214=ORIENTED_EDGE('',*,*,#19215,.F.) ;
#28215=ORIENTED_EDGE('',*,*,#19573,.F.) ;
#28216=ORIENTED_EDGE('',*,*,#19574,.F.) ;
#28217=ORIENTED_EDGE('',*,*,#19570,.F.) ;
#28218=ORIENTED_EDGE('',*,*,#19561,.F.) ;
#28219=ORIENTED_EDGE('',*,*,#19483,.F.) ;
#28220=ORIENTED_EDGE('',*,*,#19217,.F.) ;
#28221=ORIENTED_EDGE('',*,*,#19220,.F.) ;
#28222=ORIENTED_EDGE('',*,*,#19223,.F.) ;
#28223=ORIENTED_EDGE('',*,*,#19566,.F.) ;
#28224=ORIENTED_EDGE('',*,*,#19575,.F.) ;
#28225=ORIENTED_EDGE('',*,*,#19576,.F.) ;
#28226=ORIENTED_EDGE('',*,*,#19577,.F.) ;
#28227=ORIENTED_EDGE('',*,*,#19578,.F.) ;
#28228=ORIENTED_EDGE('',*,*,#19506,.F.) ;
#28229=ORIENTED_EDGE('',*,*,#19579,.F.) ;
#28230=ORIENTED_EDGE('',*,*,#19568,.F.) ;
#28231=ORIENTED_EDGE('',*,*,#19577,.T.) ;
#28232=ORIENTED_EDGE('',*,*,#19579,.T.) ;
#28233=ORIENTED_EDGE('',*,*,#19529,.T.) ;
#28234=ORIENTED_EDGE('',*,*,#19580,.T.) ;
#28235=ORIENTED_EDGE('',*,*,#19503,.T.) ;
#28236=ORIENTED_EDGE('',*,*,#19578,.T.) ;
#28237=ORIENTED_EDGE('',*,*,#19576,.T.) ;
#28238=ORIENTED_EDGE('',*,*,#19580,.F.) ;
#28239=ORIENTED_EDGE('',*,*,#19581,.T.) ;
#28240=ORIENTED_EDGE('',*,*,#19582,.T.) ;
#28241=ORIENTED_EDGE('',*,*,#19500,.F.) ;
#28242=ORIENTED_EDGE('',*,*,#19504,.T.) ;
#28243=ORIENTED_EDGE('',*,*,#19582,.F.) ;
#28244=ORIENTED_EDGE('',*,*,#19583,.T.) ;
#28245=ORIENTED_EDGE('',*,*,#19567,.F.) ;
#28246=ORIENTED_EDGE('',*,*,#19584,.T.) ;
#28247=ORIENTED_EDGE('',*,*,#19581,.F.) ;
#28248=ORIENTED_EDGE('',*,*,#19575,.T.) ;
#28249=ORIENTED_EDGE('',*,*,#19399,.F.) ;
#28250=ORIENTED_EDGE('',*,*,#19585,.T.) ;
#28251=ORIENTED_EDGE('',*,*,#19410,.F.) ;
#28252=ORIENTED_EDGE('',*,*,#19586,.T.) ;
#28253=ORIENTED_EDGE('',*,*,#19275,.F.) ;
#28254=ORIENTED_EDGE('',*,*,#19587,.T.) ;
#28255=ORIENTED_EDGE('',*,*,#19277,.F.) ;
#28256=ORIENTED_EDGE('',*,*,#19588,.T.) ;
#28257=ORIENTED_EDGE('',*,*,#19501,.F.) ;
#28258=ORIENTED_EDGE('',*,*,#19589,.T.) ;
#28259=ORIENTED_EDGE('',*,*,#19512,.F.) ;
#28260=ORIENTED_EDGE('',*,*,#19590,.T.) ;
#28261=ORIENTED_EDGE('',*,*,#19358,.F.) ;
#28262=ORIENTED_EDGE('',*,*,#19591,.F.) ;
#28263=ORIENTED_EDGE('',*,*,#19441,.F.) ;
#28264=ORIENTED_EDGE('',*,*,#19437,.F.) ;
#28265=ORIENTED_EDGE('',*,*,#19435,.F.) ;
#28266=ORIENTED_EDGE('',*,*,#19362,.F.) ;
#28267=ORIENTED_EDGE('',*,*,#19499,.F.) ;
#28268=ORIENTED_EDGE('',*,*,#19590,.F.) ;
#28269=ORIENTED_EDGE('',*,*,#19515,.F.) ;
#28270=ORIENTED_EDGE('',*,*,#19519,.F.) ;
#28271=ORIENTED_EDGE('',*,*,#19507,.F.) ;
#28272=ORIENTED_EDGE('',*,*,#19495,.F.) ;
#28273=ORIENTED_EDGE('',*,*,#19589,.F.) ;
#28274=ORIENTED_EDGE('',*,*,#19583,.F.) ;
#28275=ORIENTED_EDGE('',*,*,#19584,.F.) ;
#28276=ORIENTED_EDGE('',*,*,#19352,.F.) ;
#28277=ORIENTED_EDGE('',*,*,#19340,.F.) ;
#28278=ORIENTED_EDGE('',*,*,#19323,.F.) ;
#28279=ORIENTED_EDGE('',*,*,#19327,.F.) ;
#28280=ORIENTED_EDGE('',*,*,#19364,.F.) ;
#28281=ORIENTED_EDGE('',*,*,#19447,.F.) ;
#28282=ORIENTED_EDGE('',*,*,#19425,.F.) ;
#28283=ORIENTED_EDGE('',*,*,#19585,.F.) ;
#28284=ORIENTED_EDGE('',*,*,#19480,.F.) ;
#28285=ORIENTED_EDGE('',*,*,#19481,.F.) ;
#28286=ORIENTED_EDGE('',*,*,#19304,.F.) ;
#28287=ORIENTED_EDGE('',*,*,#19292,.F.) ;
#28288=ORIENTED_EDGE('',*,*,#19587,.F.) ;
#28289=ORIENTED_EDGE('',*,*,#19267,.F.) ;
#28290=ORIENTED_EDGE('',*,*,#19548,.F.) ;
#28291=ORIENTED_EDGE('',*,*,#19551,.F.) ;
#28292=ORIENTED_EDGE('',*,*,#19527,.F.) ;
#28293=ORIENTED_EDGE('',*,*,#19545,.F.) ;
#28294=ORIENTED_EDGE('',*,*,#19592,.T.) ;
#28295=ORIENTED_EDGE('',*,*,#19593,.T.) ;
#28296=ORIENTED_EDGE('',*,*,#19251,.T.) ;
#28297=ORIENTED_EDGE('',*,*,#19247,.T.) ;
#28298=ORIENTED_EDGE('',*,*,#19252,.T.) ;
#28299=ORIENTED_EDGE('',*,*,#19593,.F.) ;
#28300=ORIENTED_EDGE('',*,*,#19594,.T.) ;
#28301=ORIENTED_EDGE('',*,*,#19260,.F.) ;
#28302=ORIENTED_EDGE('',*,*,#19595,.T.) ;
#28303=ORIENTED_EDGE('',*,*,#19544,.F.) ;
#28304=ORIENTED_EDGE('',*,*,#19557,.T.) ;
#28305=ORIENTED_EDGE('',*,*,#19272,.F.) ;
#28306=ORIENTED_EDGE('',*,*,#19596,.T.) ;
#28307=ORIENTED_EDGE('',*,*,#19283,.F.) ;
#28308=ORIENTED_EDGE('',*,*,#19286,.F.) ;
#28309=ORIENTED_EDGE('',*,*,#19597,.T.) ;
#28310=ORIENTED_EDGE('',*,*,#19269,.F.) ;
#28311=ORIENTED_EDGE('',*,*,#19144,.F.) ;
#28312=ORIENTED_EDGE('',*,*,#19598,.T.) ;
#28313=ORIENTED_EDGE('',*,*,#19599,.T.) ;
#28314=ORIENTED_EDGE('',*,*,#19469,.T.) ;
#28315=ORIENTED_EDGE('',*,*,#19150,.F.) ;
#28316=ORIENTED_EDGE('',*,*,#19145,.F.) ;
#28317=ORIENTED_EDGE('',*,*,#19467,.T.) ;
#28318=ORIENTED_EDGE('',*,*,#19470,.T.) ;
#28319=ORIENTED_EDGE('',*,*,#19599,.F.) ;
#28320=ORIENTED_EDGE('',*,*,#19600,.T.) ;
#28321=ORIENTED_EDGE('',*,*,#19592,.F.) ;
#28322=ORIENTED_EDGE('',*,*,#19595,.F.) ;
#28323=ORIENTED_EDGE('',*,*,#19263,.F.) ;
#28324=ORIENTED_EDGE('',*,*,#19597,.F.) ;
#28325=ORIENTED_EDGE('',*,*,#19289,.F.) ;
#28326=ORIENTED_EDGE('',*,*,#19465,.F.) ;
#28327=ORIENTED_EDGE('',*,*,#19468,.F.) ;
#28328=ORIENTED_EDGE('',*,*,#19601,.T.) ;
#28329=ORIENTED_EDGE('',*,*,#19594,.F.) ;
#28330=ORIENTED_EDGE('',*,*,#19601,.F.) ;
#28331=ORIENTED_EDGE('',*,*,#19600,.F.) ;
#28332=ORIENTED_EDGE('',*,*,#19602,.T.) ;
#28333=ORIENTED_EDGE('',*,*,#19248,.F.) ;
#28334=ORIENTED_EDGE('',*,*,#19602,.F.) ;
#28335=ORIENTED_EDGE('',*,*,#19598,.F.) ;
#28336=ORIENTED_EDGE('',*,*,#19170,.T.) ;
#28337=ORIENTED_EDGE('',*,*,#19603,.T.) ;
#28338=ORIENTED_EDGE('',*,*,#19604,.T.) ;
#28339=ORIENTED_EDGE('',*,*,#19199,.F.) ;
#28340=ORIENTED_EDGE('',*,*,#19204,.T.) ;
#28341=ORIENTED_EDGE('',*,*,#19443,.F.) ;
#28342=ORIENTED_EDGE('',*,*,#19605,.T.) ;
#28343=ORIENTED_EDGE('',*,*,#19603,.F.) ;
#28344=ORIENTED_EDGE('',*,*,#19203,.T.) ;
#28345=ORIENTED_EDGE('',*,*,#19360,.F.) ;
#28346=ORIENTED_EDGE('',*,*,#19606,.T.) ;
#28347=ORIENTED_EDGE('',*,*,#19442,.F.) ;
#28348=ORIENTED_EDGE('',*,*,#19591,.T.) ;
#28349=ORIENTED_EDGE('',*,*,#19316,.F.) ;
#28350=ORIENTED_EDGE('',*,*,#19607,.T.) ;
#28351=ORIENTED_EDGE('',*,*,#19359,.F.) ;
#28352=ORIENTED_EDGE('',*,*,#19361,.T.) ;
#28353=ORIENTED_EDGE('',*,*,#19608,.T.) ;
#28354=ORIENTED_EDGE('',*,*,#19609,.T.) ;
#28355=ORIENTED_EDGE('',*,*,#19571,.F.) ;
#28356=ORIENTED_EDGE('',*,*,#19574,.T.) ;
#28357=ORIENTED_EDGE('',*,*,#19206,.F.) ;
#28358=ORIENTED_EDGE('',*,*,#19610,.T.) ;
#28359=ORIENTED_EDGE('',*,*,#19608,.F.) ;
#28360=ORIENTED_EDGE('',*,*,#19573,.T.) ;
#28361=ORIENTED_EDGE('',*,*,#19212,.F.) ;
#28362=ORIENTED_EDGE('',*,*,#19207,.F.) ;
#28363=ORIENTED_EDGE('',*,*,#19605,.F.) ;
#28364=ORIENTED_EDGE('',*,*,#19606,.F.) ;
#28365=ORIENTED_EDGE('',*,*,#19607,.F.) ;
#28366=ORIENTED_EDGE('',*,*,#19320,.F.) ;
#28367=ORIENTED_EDGE('',*,*,#19337,.F.) ;
#28368=ORIENTED_EDGE('',*,*,#19569,.F.) ;
#28369=ORIENTED_EDGE('',*,*,#19572,.F.) ;
#28370=ORIENTED_EDGE('',*,*,#19611,.T.) ;
#28371=ORIENTED_EDGE('',*,*,#19604,.F.) ;
#28372=ORIENTED_EDGE('',*,*,#19611,.F.) ;
#28373=ORIENTED_EDGE('',*,*,#19609,.F.) ;
#28374=ORIENTED_EDGE('',*,*,#19612,.T.) ;
#28375=ORIENTED_EDGE('',*,*,#19200,.F.) ;
#28376=ORIENTED_EDGE('',*,*,#19612,.F.) ;
#28377=ORIENTED_EDGE('',*,*,#19610,.F.) ;
#28378=ORIENTED_EDGE('',*,*,#19164,.T.) ;
#28379=ORIENTED_EDGE('',*,*,#19174,.T.) ;
#28380=ORIENTED_EDGE('',*,*,#19613,.T.) ;
#28381=ORIENTED_EDGE('',*,*,#19614,.T.) ;
#28382=ORIENTED_EDGE('',*,*,#19615,.F.) ;
#28383=ORIENTED_EDGE('',*,*,#19614,.F.) ;
#28384=ORIENTED_EDGE('',*,*,#19616,.T.) ;
#28385=ORIENTED_EDGE('',*,*,#19111,.T.) ;
#28386=ORIENTED_EDGE('',*,*,#19141,.T.) ;
#28387=ORIENTED_EDGE('',*,*,#19382,.T.) ;
#28388=ORIENTED_EDGE('',*,*,#19116,.F.) ;
#28389=ORIENTED_EDGE('',*,*,#19274,.F.) ;
#28390=ORIENTED_EDGE('',*,*,#19588,.F.) ;
#28391=ORIENTED_EDGE('',*,*,#19280,.F.) ;
#28392=ORIENTED_EDGE('',*,*,#19596,.F.) ;
#28393=ORIENTED_EDGE('',*,*,#19397,.F.) ;
#28394=ORIENTED_EDGE('',*,*,#19586,.F.) ;
#28395=ORIENTED_EDGE('',*,*,#19413,.F.) ;
#28396=ORIENTED_EDGE('',*,*,#19417,.F.) ;
#28397=ORIENTED_EDGE('',*,*,#19405,.F.) ;
#28398=ORIENTED_EDGE('',*,*,#19393,.F.) ;
#28399=ORIENTED_EDGE('',*,*,#19615,.T.) ;
#28400=ORIENTED_EDGE('',*,*,#19380,.F.) ;
#28401=ORIENTED_EDGE('',*,*,#19379,.F.) ;
#28402=ORIENTED_EDGE('',*,*,#19378,.F.) ;
#28403=ORIENTED_EDGE('',*,*,#19377,.F.) ;
#28404=ORIENTED_EDGE('',*,*,#19089,.F.) ;
#28405=ORIENTED_EDGE('',*,*,#19093,.F.) ;
#28406=ORIENTED_EDGE('',*,*,#19096,.F.) ;
#28407=ORIENTED_EDGE('',*,*,#19099,.F.) ;
#28408=ORIENTED_EDGE('',*,*,#19102,.F.) ;
#28409=ORIENTED_EDGE('',*,*,#19105,.F.) ;
#28410=ORIENTED_EDGE('',*,*,#19108,.F.) ;
#28411=ORIENTED_EDGE('',*,*,#19112,.F.) ;
#28412=ORIENTED_EDGE('',*,*,#19616,.F.) ;
#28413=ORIENTED_EDGE('',*,*,#19613,.F.) ;
#28414=ORIENTED_EDGE('',*,*,#19115,.T.) ;
#28415=ORIENTED_EDGE('',*,*,#19119,.T.) ;
#28416=ORIENTED_EDGE('',*,*,#19122,.T.) ;
#28417=ORIENTED_EDGE('',*,*,#19125,.T.) ;
#28418=ORIENTED_EDGE('',*,*,#19128,.T.) ;
#28419=ORIENTED_EDGE('',*,*,#19131,.T.) ;
#28420=ORIENTED_EDGE('',*,*,#19134,.T.) ;
#28421=ORIENTED_EDGE('',*,*,#19139,.T.) ;
#30547=CYLINDRICAL_SURFACE('',#35476,1.2370442518096) ;
#30548=CYLINDRICAL_SURFACE('',#35477,1.2370442518096) ;
#30549=CYLINDRICAL_SURFACE('',#35478,1.2370442518096) ;
#30550=CYLINDRICAL_SURFACE('',#35479,1.2370442518096) ;
#30551=CYLINDRICAL_SURFACE('',#35480,1.2370442518096) ;
#30552=CYLINDRICAL_SURFACE('',#35481,1.2370442518096) ;
#30553=CYLINDRICAL_SURFACE('',#35482,1.2370442518096) ;
#30554=CYLINDRICAL_SURFACE('',#35483,1.2370442518096) ;
#30555=CYLINDRICAL_SURFACE('',#35485,1.7526) ;
#30556=CYLINDRICAL_SURFACE('',#35487,1.7526) ;
#30557=CYLINDRICAL_SURFACE('',#35488,1.7526) ;
#30558=CYLINDRICAL_SURFACE('',#35489,1.7526) ;
#30559=CYLINDRICAL_SURFACE('',#35490,1.7526) ;
#30560=CYLINDRICAL_SURFACE('',#35491,1.7526) ;
#30561=CYLINDRICAL_SURFACE('',#35492,1.7526) ;
#30562=CYLINDRICAL_SURFACE('',#35493,1.7526) ;
#30563=CYLINDRICAL_SURFACE('',#35495,1.2370442518096) ;
#30564=CYLINDRICAL_SURFACE('',#35529,0.1) ;
#30565=CYLINDRICAL_SURFACE('',#35553,0.1) ;
#30566=CYLINDRICAL_SURFACE('',#35561,0.1) ;
#30567=CYLINDRICAL_SURFACE('',#35571,0.1) ;
#30568=CYLINDRICAL_SURFACE('',#35592,0.1) ;
#30569=CYLINDRICAL_SURFACE('',#35596,0.1) ;
#30570=CYLINDRICAL_SURFACE('',#35603,0.1) ;
#30571=CYLINDRICAL_SURFACE('',#35622,0.1) ;
#30572=CYLINDRICAL_SURFACE('',#35635,0.1) ;
#30573=CYLINDRICAL_SURFACE('',#35639,0.1) ;
#30574=CYLINDRICAL_SURFACE('',#35646,0.1) ;
#30575=CYLINDRICAL_SURFACE('',#35650,0.1) ;
#30576=CYLINDRICAL_SURFACE('',#35657,0.1) ;
#30577=CYLINDRICAL_SURFACE('',#35681,0.1) ;
#30578=CYLINDRICAL_SURFACE('',#35694,0.1) ;
#30579=CYLINDRICAL_SURFACE('',#35697,0.1) ;
#30580=CYLINDRICAL_SURFACE('',#35702,0.1) ;
#30581=CYLINDRICAL_SURFACE('',#35708,0.1) ;
#30582=CYLINDRICAL_SURFACE('',#35715,0.1) ;
#30583=CYLINDRICAL_SURFACE('',#35718,0.1) ;
#30584=CYLINDRICAL_SURFACE('',#35722,0.1) ;
#30585=CYLINDRICAL_SURFACE('',#35723,0.1) ;
#30586=CYLINDRICAL_SURFACE('',#35728,0.1) ;
#30587=CYLINDRICAL_SURFACE('',#35733,0.1) ;
#30588=CYLINDRICAL_SURFACE('',#35747,0.1) ;
#30589=CYLINDRICAL_SURFACE('',#35752,0.1) ;
#30590=CYLINDRICAL_SURFACE('',#35753,0.1) ;
#30591=CYLINDRICAL_SURFACE('',#35757,0.1) ;
#30592=CYLINDRICAL_SURFACE('',#35758,0.1) ;
#30593=CYLINDRICAL_SURFACE('',#35759,0.1) ;
#30594=CYLINDRICAL_SURFACE('',#35776,0.1) ;
#30595=CYLINDRICAL_SURFACE('',#35789,0.1) ;
#30596=CYLINDRICAL_SURFACE('',#35792,0.1) ;
#30597=CYLINDRICAL_SURFACE('',#35795,0.1) ;
#30598=CYLINDRICAL_SURFACE('',#35804,0.1) ;
#30599=CYLINDRICAL_SURFACE('',#35811,0.1) ;
#30600=CYLINDRICAL_SURFACE('',#35812,0.1) ;
#30601=CYLINDRICAL_SURFACE('',#35815,0.1) ;
#30602=CYLINDRICAL_SURFACE('',#35819,0.1) ;
#30603=CYLINDRICAL_SURFACE('',#35821,0.1) ;
#30604=CYLINDRICAL_SURFACE('',#35826,0.1) ;
#30605=CYLINDRICAL_SURFACE('',#35831,0.1) ;
#30606=CYLINDRICAL_SURFACE('',#35848,0.1) ;
#30607=CYLINDRICAL_SURFACE('',#35849,0.1) ;
#30608=CYLINDRICAL_SURFACE('',#35853,0.1) ;
#30609=CYLINDRICAL_SURFACE('',#35854,0.1) ;
#30610=CYLINDRICAL_SURFACE('',#35876,0.1) ;
#30611=CYLINDRICAL_SURFACE('',#35882,3.429) ;
#30612=CYLINDRICAL_SURFACE('',#35891,0.1) ;
#30613=CYLINDRICAL_SURFACE('',#35896,3.429) ;
#32103=ADVANCED_FACE('',(#3624),#30547,.T.) ;
#32104=ADVANCED_FACE('',(#3625),#30548,.T.) ;
#32105=ADVANCED_FACE('',(#3626),#30549,.T.) ;
#32106=ADVANCED_FACE('',(#3627),#30550,.T.) ;
#32107=ADVANCED_FACE('',(#3628),#30551,.T.) ;
#32108=ADVANCED_FACE('',(#3629),#30552,.T.) ;
#32109=ADVANCED_FACE('',(#3630),#30553,.T.) ;
#32110=ADVANCED_FACE('',(#3631),#30554,.T.) ;
#32111=ADVANCED_FACE('',(#3632),#30555,.T.) ;
#32112=ADVANCED_FACE('',(#3633),#30556,.T.) ;
#32113=ADVANCED_FACE('',(#3634),#30557,.T.) ;
#32114=ADVANCED_FACE('',(#3635),#30558,.T.) ;
#32115=ADVANCED_FACE('',(#3636),#30559,.T.) ;
#32116=ADVANCED_FACE('',(#3637),#30560,.T.) ;
#32117=ADVANCED_FACE('',(#3638),#30561,.T.) ;
#32118=ADVANCED_FACE('',(#3639),#30562,.T.) ;
#32119=ADVANCED_FACE('',(#3640),#30563,.T.) ;
#32120=ADVANCED_FACE('',(#3641),#922,.T.) ;
#32121=ADVANCED_FACE('',(#3642),#923,.T.) ;
#32122=ADVANCED_FACE('',(#3643),#924,.T.) ;
#32123=ADVANCED_FACE('',(#3644),#925,.T.) ;
#32124=ADVANCED_FACE('',(#3645),#926,.T.) ;
#32125=ADVANCED_FACE('',(#3646),#927,.T.) ;
#32126=ADVANCED_FACE('',(#3647),#928,.T.) ;
#32127=ADVANCED_FACE('',(#3648),#929,.F.) ;
#32128=ADVANCED_FACE('',(#3649),#410,.T.) ;
#32129=ADVANCED_FACE('',(#3650),#411,.T.) ;
#32130=ADVANCED_FACE('',(#3651),#930,.T.) ;
#32131=ADVANCED_FACE('',(#3652),#931,.T.) ;
#32132=ADVANCED_FACE('',(#3653),#932,.T.) ;
#32133=ADVANCED_FACE('',(#3654),#933,.T.) ;
#32134=ADVANCED_FACE('',(#3655),#934,.T.) ;
#32135=ADVANCED_FACE('',(#3656),#935,.T.) ;
#32136=ADVANCED_FACE('',(#3657),#936,.T.) ;
#32137=ADVANCED_FACE('',(#3658),#30564,.T.) ;
#32138=ADVANCED_FACE('',(#3659),#2148,.T.) ;
#32139=ADVANCED_FACE('',(#3660),#937,.T.) ;
#32140=ADVANCED_FACE('',(#3661),#938,.T.) ;
#32141=ADVANCED_FACE('',(#3662),#939,.T.) ;
#32142=ADVANCED_FACE('',(#3663),#940,.T.) ;
#32143=ADVANCED_FACE('',(#3664),#941,.T.) ;
#32144=ADVANCED_FACE('',(#3665),#942,.T.) ;
#32145=ADVANCED_FACE('',(#3666),#943,.T.) ;
#32146=ADVANCED_FACE('',(#3667),#944,.F.) ;
#32147=ADVANCED_FACE('',(#3668),#412,.T.) ;
#32148=ADVANCED_FACE('',(#3669),#945,.T.) ;
#32149=ADVANCED_FACE('',(#3670),#946,.T.) ;
#32150=ADVANCED_FACE('',(#3671),#947,.T.) ;
#32151=ADVANCED_FACE('',(#3672),#948,.T.) ;
#32152=ADVANCED_FACE('',(#3673),#949,.T.) ;
#32153=ADVANCED_FACE('',(#3674),#950,.T.) ;
#32154=ADVANCED_FACE('',(#3675),#951,.T.) ;
#32155=ADVANCED_FACE('',(#3676),#30565,.T.) ;
#32156=ADVANCED_FACE('',(#3677),#2149,.F.) ;
#32157=ADVANCED_FACE('',(#3678),#952,.F.) ;
#32158=ADVANCED_FACE('',(#3679),#30566,.T.) ;
#32159=ADVANCED_FACE('',(#3680),#83,.T.) ;
#32160=ADVANCED_FACE('',(#3681),#413,.T.) ;
#32161=ADVANCED_FACE('',(#3682),#2150,.T.) ;
#32162=ADVANCED_FACE('',(#3683),#30567,.F.) ;
#32163=ADVANCED_FACE('',(#3684),#953,.T.) ;
#32164=ADVANCED_FACE('',(#3685),#954,.T.) ;
#32165=ADVANCED_FACE('',(#3686),#955,.T.) ;
#32166=ADVANCED_FACE('',(#3687),#84,.F.) ;
#32167=ADVANCED_FACE('',(#3688),#85,.F.) ;
#32168=ADVANCED_FACE('',(#3689),#956,.T.) ;
#32169=ADVANCED_FACE('',(#3690),#957,.T.) ;
#32170=ADVANCED_FACE('',(#3691),#958,.T.) ;
#32171=ADVANCED_FACE('',(#3692),#414,.T.) ;
#32172=ADVANCED_FACE('',(#3693),#2151,.T.) ;
#32173=ADVANCED_FACE('',(#3694),#30568,.F.) ;
#32174=ADVANCED_FACE('',(#3695),#959,.F.) ;
#32175=ADVANCED_FACE('',(#3696),#30569,.T.) ;
#32176=ADVANCED_FACE('',(#3697),#86,.T.) ;
#32177=ADVANCED_FACE('',(#3698),#2152,.T.) ;
#32178=ADVANCED_FACE('',(#3699),#30570,.F.) ;
#32179=ADVANCED_FACE('',(#3700),#87,.F.) ;
#32180=ADVANCED_FACE('',(#3701),#960,.T.) ;
#32181=ADVANCED_FACE('',(#3702),#961,.T.) ;
#32182=ADVANCED_FACE('',(#3703),#962,.T.) ;
#32183=ADVANCED_FACE('',(#3704),#415,.T.) ;
#32184=ADVANCED_FACE('',(#3705),#892,.F.) ;
#32185=ADVANCED_FACE('',(#3706),#416,.F.) ;
#32186=ADVANCED_FACE('',(#3707),#30571,.F.) ;
#32187=ADVANCED_FACE('',(#3708),#88,.F.) ;
#32188=ADVANCED_FACE('',(#3709),#963,.T.) ;
#32189=ADVANCED_FACE('',(#3710),#964,.T.) ;
#32190=ADVANCED_FACE('',(#3711),#965,.T.) ;
#32191=ADVANCED_FACE('',(#3712),#417,.T.) ;
#32192=ADVANCED_FACE('',(#3713),#2153,.T.) ;
#32193=ADVANCED_FACE('',(#3714),#30572,.F.) ;
#32194=ADVANCED_FACE('',(#3715),#966,.F.) ;
#32195=ADVANCED_FACE('',(#3716),#30573,.T.) ;
#32196=ADVANCED_FACE('',(#3717),#89,.T.) ;
#32197=ADVANCED_FACE('',(#3718),#2154,.T.) ;
#32198=ADVANCED_FACE('',(#3719),#30574,.F.) ;
#32199=ADVANCED_FACE('',(#3720),#967,.F.) ;
#32200=ADVANCED_FACE('',(#3721),#30575,.T.) ;
#32201=ADVANCED_FACE('',(#3722),#90,.T.) ;
#32202=ADVANCED_FACE('',(#3723),#2155,.T.) ;
#32203=ADVANCED_FACE('',(#3724),#30576,.F.) ;
#32204=ADVANCED_FACE('',(#3725),#968,.T.) ;
#32205=ADVANCED_FACE('',(#3726),#418,.F.) ;
#32206=ADVANCED_FACE('',(#3727),#969,.T.) ;
#32207=ADVANCED_FACE('',(#3728),#744,.T.) ;
#32208=ADVANCED_FACE('',(#3729,#1169),#2156,.T.) ;
#32209=ADVANCED_FACE('',(#3730),#970,.T.) ;
#32210=ADVANCED_FACE('',(#3731),#971,.T.) ;
#32211=ADVANCED_FACE('',(#3732),#972,.T.) ;
#32212=ADVANCED_FACE('',(#3733),#91,.F.) ;
#32213=ADVANCED_FACE('',(#3734),#2157,.T.) ;
#32214=ADVANCED_FACE('',(#3735),#30577,.T.) ;
#32215=ADVANCED_FACE('',(#3736),#419,.T.) ;
#32216=ADVANCED_FACE('',(#3737),#92,.F.) ;
#32217=ADVANCED_FACE('',(#3738),#973,.T.) ;
#32218=ADVANCED_FACE('',(#3739),#974,.T.) ;
#32219=ADVANCED_FACE('',(#3740),#975,.T.) ;
#32220=ADVANCED_FACE('',(#3741),#30578,.T.) ;
#32221=ADVANCED_FACE('',(#3742),#2158,.T.) ;
#32222=ADVANCED_FACE('',(#3743),#30579,.F.) ;
#32223=ADVANCED_FACE('',(#3744),#2159,.F.) ;
#32224=ADVANCED_FACE('',(#3745),#976,.F.) ;
#32225=ADVANCED_FACE('',(#3746),#30580,.T.) ;
#32226=ADVANCED_FACE('',(#3747),#977,.F.) ;
#32227=ADVANCED_FACE('',(#3748),#30581,.T.) ;
#32228=ADVANCED_FACE('',(#3749),#93,.T.) ;
#32229=ADVANCED_FACE('',(#3750),#94,.T.) ;
#32230=ADVANCED_FACE('',(#3751),#30582,.F.) ;
#32231=ADVANCED_FACE('',(#3752),#2160,.T.) ;
#32232=ADVANCED_FACE('',(#3753),#30583,.F.) ;
#32233=ADVANCED_FACE('',(#3754),#95,.T.) ;
#32234=ADVANCED_FACE('',(#3755),#30584,.T.) ;
#32235=ADVANCED_FACE('',(#3756),#30585,.T.) ;
#32236=ADVANCED_FACE('',(#3757),#978,.F.) ;
#32237=ADVANCED_FACE('',(#3758),#979,.F.) ;
#32238=ADVANCED_FACE('',(#3759),#30586,.T.) ;
#32239=ADVANCED_FACE('',(#3760),#96,.T.) ;
#32240=ADVANCED_FACE('',(#3761),#30587,.T.) ;
#32241=ADVANCED_FACE('',(#3762),#980,.F.) ;
#32242=ADVANCED_FACE('',(#3763),#97,.T.) ;
#32243=ADVANCED_FACE('',(#3764),#420,.T.) ;
#32244=ADVANCED_FACE('',(#3765),#421,.T.) ;
#32245=ADVANCED_FACE('',(#3766),#2161,.F.) ;
#32246=ADVANCED_FACE('',(#3767),#30588,.F.) ;
#32247=ADVANCED_FACE('',(#3768),#2162,.T.) ;
#32248=ADVANCED_FACE('',(#3769),#98,.T.) ;
#32249=ADVANCED_FACE('',(#3770),#30589,.T.) ;
#32250=ADVANCED_FACE('',(#3771),#30590,.T.) ;
#32251=ADVANCED_FACE('',(#3772),#981,.F.) ;
#32252=ADVANCED_FACE('',(#3773),#30591,.F.) ;
#32253=ADVANCED_FACE('',(#3774),#30592,.F.) ;
#32254=ADVANCED_FACE('',(#3775),#982,.F.) ;
#32255=ADVANCED_FACE('',(#3776),#983,.F.) ;
#32256=ADVANCED_FACE('',(#3777),#30593,.F.) ;
#32257=ADVANCED_FACE('',(#3778),#984,.T.) ;
#32258=ADVANCED_FACE('',(#3779),#985,.T.) ;
#32259=ADVANCED_FACE('',(#3780),#986,.T.) ;
#32260=ADVANCED_FACE('',(#3781),#99,.F.) ;
#32261=ADVANCED_FACE('',(#3782),#2163,.T.) ;
#32262=ADVANCED_FACE('',(#3783),#30594,.T.) ;
#32263=ADVANCED_FACE('',(#3784),#422,.T.) ;
#32264=ADVANCED_FACE('',(#3785),#100,.F.) ;
#32265=ADVANCED_FACE('',(#3786),#987,.T.) ;
#32266=ADVANCED_FACE('',(#3787),#988,.T.) ;
#32267=ADVANCED_FACE('',(#3788),#989,.T.) ;
#32268=ADVANCED_FACE('',(#3789),#30595,.T.) ;
#32269=ADVANCED_FACE('',(#3790),#2164,.T.) ;
#32270=ADVANCED_FACE('',(#3791),#30596,.F.) ;
#32271=ADVANCED_FACE('',(#3792),#2165,.F.) ;
#32272=ADVANCED_FACE('',(#3793),#30597,.T.) ;
#32273=ADVANCED_FACE('',(#3794),#990,.F.) ;
#32274=ADVANCED_FACE('',(#3795),#991,.F.) ;
#32275=ADVANCED_FACE('',(#3796),#30598,.T.) ;
#32276=ADVANCED_FACE('',(#3797),#101,.T.) ;
#32277=ADVANCED_FACE('',(#3798),#102,.T.) ;
#32278=ADVANCED_FACE('',(#3799),#30599,.F.) ;
#32279=ADVANCED_FACE('',(#3800),#30600,.F.) ;
#32280=ADVANCED_FACE('',(#3801),#2166,.T.) ;
#32281=ADVANCED_FACE('',(#3802),#30601,.F.) ;
#32282=ADVANCED_FACE('',(#3803),#103,.T.) ;
#32283=ADVANCED_FACE('',(#3804),#30602,.T.) ;
#32284=ADVANCED_FACE('',(#3805),#992,.F.) ;
#32285=ADVANCED_FACE('',(#3806),#30603,.T.) ;
#32286=ADVANCED_FACE('',(#3807),#2167,.T.) ;
#32287=ADVANCED_FACE('',(#3808),#993,.F.) ;
#32288=ADVANCED_FACE('',(#3809),#30604,.T.) ;
#32289=ADVANCED_FACE('',(#3810),#104,.T.) ;
#32290=ADVANCED_FACE('',(#3811),#30605,.T.) ;
#32291=ADVANCED_FACE('',(#3812),#994,.F.) ;
#32292=ADVANCED_FACE('',(#3813),#105,.T.) ;
#32293=ADVANCED_FACE('',(#3814),#423,.T.) ;
#32294=ADVANCED_FACE('',(#3815),#424,.T.) ;
#32295=ADVANCED_FACE('',(#3816),#2168,.T.) ;
#32296=ADVANCED_FACE('',(#3817),#2169,.T.) ;
#32297=ADVANCED_FACE('',(#3818),#106,.T.) ;
#32298=ADVANCED_FACE('',(#3819),#30606,.T.) ;
#32299=ADVANCED_FACE('',(#3820),#30607,.T.) ;
#32300=ADVANCED_FACE('',(#3821),#995,.F.) ;
#32301=ADVANCED_FACE('',(#3822),#30608,.F.) ;
#32302=ADVANCED_FACE('',(#3823),#30609,.F.) ;
#32303=ADVANCED_FACE('',(#3824),#425,.F.) ;
#32304=ADVANCED_FACE('',(#3825),#426,.F.) ;
#32305=ADVANCED_FACE('',(#3826),#427,.F.) ;
#32306=ADVANCED_FACE('',(#3827),#2170,.T.) ;
#32307=ADVANCED_FACE('',(#3828),#893,.F.) ;
#32308=ADVANCED_FACE('',(#3829),#2171,.T.) ;
#32309=ADVANCED_FACE('',(#3830),#428,.T.) ;
#32310=ADVANCED_FACE('',(#3831),#996,.F.) ;
#32311=ADVANCED_FACE('',(#3832),#429,.T.) ;
#32312=ADVANCED_FACE('',(#3833),#430,.T.) ;
#32313=ADVANCED_FACE('',(#3834),#30610,.T.) ;
#32314=ADVANCED_FACE('',(#3835),#997,.F.) ;
#32315=ADVANCED_FACE('',(#3836),#107,.T.) ;
#32316=ADVANCED_FACE('',(#3837),#431,.T.) ;
#32317=ADVANCED_FACE('',(#3838),#30611,.T.) ;
#32318=ADVANCED_FACE('',(#3839),#998,.F.) ;
#32319=ADVANCED_FACE('',(#3840),#432,.T.) ;
#32320=ADVANCED_FACE('',(#3841),#433,.T.) ;
#32321=ADVANCED_FACE('',(#3842),#434,.T.) ;
#32322=ADVANCED_FACE('',(#3843),#999,.F.) ;
#32323=ADVANCED_FACE('',(#3844),#30612,.T.) ;
#32324=ADVANCED_FACE('',(#3845),#108,.T.) ;
#32325=ADVANCED_FACE('',(#3846),#435,.T.) ;
#32326=ADVANCED_FACE('',(#3847),#30613,.T.) ;
#32327=ADVANCED_FACE('',(#3848),#894,.T.) ;
#32328=ADVANCED_FACE('',(#3849),#895,.F.) ;
#32329=ADVANCED_FACE('',(#3850),#896,.F.) ;
#32330=ADVANCED_FACE('',(#3851),#2172,.F.) ;
#32331=ADVANCED_FACE('',(#3852),#745,.T.) ;
#32642=CLOSED_SHELL('',(#32103,#32104,#32105,#32106,#32107,#32108,#32109,
#32110,#32111,#32112,#32113,#32114,#32115,#32116,#32117,#32118,#32119,#32120,
#32121,#32122,#32123,#32124,#32125,#32126,#32127,#32128,#32129,#32130,#32131,
#32132,#32133,#32134,#32135,#32136,#32137,#32138,#32139,#32140,#32141,#32142,
#32143,#32144,#32145,#32146,#32147,#32148,#32149,#32150,#32151,#32152,#32153,
#32154,#32155,#32156,#32157,#32158,#32159,#32160,#32161,#32162,#32163,#32164,
#32165,#32166,#32167,#32168,#32169,#32170,#32171,#32172,#32173,#32174,#32175,
#32176,#32177,#32178,#32179,#32180,#32181,#32182,#32183,#32184,#32185,#32186,
#32187,#32188,#32189,#32190,#32191,#32192,#32193,#32194,#32195,#32196,#32197,
#32198,#32199,#32200,#32201,#32202,#32203,#32204,#32205,#32206,#32207,#32208,
#32209,#32210,#32211,#32212,#32213,#32214,#32215,#32216,#32217,#32218,#32219,
#32220,#32221,#32222,#32223,#32224,#32225,#32226,#32227,#32228,#32229,#32230,
#32231,#32232,#32233,#32234,#32235,#32236,#32237,#32238,#32239,#32240,#32241,
#32242,#32243,#32244,#32245,#32246,#32247,#32248,#32249,#32250,#32251,#32252,
#32253,#32254,#32255,#32256,#32257,#32258,#32259,#32260,#32261,#32262,#32263,
#32264,#32265,#32266,#32267,#32268,#32269,#32270,#32271,#32272,#32273,#32274,
#32275,#32276,#32277,#32278,#32279,#32280,#32281,#32282,#32283,#32284,#32285,
#32286,#32287,#32288,#32289,#32290,#32291,#32292,#32293,#32294,#32295,#32296,
#32297,#32298,#32299,#32300,#32301,#32302,#32303,#32304,#32305,#32306,#32307,
#32308,#32309,#32310,#32311,#32312,#32313,#32314,#32315,#32316,#32317,#32318,
#32319,#32320,#32321,#32322,#32323,#32324,#32325,#32326,#32327,#32328,#32329,
#32330,#32331)) ;
#35475=AXIS2_PLACEMENT_3D('',#73261,#43757,#43758) ;
#35476=AXIS2_PLACEMENT_3D('',#73262,#43759,#43760) ;
#35477=AXIS2_PLACEMENT_3D('',#73333,#43762,#43763) ;
#35478=AXIS2_PLACEMENT_3D('',#73409,#43765,#43766) ;
#35479=AXIS2_PLACEMENT_3D('',#73485,#43768,#43769) ;
#35480=AXIS2_PLACEMENT_3D('',#73561,#43771,#43772) ;
#35481=AXIS2_PLACEMENT_3D('',#73637,#43774,#43775) ;
#35482=AXIS2_PLACEMENT_3D('',#73713,#43777,#43778) ;
#35483=AXIS2_PLACEMENT_3D('',#73789,#43780,#43781) ;
#35484=AXIS2_PLACEMENT_3D('',#73794,#43783,#43784) ;
#35485=AXIS2_PLACEMENT_3D('',#73865,#43785,#43786) ;
#35486=AXIS2_PLACEMENT_3D('',#73895,#43788,#43789) ;
#35487=AXIS2_PLACEMENT_3D('',#73916,#43790,#43791) ;
#35488=AXIS2_PLACEMENT_3D('',#73992,#43793,#43794) ;
#35489=AXIS2_PLACEMENT_3D('',#74068,#43796,#43797) ;
#35490=AXIS2_PLACEMENT_3D('',#74144,#43799,#43800) ;
#35491=AXIS2_PLACEMENT_3D('',#74220,#43802,#43803) ;
#35492=AXIS2_PLACEMENT_3D('',#74296,#43805,#43806) ;
#35493=AXIS2_PLACEMENT_3D('',#74372,#43808,#43809) ;
#35494=AXIS2_PLACEMENT_3D('',#74399,#43810,#43811) ;
#35495=AXIS2_PLACEMENT_3D('',#74431,#43812,#43813) ;
#35496=AXIS2_PLACEMENT_3D('',#74437,#43814,#43815) ;
#35497=AXIS2_PLACEMENT_3D('',#74464,#43816,#43817) ;
#35498=AXIS2_PLACEMENT_3D('',#74504,#43818,#43819) ;
#35499=AXIS2_PLACEMENT_3D('',#74540,#43820,#43821) ;
#35500=AXIS2_PLACEMENT_3D('',#74573,#43822,#43823) ;
#35501=AXIS2_PLACEMENT_3D('',#74574,#43824,#43825) ;
#35502=AXIS2_PLACEMENT_3D('',#74575,#43826,#43827) ;
#35503=AXIS2_PLACEMENT_3D('',#74650,#43828,#43829) ;
#35504=AXIS2_PLACEMENT_3D('',#74683,#43831,#43832) ;
#35505=AXIS2_PLACEMENT_3D('',#74772,#43835,#43836) ;
#35506=AXIS2_PLACEMENT_3D('',#74773,#43837,#43838) ;
#35507=AXIS2_PLACEMENT_3D('',#74774,#43839,#43840) ;
#35508=AXIS2_PLACEMENT_3D('',#74777,#43841,#43842) ;
#35509=AXIS2_PLACEMENT_3D('',#74786,#43843,#43844) ;
#35510=AXIS2_PLACEMENT_3D('',#74788,#43845,#43846) ;
#35511=AXIS2_PLACEMENT_3D('',#74790,#43847,#43848) ;
#35512=AXIS2_PLACEMENT_3D('',#74798,#43849,#43850) ;
#35513=AXIS2_PLACEMENT_3D('',#74800,#43851,#43852) ;
#35514=AXIS2_PLACEMENT_3D('',#74802,#43853,#43854) ;
#35515=AXIS2_PLACEMENT_3D('',#74810,#43855,#43856) ;
#35516=AXIS2_PLACEMENT_3D('',#74812,#43857,#43858) ;
#35517=AXIS2_PLACEMENT_3D('',#74813,#43859,#43860) ;
#35518=AXIS2_PLACEMENT_3D('',#74814,#43861,#43862) ;
#35519=AXIS2_PLACEMENT_3D('',#74816,#43863,#43864) ;
#35520=AXIS2_PLACEMENT_3D('',#74818,#43865,#43866) ;
#35521=AXIS2_PLACEMENT_3D('',#74825,#43867,#43868) ;
#35522=AXIS2_PLACEMENT_3D('',#74851,#43869,#43870) ;
#35523=AXIS2_PLACEMENT_3D('',#74879,#43871,#43872) ;
#35524=AXIS2_PLACEMENT_3D('',#74916,#43873,#43874) ;
#35525=AXIS2_PLACEMENT_3D('',#74943,#43875,#43876) ;
#35526=AXIS2_PLACEMENT_3D('',#74944,#43877,#43878) ;
#35527=AXIS2_PLACEMENT_3D('',#75016,#43880,#43881) ;
#35528=AXIS2_PLACEMENT_3D('',#75040,#43883,#43884) ;
#35529=AXIS2_PLACEMENT_3D('',#75111,#43886,#43887) ;
#35530=AXIS2_PLACEMENT_3D('',#75115,#43889,#43890) ;
#35531=AXIS2_PLACEMENT_3D('',#75117,#43892,#43893) ;
#35532=AXIS2_PLACEMENT_3D('',#75123,#43896,#43897) ;
#35533=AXIS2_PLACEMENT_3D('',#75154,#43898,#43899) ;
#35534=AXIS2_PLACEMENT_3D('',#75187,#43900,#43901) ;
#35535=AXIS2_PLACEMENT_3D('',#75223,#43902,#43903) ;
#35536=AXIS2_PLACEMENT_3D('',#75256,#43904,#43905) ;
#35537=AXIS2_PLACEMENT_3D('',#75257,#43906,#43907) ;
#35538=AXIS2_PLACEMENT_3D('',#75258,#43908,#43909) ;
#35539=AXIS2_PLACEMENT_3D('',#75306,#43910,#43911) ;
#35540=AXIS2_PLACEMENT_3D('',#75392,#43913,#43914) ;
#35541=AXIS2_PLACEMENT_3D('',#75478,#43917,#43918) ;
#35542=AXIS2_PLACEMENT_3D('',#75479,#43919,#43920) ;
#35543=AXIS2_PLACEMENT_3D('',#75481,#43921,#43922) ;
#35544=AXIS2_PLACEMENT_3D('',#75483,#43923,#43924) ;
#35545=AXIS2_PLACEMENT_3D('',#75490,#43925,#43926) ;
#35546=AXIS2_PLACEMENT_3D('',#75516,#43927,#43928) ;
#35547=AXIS2_PLACEMENT_3D('',#75544,#43929,#43930) ;
#35548=AXIS2_PLACEMENT_3D('',#75581,#43931,#43932) ;
#35549=AXIS2_PLACEMENT_3D('',#75608,#43933,#43934) ;
#35550=AXIS2_PLACEMENT_3D('',#75609,#43935,#43936) ;
#35551=AXIS2_PLACEMENT_3D('',#75681,#43938,#43939) ;
#35552=AXIS2_PLACEMENT_3D('',#75705,#43941,#43942) ;
#35553=AXIS2_PLACEMENT_3D('',#75776,#43944,#43945) ;
#35554=AXIS2_PLACEMENT_3D('',#75780,#43947,#43948) ;
#35555=AXIS2_PLACEMENT_3D('',#75782,#43950,#43951) ;
#35556=AXIS2_PLACEMENT_3D('',#75788,#43954,#43955) ;
#35557=AXIS2_PLACEMENT_3D('',#75789,#43956,#43957) ;
#35558=AXIS2_PLACEMENT_3D('',#75808,#43958,#43959) ;
#35559=AXIS2_PLACEMENT_3D('',#75810,#43960,#43961) ;
#35560=AXIS2_PLACEMENT_3D('',#75811,#43962,#43963) ;
#35561=AXIS2_PLACEMENT_3D('',#75812,#43964,#43965) ;
#35562=AXIS2_PLACEMENT_3D('',#75816,#43967,#43968) ;
#35563=AXIS2_PLACEMENT_3D('',#75818,#43970,#43971) ;
#35564=AXIS2_PLACEMENT_3D('',#75820,#43972,#43973) ;
#35565=AXIS2_PLACEMENT_3D('',#75821,#43974,#43975) ;
#35566=AXIS2_PLACEMENT_3D('',#75822,#43976,#43977) ;
#35567=AXIS2_PLACEMENT_3D('',#75824,#43978,#43979) ;
#35568=AXIS2_PLACEMENT_3D('',#75832,#43980,#43981) ;
#35569=AXIS2_PLACEMENT_3D('',#75833,#43982,#43983) ;
#35570=AXIS2_PLACEMENT_3D('',#75841,#43985,#43986) ;
#35571=AXIS2_PLACEMENT_3D('',#75842,#43987,#43988) ;
#35572=AXIS2_PLACEMENT_3D('',#75845,#43990,#43991) ;
#35573=AXIS2_PLACEMENT_3D('',#75883,#43992,#43993) ;
#35574=AXIS2_PLACEMENT_3D('',#75905,#43994,#43995) ;
#35575=AXIS2_PLACEMENT_3D('',#75906,#43996,#43997) ;
#35576=AXIS2_PLACEMENT_3D('',#75928,#43998,#43999) ;
#35577=AXIS2_PLACEMENT_3D('',#75937,#44000,#44001) ;
#35578=AXIS2_PLACEMENT_3D('',#75938,#44002,#44003) ;
#35579=AXIS2_PLACEMENT_3D('',#75939,#44004,#44005) ;
#35580=AXIS2_PLACEMENT_3D('',#75942,#44006,#44007) ;
#35581=AXIS2_PLACEMENT_3D('',#75944,#44008,#44009) ;
#35582=AXIS2_PLACEMENT_3D('',#75945,#44010,#44011) ;
#35583=AXIS2_PLACEMENT_3D('',#75968,#44012,#44013) ;
#35584=AXIS2_PLACEMENT_3D('',#76003,#44014,#44015) ;
#35585=AXIS2_PLACEMENT_3D('',#76004,#44016,#44017) ;
#35586=AXIS2_PLACEMENT_3D('',#76005,#44018,#44019) ;
#35587=AXIS2_PLACEMENT_3D('',#76049,#44020,#44021) ;
#35588=AXIS2_PLACEMENT_3D('',#76051,#44022,#44023) ;
#35589=AXIS2_PLACEMENT_3D('',#76053,#44024,#44025) ;
#35590=AXIS2_PLACEMENT_3D('',#76054,#44026,#44027) ;
#35591=AXIS2_PLACEMENT_3D('',#76055,#44028,#44029) ;
#35592=AXIS2_PLACEMENT_3D('',#76059,#44032,#44033) ;
#35593=AXIS2_PLACEMENT_3D('',#76062,#44035,#44036) ;
#35594=AXIS2_PLACEMENT_3D('',#76080,#44037,#44038) ;
#35595=AXIS2_PLACEMENT_3D('',#76081,#44039,#44040) ;
#35596=AXIS2_PLACEMENT_3D('',#76082,#44041,#44042) ;
#35597=AXIS2_PLACEMENT_3D('',#76085,#44044,#44045) ;
#35598=AXIS2_PLACEMENT_3D('',#76086,#44046,#44047) ;
#35599=AXIS2_PLACEMENT_3D('',#76087,#44048,#44049) ;
#35600=AXIS2_PLACEMENT_3D('',#76088,#44050,#44051) ;
#35601=AXIS2_PLACEMENT_3D('',#76094,#44054,#44055) ;
#35602=AXIS2_PLACEMENT_3D('',#76097,#44057,#44058) ;
#35603=AXIS2_PLACEMENT_3D('',#76098,#44059,#44060) ;
#35604=AXIS2_PLACEMENT_3D('',#76101,#44062,#44063) ;
#35605=AXIS2_PLACEMENT_3D('',#76102,#44064,#44065) ;
#35606=AXIS2_PLACEMENT_3D('',#76105,#44066,#44067) ;
#35607=AXIS2_PLACEMENT_3D('',#76107,#44068,#44069) ;
#35608=AXIS2_PLACEMENT_3D('',#76108,#44070,#44071) ;
#35609=AXIS2_PLACEMENT_3D('',#76131,#44072,#44073) ;
#35610=AXIS2_PLACEMENT_3D('',#76165,#44074,#44075) ;
#35611=AXIS2_PLACEMENT_3D('',#76167,#44076,#44077) ;
#35612=AXIS2_PLACEMENT_3D('',#76168,#44078,#44079) ;
#35613=AXIS2_PLACEMENT_3D('',#76212,#44080,#44081) ;
#35614=AXIS2_PLACEMENT_3D('',#76214,#44082,#44083) ;
#35615=AXIS2_PLACEMENT_3D('',#76216,#44084,#44085) ;
#35616=AXIS2_PLACEMENT_3D('',#76224,#44086,#44087) ;
#35617=AXIS2_PLACEMENT_3D('',#76225,#44088,#44089) ;
#35618=AXIS2_PLACEMENT_3D('',#76227,#44090,#44091) ;
#35619=AXIS2_PLACEMENT_3D('',#76236,#44092,#44093) ;
#35620=AXIS2_PLACEMENT_3D('',#76238,#44094,#44095) ;
#35621=AXIS2_PLACEMENT_3D('',#76239,#44096,#44097) ;
#35622=AXIS2_PLACEMENT_3D('',#76240,#44098,#44099) ;
#35623=AXIS2_PLACEMENT_3D('',#76244,#44101,#44102) ;
#35624=AXIS2_PLACEMENT_3D('',#76246,#44104,#44105) ;
#35625=AXIS2_PLACEMENT_3D('',#76248,#44106,#44107) ;
#35626=AXIS2_PLACEMENT_3D('',#76249,#44108,#44109) ;
#35627=AXIS2_PLACEMENT_3D('',#76271,#44110,#44111) ;
#35628=AXIS2_PLACEMENT_3D('',#76297,#44112,#44113) ;
#35629=AXIS2_PLACEMENT_3D('',#76298,#44114,#44115) ;
#35630=AXIS2_PLACEMENT_3D('',#76335,#44116,#44117) ;
#35631=AXIS2_PLACEMENT_3D('',#76337,#44118,#44119) ;
#35632=AXIS2_PLACEMENT_3D('',#76339,#44120,#44121) ;
#35633=AXIS2_PLACEMENT_3D('',#76340,#44122,#44123) ;
#35634=AXIS2_PLACEMENT_3D('',#76341,#44124,#44125) ;
#35635=AXIS2_PLACEMENT_3D('',#76345,#44128,#44129) ;
#35636=AXIS2_PLACEMENT_3D('',#76348,#44131,#44132) ;
#35637=AXIS2_PLACEMENT_3D('',#76366,#44133,#44134) ;
#35638=AXIS2_PLACEMENT_3D('',#76367,#44135,#44136) ;
#35639=AXIS2_PLACEMENT_3D('',#76368,#44137,#44138) ;
#35640=AXIS2_PLACEMENT_3D('',#76371,#44140,#44141) ;
#35641=AXIS2_PLACEMENT_3D('',#76372,#44142,#44143) ;
#35642=AXIS2_PLACEMENT_3D('',#76373,#44144,#44145) ;
#35643=AXIS2_PLACEMENT_3D('',#76374,#44146,#44147) ;
#35644=AXIS2_PLACEMENT_3D('',#76380,#44150,#44151) ;
#35645=AXIS2_PLACEMENT_3D('',#76383,#44153,#44154) ;
#35646=AXIS2_PLACEMENT_3D('',#76384,#44155,#44156) ;
#35647=AXIS2_PLACEMENT_3D('',#76387,#44158,#44159) ;
#35648=AXIS2_PLACEMENT_3D('',#76405,#44160,#44161) ;
#35649=AXIS2_PLACEMENT_3D('',#76406,#44162,#44163) ;
#35650=AXIS2_PLACEMENT_3D('',#76407,#44164,#44165) ;
#35651=AXIS2_PLACEMENT_3D('',#76411,#44167,#44168) ;
#35652=AXIS2_PLACEMENT_3D('',#76413,#44170,#44171) ;
#35653=AXIS2_PLACEMENT_3D('',#76415,#44172,#44173) ;
#35654=AXIS2_PLACEMENT_3D('',#76416,#44174,#44175) ;
#35655=AXIS2_PLACEMENT_3D('',#76417,#44176,#44177) ;
#35656=AXIS2_PLACEMENT_3D('',#76418,#44178,#44179) ;
#35657=AXIS2_PLACEMENT_3D('',#76419,#44180,#44181) ;
#35658=AXIS2_PLACEMENT_3D('',#76423,#44183,#44184) ;
#35659=AXIS2_PLACEMENT_3D('',#76495,#44186,#44187) ;
#35660=AXIS2_PLACEMENT_3D('',#76497,#44188,#44189) ;
#35661=AXIS2_PLACEMENT_3D('',#76544,#44190,#44191) ;
#35662=AXIS2_PLACEMENT_3D('',#76564,#44192,#44193) ;
#35663=AXIS2_PLACEMENT_3D('',#76694,#44194,#44195) ;
#35664=AXIS2_PLACEMENT_3D('',#76695,#44196,#44197) ;
#35665=AXIS2_PLACEMENT_3D('',#77298,#44198,#44199) ;
#35666=AXIS2_PLACEMENT_3D('',#77325,#44200,#44201) ;
#35667=AXIS2_PLACEMENT_3D('',#77327,#44202,#44203) ;
#35668=AXIS2_PLACEMENT_3D('',#77329,#44204,#44205) ;
#35669=AXIS2_PLACEMENT_3D('',#77331,#44206,#44207) ;
#35670=AXIS2_PLACEMENT_3D('',#77337,#44210,#44211) ;
#35671=AXIS2_PLACEMENT_3D('',#77339,#44212,#44213) ;
#35672=AXIS2_PLACEMENT_3D('',#77340,#44214,#44215) ;
#35673=AXIS2_PLACEMENT_3D('',#77363,#44216,#44217) ;
#35674=AXIS2_PLACEMENT_3D('',#77364,#44218,#44219) ;
#35675=AXIS2_PLACEMENT_3D('',#77365,#44220,#44221) ;
#35676=AXIS2_PLACEMENT_3D('',#77389,#44223,#44224) ;
#35677=AXIS2_PLACEMENT_3D('',#77391,#44226,#44227) ;
#35678=AXIS2_PLACEMENT_3D('',#77393,#44228,#44229) ;
#35679=AXIS2_PLACEMENT_3D('',#77394,#44230,#44231) ;
#35680=AXIS2_PLACEMENT_3D('',#77395,#44232,#44233) ;
#35681=AXIS2_PLACEMENT_3D('',#77401,#44237,#44238) ;
#35682=AXIS2_PLACEMENT_3D('',#77404,#44240,#44241) ;
#35683=AXIS2_PLACEMENT_3D('',#77405,#44242,#44243) ;
#35684=AXIS2_PLACEMENT_3D('',#77407,#44244,#44245) ;
#35685=AXIS2_PLACEMENT_3D('',#77420,#44246,#44247) ;
#35686=AXIS2_PLACEMENT_3D('',#77421,#44248,#44249) ;
#35687=AXIS2_PLACEMENT_3D('',#77424,#44250,#44251) ;
#35688=AXIS2_PLACEMENT_3D('',#77426,#44252,#44253) ;
#35689=AXIS2_PLACEMENT_3D('',#77427,#44254,#44255) ;
#35690=AXIS2_PLACEMENT_3D('',#77450,#44256,#44257) ;
#35691=AXIS2_PLACEMENT_3D('',#77474,#44260,#44261) ;
#35692=AXIS2_PLACEMENT_3D('',#77475,#44262,#44263) ;
#35693=AXIS2_PLACEMENT_3D('',#77476,#44264,#44265) ;
#35694=AXIS2_PLACEMENT_3D('',#77518,#44266,#44267) ;
#35695=AXIS2_PLACEMENT_3D('',#77522,#44269,#44270) ;
#35696=AXIS2_PLACEMENT_3D('',#77524,#44272,#44273) ;
#35697=AXIS2_PLACEMENT_3D('',#77528,#44276,#44277) ;
#35698=AXIS2_PLACEMENT_3D('',#77531,#44279,#44280) ;
#35699=AXIS2_PLACEMENT_3D('',#77532,#44281,#44282) ;
#35700=AXIS2_PLACEMENT_3D('',#77556,#44287,#44288) ;
#35701=AXIS2_PLACEMENT_3D('',#77557,#44289,#44290) ;
#35702=AXIS2_PLACEMENT_3D('',#77558,#44291,#44292) ;
#35703=AXIS2_PLACEMENT_3D('',#77561,#44293,#44294) ;
#35704=AXIS2_PLACEMENT_3D('',#77589,#44297,#44298) ;
#35705=AXIS2_PLACEMENT_3D('',#77591,#44299,#44300) ;
#35706=AXIS2_PLACEMENT_3D('',#77592,#44301,#44302) ;
#35707=AXIS2_PLACEMENT_3D('',#77593,#44303,#44304) ;
#35708=AXIS2_PLACEMENT_3D('',#77594,#44305,#44306) ;
#35709=AXIS2_PLACEMENT_3D('',#77596,#44307,#44308) ;
#35710=AXIS2_PLACEMENT_3D('',#77598,#44310,#44311) ;
#35711=AXIS2_PLACEMENT_3D('',#77600,#44312,#44313) ;
#35712=AXIS2_PLACEMENT_3D('',#77601,#44314,#44315) ;
#35713=AXIS2_PLACEMENT_3D('',#77602,#44316,#44317) ;
#35714=AXIS2_PLACEMENT_3D('',#77603,#44318,#44319) ;
#35715=AXIS2_PLACEMENT_3D('',#77604,#44320,#44321) ;
#35716=AXIS2_PLACEMENT_3D('',#77607,#44323,#44324) ;
#35717=AXIS2_PLACEMENT_3D('',#77609,#44326,#44327) ;
#35718=AXIS2_PLACEMENT_3D('',#77613,#44330,#44331) ;
#35719=AXIS2_PLACEMENT_3D('',#77614,#44332,#44333) ;
#35720=AXIS2_PLACEMENT_3D('',#77615,#44334,#44335) ;
#35721=AXIS2_PLACEMENT_3D('',#77616,#44336,#44337) ;
#35722=AXIS2_PLACEMENT_3D('',#77617,#44338,#44339) ;
#35723=AXIS2_PLACEMENT_3D('',#77618,#44340,#44341) ;
#35724=AXIS2_PLACEMENT_3D('',#77619,#44342,#44343) ;
#35725=AXIS2_PLACEMENT_3D('',#77662,#44344,#44345) ;
#35726=AXIS2_PLACEMENT_3D('',#77663,#44346,#44347) ;
#35727=AXIS2_PLACEMENT_3D('',#77664,#44348,#44349) ;
#35728=AXIS2_PLACEMENT_3D('',#77665,#44350,#44351) ;
#35729=AXIS2_PLACEMENT_3D('',#77667,#44352,#44353) ;
#35730=AXIS2_PLACEMENT_3D('',#77669,#44355,#44356) ;
#35731=AXIS2_PLACEMENT_3D('',#77671,#44357,#44358) ;
#35732=AXIS2_PLACEMENT_3D('',#77672,#44359,#44360) ;
#35733=AXIS2_PLACEMENT_3D('',#77673,#44361,#44362) ;
#35734=AXIS2_PLACEMENT_3D('',#77675,#44363,#44364) ;
#35735=AXIS2_PLACEMENT_3D('',#77677,#44365,#44366) ;
#35736=AXIS2_PLACEMENT_3D('',#77695,#44368,#44369) ;
#35737=AXIS2_PLACEMENT_3D('',#77696,#44370,#44371) ;
#35738=AXIS2_PLACEMENT_3D('',#77697,#44372,#44373) ;
#35739=AXIS2_PLACEMENT_3D('',#77698,#44374,#44375) ;
#35740=AXIS2_PLACEMENT_3D('',#77699,#44376,#44377) ;
#35741=AXIS2_PLACEMENT_3D('',#77700,#44378,#44379) ;
#35742=AXIS2_PLACEMENT_3D('',#77702,#44380,#44381) ;
#35743=AXIS2_PLACEMENT_3D('',#77704,#44382,#44383) ;
#35744=AXIS2_PLACEMENT_3D('',#77705,#44384,#44385) ;
#35745=AXIS2_PLACEMENT_3D('',#77706,#44386,#44387) ;
#35746=AXIS2_PLACEMENT_3D('',#77709,#44389,#44390) ;
#35747=AXIS2_PLACEMENT_3D('',#77711,#44392,#44393) ;
#35748=AXIS2_PLACEMENT_3D('',#77712,#44394,#44395) ;
#35749=AXIS2_PLACEMENT_3D('',#77718,#44399,#44400) ;
#35750=AXIS2_PLACEMENT_3D('',#77719,#44401,#44402) ;
#35751=AXIS2_PLACEMENT_3D('',#77720,#44403,#44404) ;
#35752=AXIS2_PLACEMENT_3D('',#77721,#44405,#44406) ;
#35753=AXIS2_PLACEMENT_3D('',#77722,#44407,#44408) ;
#35754=AXIS2_PLACEMENT_3D('',#77723,#44409,#44410) ;
#35755=AXIS2_PLACEMENT_3D('',#77741,#44411,#44412) ;
#35756=AXIS2_PLACEMENT_3D('',#77742,#44413,#44414) ;
#35757=AXIS2_PLACEMENT_3D('',#77743,#44415,#44416) ;
#35758=AXIS2_PLACEMENT_3D('',#77745,#44418,#44419) ;
#35759=AXIS2_PLACEMENT_3D('',#77779,#44421,#44422) ;
#35760=AXIS2_PLACEMENT_3D('',#77784,#44425,#44426) ;
#35761=AXIS2_PLACEMENT_3D('',#77811,#44427,#44428) ;
#35762=AXIS2_PLACEMENT_3D('',#77813,#44429,#44430) ;
#35763=AXIS2_PLACEMENT_3D('',#77815,#44431,#44432) ;
#35764=AXIS2_PLACEMENT_3D('',#77817,#44433,#44434) ;
#35765=AXIS2_PLACEMENT_3D('',#77823,#44437,#44438) ;
#35766=AXIS2_PLACEMENT_3D('',#77825,#44439,#44440) ;
#35767=AXIS2_PLACEMENT_3D('',#77826,#44441,#44442) ;
#35768=AXIS2_PLACEMENT_3D('',#77849,#44443,#44444) ;
#35769=AXIS2_PLACEMENT_3D('',#77850,#44445,#44446) ;
#35770=AXIS2_PLACEMENT_3D('',#77851,#44447,#44448) ;
#35771=AXIS2_PLACEMENT_3D('',#77875,#44450,#44451) ;
#35772=AXIS2_PLACEMENT_3D('',#77877,#44453,#44454) ;
#35773=AXIS2_PLACEMENT_3D('',#77879,#44455,#44456) ;
#35774=AXIS2_PLACEMENT_3D('',#77880,#44457,#44458) ;
#35775=AXIS2_PLACEMENT_3D('',#77881,#44459,#44460) ;
#35776=AXIS2_PLACEMENT_3D('',#77887,#44464,#44465) ;
#35777=AXIS2_PLACEMENT_3D('',#77890,#44467,#44468) ;
#35778=AXIS2_PLACEMENT_3D('',#77891,#44469,#44470) ;
#35779=AXIS2_PLACEMENT_3D('',#77893,#44471,#44472) ;
#35780=AXIS2_PLACEMENT_3D('',#77906,#44473,#44474) ;
#35781=AXIS2_PLACEMENT_3D('',#77907,#44475,#44476) ;
#35782=AXIS2_PLACEMENT_3D('',#77910,#44477,#44478) ;
#35783=AXIS2_PLACEMENT_3D('',#77912,#44479,#44480) ;
#35784=AXIS2_PLACEMENT_3D('',#77913,#44481,#44482) ;
#35785=AXIS2_PLACEMENT_3D('',#77936,#44483,#44484) ;
#35786=AXIS2_PLACEMENT_3D('',#77960,#44487,#44488) ;
#35787=AXIS2_PLACEMENT_3D('',#77961,#44489,#44490) ;
#35788=AXIS2_PLACEMENT_3D('',#77962,#44491,#44492) ;
#35789=AXIS2_PLACEMENT_3D('',#78004,#44493,#44494) ;
#35790=AXIS2_PLACEMENT_3D('',#78008,#44496,#44497) ;
#35791=AXIS2_PLACEMENT_3D('',#78010,#44499,#44500) ;
#35792=AXIS2_PLACEMENT_3D('',#78014,#44503,#44504) ;
#35793=AXIS2_PLACEMENT_3D('',#78017,#44506,#44507) ;
#35794=AXIS2_PLACEMENT_3D('',#78018,#44508,#44509) ;
#35795=AXIS2_PLACEMENT_3D('',#78023,#44513,#44514) ;
#35796=AXIS2_PLACEMENT_3D('',#78026,#44515,#44516) ;
#35797=AXIS2_PLACEMENT_3D('',#78030,#44518,#44519) ;
#35798=AXIS2_PLACEMENT_3D('',#78049,#44521,#44522) ;
#35799=AXIS2_PLACEMENT_3D('',#78050,#44523,#44524) ;
#35800=AXIS2_PLACEMENT_3D('',#78076,#44525,#44526) ;
#35801=AXIS2_PLACEMENT_3D('',#78078,#44527,#44528) ;
#35802=AXIS2_PLACEMENT_3D('',#78079,#44529,#44530) ;
#35803=AXIS2_PLACEMENT_3D('',#78080,#44531,#44532) ;
#35804=AXIS2_PLACEMENT_3D('',#78081,#44533,#44534) ;
#35805=AXIS2_PLACEMENT_3D('',#78083,#44535,#44536) ;
#35806=AXIS2_PLACEMENT_3D('',#78085,#44538,#44539) ;
#35807=AXIS2_PLACEMENT_3D('',#78087,#44540,#44541) ;
#35808=AXIS2_PLACEMENT_3D('',#78088,#44542,#44543) ;
#35809=AXIS2_PLACEMENT_3D('',#78089,#44544,#44545) ;
#35810=AXIS2_PLACEMENT_3D('',#78090,#44546,#44547) ;
#35811=AXIS2_PLACEMENT_3D('',#78091,#44548,#44549) ;
#35812=AXIS2_PLACEMENT_3D('',#78094,#44552,#44553) ;
#35813=AXIS2_PLACEMENT_3D('',#78097,#44555,#44556) ;
#35814=AXIS2_PLACEMENT_3D('',#78099,#44558,#44559) ;
#35815=AXIS2_PLACEMENT_3D('',#78103,#44562,#44563) ;
#35816=AXIS2_PLACEMENT_3D('',#78104,#44564,#44565) ;
#35817=AXIS2_PLACEMENT_3D('',#78105,#44566,#44567) ;
#35818=AXIS2_PLACEMENT_3D('',#78106,#44568,#44569) ;
#35819=AXIS2_PLACEMENT_3D('',#78107,#44570,#44571) ;
#35820=AXIS2_PLACEMENT_3D('',#78124,#44572,#44573) ;
#35821=AXIS2_PLACEMENT_3D('',#78125,#44574,#44575) ;
#35822=AXIS2_PLACEMENT_3D('',#78126,#44576,#44577) ;
#35823=AXIS2_PLACEMENT_3D('',#78127,#44578,#44579) ;
#35824=AXIS2_PLACEMENT_3D('',#78153,#44580,#44581) ;
#35825=AXIS2_PLACEMENT_3D('',#78154,#44582,#44583) ;
#35826=AXIS2_PLACEMENT_3D('',#78155,#44584,#44585) ;
#35827=AXIS2_PLACEMENT_3D('',#78157,#44586,#44587) ;
#35828=AXIS2_PLACEMENT_3D('',#78159,#44589,#44590) ;
#35829=AXIS2_PLACEMENT_3D('',#78161,#44591,#44592) ;
#35830=AXIS2_PLACEMENT_3D('',#78162,#44593,#44594) ;
#35831=AXIS2_PLACEMENT_3D('',#78163,#44595,#44596) ;
#35832=AXIS2_PLACEMENT_3D('',#78165,#44597,#44598) ;
#35833=AXIS2_PLACEMENT_3D('',#78167,#44599,#44600) ;
#35834=AXIS2_PLACEMENT_3D('',#78185,#44602,#44603) ;
#35835=AXIS2_PLACEMENT_3D('',#78186,#44604,#44605) ;
#35836=AXIS2_PLACEMENT_3D('',#78187,#44606,#44607) ;
#35837=AXIS2_PLACEMENT_3D('',#78188,#44608,#44609) ;
#35838=AXIS2_PLACEMENT_3D('',#78189,#44610,#44611) ;
#35839=AXIS2_PLACEMENT_3D('',#78190,#44612,#44613) ;
#35840=AXIS2_PLACEMENT_3D('',#78192,#44614,#44615) ;
#35841=AXIS2_PLACEMENT_3D('',#78194,#44616,#44617) ;
#35842=AXIS2_PLACEMENT_3D('',#78195,#44618,#44619) ;
#35843=AXIS2_PLACEMENT_3D('',#78196,#44620,#44621) ;
#35844=AXIS2_PLACEMENT_3D('',#78204,#44623,#44624) ;
#35845=AXIS2_PLACEMENT_3D('',#78210,#44628,#44629) ;
#35846=AXIS2_PLACEMENT_3D('',#78211,#44630,#44631) ;
#35847=AXIS2_PLACEMENT_3D('',#78212,#44632,#44633) ;
#35848=AXIS2_PLACEMENT_3D('',#78213,#44634,#44635) ;
#35849=AXIS2_PLACEMENT_3D('',#78214,#44636,#44637) ;
#35850=AXIS2_PLACEMENT_3D('',#78215,#44638,#44639) ;
#35851=AXIS2_PLACEMENT_3D('',#78233,#44640,#44641) ;
#35852=AXIS2_PLACEMENT_3D('',#78234,#44642,#44643) ;
#35853=AXIS2_PLACEMENT_3D('',#78235,#44644,#44645) ;
#35854=AXIS2_PLACEMENT_3D('',#78237,#44647,#44648) ;
#35855=AXIS2_PLACEMENT_3D('',#78239,#44650,#44651) ;
#35856=AXIS2_PLACEMENT_3D('',#78240,#44652,#44653) ;
#35857=AXIS2_PLACEMENT_3D('',#78241,#44654,#44655) ;
#35858=AXIS2_PLACEMENT_3D('',#78242,#44656,#44657) ;
#35859=AXIS2_PLACEMENT_3D('',#78243,#44658,#44659) ;
#35860=AXIS2_PLACEMENT_3D('',#78244,#44660,#44661) ;
#35861=AXIS2_PLACEMENT_3D('',#78245,#44662,#44663) ;
#35862=AXIS2_PLACEMENT_3D('',#78246,#44664,#44665) ;
#35863=AXIS2_PLACEMENT_3D('',#78247,#44666,#44667) ;
#35864=AXIS2_PLACEMENT_3D('',#78248,#44668,#44669) ;
#35865=AXIS2_PLACEMENT_3D('',#78249,#44670,#44671) ;
#35866=AXIS2_PLACEMENT_3D('',#78250,#44672,#44673) ;
#35867=AXIS2_PLACEMENT_3D('',#78251,#44674,#44675) ;
#35868=AXIS2_PLACEMENT_3D('',#78252,#44676,#44677) ;
#35869=AXIS2_PLACEMENT_3D('',#78254,#44678,#44679) ;
#35870=AXIS2_PLACEMENT_3D('',#78255,#44680,#44681) ;
#35871=AXIS2_PLACEMENT_3D('',#78284,#44682,#44683) ;
#35872=AXIS2_PLACEMENT_3D('',#78285,#44684,#44685) ;
#35873=AXIS2_PLACEMENT_3D('',#78286,#44686,#44687) ;
#35874=AXIS2_PLACEMENT_3D('',#78287,#44688,#44689) ;
#35875=AXIS2_PLACEMENT_3D('',#78288,#44690,#44691) ;
#35876=AXIS2_PLACEMENT_3D('',#78289,#44692,#44693) ;
#35877=AXIS2_PLACEMENT_3D('',#78292,#44695,#44696) ;
#35878=AXIS2_PLACEMENT_3D('',#78321,#44697,#44698) ;
#35879=AXIS2_PLACEMENT_3D('',#78322,#44699,#44700) ;
#35880=AXIS2_PLACEMENT_3D('',#78323,#44701,#44702) ;
#35881=AXIS2_PLACEMENT_3D('',#78324,#44703,#44704) ;
#35882=AXIS2_PLACEMENT_3D('',#78325,#44705,#44706) ;
#35883=AXIS2_PLACEMENT_3D('',#78357,#44707,#44708) ;
#35884=AXIS2_PLACEMENT_3D('',#78374,#44709,#44710) ;
#35885=AXIS2_PLACEMENT_3D('',#78375,#44711,#44712) ;
#35886=AXIS2_PLACEMENT_3D('',#78376,#44713,#44714) ;
#35887=AXIS2_PLACEMENT_3D('',#78377,#44715,#44716) ;
#35888=AXIS2_PLACEMENT_3D('',#78378,#44717,#44718) ;
#35889=AXIS2_PLACEMENT_3D('',#78379,#44719,#44720) ;
#35890=AXIS2_PLACEMENT_3D('',#78411,#44721,#44722) ;
#35891=AXIS2_PLACEMENT_3D('',#78428,#44723,#44724) ;
#35892=AXIS2_PLACEMENT_3D('',#78430,#44726,#44727) ;
#35893=AXIS2_PLACEMENT_3D('',#78431,#44728,#44729) ;
#35894=AXIS2_PLACEMENT_3D('',#78432,#44730,#44731) ;
#35895=AXIS2_PLACEMENT_3D('',#78433,#44732,#44733) ;
#35896=AXIS2_PLACEMENT_3D('',#78434,#44734,#44735) ;
#35897=AXIS2_PLACEMENT_3D('',#78435,#44736,#44737) ;
#35898=AXIS2_PLACEMENT_3D('',#78459,#44739,#44740) ;
#35899=AXIS2_PLACEMENT_3D('',#78484,#44741,#44742) ;
#35900=AXIS2_PLACEMENT_3D('',#78485,#44743,#44744) ;
#35901=AXIS2_PLACEMENT_3D('',#78486,#44745,#44746) ;
#43757=DIRECTION('axis',(0.,0.,1.)) ;
#43758=DIRECTION('refdir',(1.,0.,0.)) ;
#43759=DIRECTION('center_axis',(-1.05010212975467E-14,-2.51767111096099E-14,
-1.)) ;
#43760=DIRECTION('ref_axis',(-2.51083656231336E-15,1.,-2.51767111096099E-14)) ;
#43761=DIRECTION('',(1.05010212975467E-14,2.51767111096099E-14,1.)) ;
#43762=DIRECTION('center_axis',(-1.05010212975467E-14,-2.51767111096099E-14,
-1.)) ;
#43763=DIRECTION('ref_axis',(-2.51083656231336E-15,1.,-2.51767111096099E-14)) ;
#43764=DIRECTION('',(1.05010212975467E-14,2.51767111096099E-14,1.)) ;
#43765=DIRECTION('center_axis',(-1.05010212975467E-14,-2.51767111096099E-14,
-1.)) ;
#43766=DIRECTION('ref_axis',(-2.51083656231336E-15,1.,-2.51767111096099E-14)) ;
#43767=DIRECTION('',(1.05010212975467E-14,2.51767111096099E-14,1.)) ;
#43768=DIRECTION('center_axis',(-1.05010212975467E-14,-2.51767111096099E-14,
-1.)) ;
#43769=DIRECTION('ref_axis',(-2.51083656231336E-15,1.,-2.51767111096099E-14)) ;
#43770=DIRECTION('',(1.05010212975467E-14,2.51767111096099E-14,1.)) ;
#43771=DIRECTION('center_axis',(-1.05010212975467E-14,-2.51767111096099E-14,
-1.)) ;
#43772=DIRECTION('ref_axis',(-2.51083656231336E-15,1.,-2.51767111096099E-14)) ;
#43773=DIRECTION('',(1.05010212975467E-14,2.51767111096099E-14,1.)) ;
#43774=DIRECTION('center_axis',(-1.05010212975467E-14,-2.51767111096099E-14,
-1.)) ;
#43775=DIRECTION('ref_axis',(-2.51083656231336E-15,1.,-2.51767111096099E-14)) ;
#43776=DIRECTION('',(1.05010212975467E-14,2.51767111096099E-14,1.)) ;
#43777=DIRECTION('center_axis',(-1.05010212975467E-14,-2.51767111096099E-14,
-1.)) ;
#43778=DIRECTION('ref_axis',(-2.51083656231336E-15,1.,-2.51767111096099E-14)) ;
#43779=DIRECTION('',(1.05010212975467E-14,2.51767111096099E-14,1.)) ;
#43780=DIRECTION('center_axis',(-1.05010212975467E-14,-2.51767111096099E-14,
-1.)) ;
#43781=DIRECTION('ref_axis',(-2.51083656231336E-15,1.,-2.51767111096099E-14)) ;
#43782=DIRECTION('',(1.05010212975467E-14,2.51767111096099E-14,1.)) ;
#43783=DIRECTION('center_axis',(-2.0775199119216E-14,2.60214901359506E-13,
-1.)) ;
#43784=DIRECTION('ref_axis',(-0.15733882491533,-0.987544679583796,-2.53705095969203E-13)) ;
#43785=DIRECTION('center_axis',(0.,0.,1.)) ;
#43786=DIRECTION('ref_axis',(1.,0.,0.)) ;
#43787=DIRECTION('',(0.,0.,-1.)) ;
#43788=DIRECTION('center_axis',(0.,0.,1.)) ;
#43789=DIRECTION('ref_axis',(1.,0.,0.)) ;
#43790=DIRECTION('center_axis',(0.,0.,1.)) ;
#43791=DIRECTION('ref_axis',(1.,0.,0.)) ;
#43792=DIRECTION('',(0.,0.,-1.)) ;
#43793=DIRECTION('center_axis',(0.,0.,1.)) ;
#43794=DIRECTION('ref_axis',(1.,0.,0.)) ;
#43795=DIRECTION('',(0.,0.,-1.)) ;
#43796=DIRECTION('center_axis',(0.,0.,1.)) ;
#43797=DIRECTION('ref_axis',(1.,0.,0.)) ;
#43798=DIRECTION('',(0.,0.,-1.)) ;
#43799=DIRECTION('center_axis',(0.,0.,1.)) ;
#43800=DIRECTION('ref_axis',(1.,0.,0.)) ;
#43801=DIRECTION('',(0.,0.,-1.)) ;
#43802=DIRECTION('center_axis',(0.,0.,1.)) ;
#43803=DIRECTION('ref_axis',(1.,0.,0.)) ;
#43804=DIRECTION('',(0.,0.,-1.)) ;
#43805=DIRECTION('center_axis',(0.,0.,1.)) ;
#43806=DIRECTION('ref_axis',(1.,0.,0.)) ;
#43807=DIRECTION('',(0.,0.,-1.)) ;
#43808=DIRECTION('center_axis',(0.,0.,1.)) ;
#43809=DIRECTION('ref_axis',(1.,0.,0.)) ;
#43810=DIRECTION('center_axis',(0.,0.,1.)) ;
#43811=DIRECTION('ref_axis',(0.38268343236509,0.923879532511287,0.)) ;
#43812=DIRECTION('center_axis',(-1.05010212975467E-14,-2.51767111096099E-14,
-1.)) ;
#43813=DIRECTION('ref_axis',(-2.51083656231336E-15,1.,-2.51767111096099E-14)) ;
#43814=DIRECTION('center_axis',(-2.0775199119216E-14,2.60214901359506E-13,
-1.)) ;
#43815=DIRECTION('ref_axis',(-0.15733882491533,-0.987544679583796,-2.53705095969203E-13)) ;
#43816=DIRECTION('center_axis',(0.431213875666469,0.456273348170848,0.778376017861333)) ;
#43817=DIRECTION('ref_axis',(0.726783280612686,-0.686866845190436,6.1949686306476E-16)) ;
#43818=DIRECTION('center_axis',(0.78416251235965,0.382514104091566,0.488643136021401)) ;
#43819=DIRECTION('ref_axis',(0.438419748448915,-0.898770340059122,1.79364045353587E-16)) ;
#43820=DIRECTION('center_axis',(0.998769717110461,5.59307539516625E-11,
0.0495888312333447)) ;
#43821=DIRECTION('ref_axis',(5.59996493620929E-11,-1.,1.83348176602366E-27)) ;
#43822=DIRECTION('center_axis',(1.,0.,-2.77555756156289E-14)) ;
#43823=DIRECTION('ref_axis',(0.,-1.,0.)) ;
#43824=DIRECTION('center_axis',(-0.186904608536419,-0.982127159191521,0.0222015874711655)) ;
#43825=DIRECTION('ref_axis',(0.982190610687812,-0.187262695295954,-0.0153064439762371)) ;
#43826=DIRECTION('center_axis',(0.,1.,0.)) ;
#43827=DIRECTION('ref_axis',(0.999909707661035,0.,0.0134378765146677)) ;
#43828=DIRECTION('center_axis',(-1.,-1.11022302462516E-14,1.80671994062472E-14)) ;
#43829=DIRECTION('ref_axis',(-5.55111512312583E-15,-0.685234561324452,-0.728322453290084)) ;
#43830=DIRECTION('',(0.999999958174326,2.12460885215939E-8,-0.00028922542396849)) ;
#43831=DIRECTION('center_axis',(-1.,0.,-6.17096200035076E-15)) ;
#43832=DIRECTION('ref_axis',(5.5511151231258E-15,-0.436809046170809,-0.899554254719163)) ;
#43833=DIRECTION('',(1.,0.,0.)) ;
#43834=DIRECTION('',(1.,0.,0.)) ;
#43835=DIRECTION('center_axis',(-0.202274762387573,0.9793288112279,0.)) ;
#43836=DIRECTION('ref_axis',(-0.81902520534733,-0.169164969825963,0.548252611475353)) ;
#43837=DIRECTION('center_axis',(-0.796046528300715,-0.164065815817298,0.582573886181473)) ;
#43838=DIRECTION('ref_axis',(0.60325914550266,-0.292808781282497,0.741849998969643)) ;
#43839=DIRECTION('center_axis',(0.,4.79371819681639E-16,1.)) ;
#43840=DIRECTION('ref_axis',(0.,-1.,5.18039323243001E-16)) ;
#43841=DIRECTION('center_axis',(0.,4.79371819681639E-16,1.)) ;
#43842=DIRECTION('ref_axis',(0.,-1.,4.79371819681639E-16)) ;
#43843=DIRECTION('center_axis',(0.79604652830067,0.164065815817297,0.582573886181535)) ;
#43844=DIRECTION('ref_axis',(0.603259145417311,-0.292808782928713,-0.741849998389284)) ;
#43845=DIRECTION('center_axis',(0.,2.3968590984082E-16,1.)) ;
#43846=DIRECTION('ref_axis',(1.,2.46314898699588E-16,-5.90382106021602E-32)) ;
#43847=DIRECTION('center_axis',(0.796046712982956,-0.164065889510482,0.582573613072345)) ;
#43848=DIRECTION('ref_axis',(0.600011337901856,0.340121293701446,-0.724088323314276)) ;
#43849=DIRECTION('center_axis',(0.,4.79371819681639E-16,1.)) ;
#43850=DIRECTION('ref_axis',(0.,-1.,4.79371819681639E-16)) ;
#43851=DIRECTION('center_axis',(0.,2.3968590984082E-16,1.)) ;
#43852=DIRECTION('ref_axis',(-1.,-1.39827749563623E-16,3.35147413751513E-32)) ;
#43853=DIRECTION('center_axis',(-0.796046712982948,0.164065889510474,0.582573613072357)) ;
#43854=DIRECTION('ref_axis',(0.60001133781454,0.340121294720491,0.724088322907961)) ;
#43855=DIRECTION('center_axis',(0.,4.79371819681639E-16,1.)) ;
#43856=DIRECTION('ref_axis',(0.,-1.,4.79371819681639E-16)) ;
#43857=DIRECTION('center_axis',(-1.,-1.22464679914735E-16,5.87061164574561E-32)) ;
#43858=DIRECTION('ref_axis',(-1.22464679914735E-16,1.,-3.23774577026876E-16)) ;
#43859=DIRECTION('center_axis',(0.,4.79371819681639E-16,1.)) ;
#43860=DIRECTION('ref_axis',(0.,-1.,4.79371819681639E-16)) ;
#43861=DIRECTION('center_axis',(0.,2.3968590984082E-16,1.)) ;
#43862=DIRECTION('ref_axis',(-1.,-9.00424887691599E-15,0.)) ;
#43863=DIRECTION('center_axis',(0.,0.,-1.)) ;
#43864=DIRECTION('ref_axis',(-1.,-1.22464679914735E-16,0.)) ;
#43865=DIRECTION('center_axis',(-0.186904608537131,0.982127159190804,0.0222015874969168)) ;
#43866=DIRECTION('ref_axis',(0.982190613229004,0.187262692788182,-0.0153063115920336)) ;
#43867=DIRECTION('center_axis',(0.202274762386253,0.979328811228172,-1.88126629740374E-12)) ;
#43868=DIRECTION('ref_axis',(-0.81902520534735,0.16916496982587,0.548252611475352)) ;
#43869=DIRECTION('center_axis',(0.431213875666332,-0.45627334817079,0.778376017861444)) ;
#43870=DIRECTION('ref_axis',(0.813949131457667,-0.175495689147709,-0.553794252850172)) ;
#43871=DIRECTION('center_axis',(0.784162512362696,-0.38251410408934,0.488643136018255)) ;
#43872=DIRECTION('ref_axis',(0.490111180257792,-0.101229659940977,-0.865761853476201)) ;
#43873=DIRECTION('center_axis',(0.998769717110462,-5.59307539516625E-11,
0.0495888312333392)) ;
#43874=DIRECTION('ref_axis',(0.0495862470879903,-0.0102088265337294,-0.998717669794889)) ;
#43875=DIRECTION('center_axis',(1.,-5.55111512312579E-15,1.65423230669149E-12)) ;
#43876=DIRECTION('ref_axis',(1.65423230669148E-12,-1.57374113740616E-12,
-1.)) ;
#43877=DIRECTION('center_axis',(0.,-1.,0.)) ;
#43878=DIRECTION('ref_axis',(0.999909707872585,0.,0.0134378607732635)) ;
#43879=DIRECTION('',(-0.99999997985201,1.21446614212548E-8,0.000200738584200413)) ;
#43880=DIRECTION('center_axis',(-1.,-5.55111512312572E-15,7.09951135811084E-14)) ;
#43881=DIRECTION('ref_axis',(-5.55111512312572E-15,1.,-7.52353615125298E-45)) ;
#43882=DIRECTION('',(-1.,0.,0.)) ;
#43883=DIRECTION('center_axis',(-1.,0.,-6.17096200035069E-15)) ;
#43884=DIRECTION('ref_axis',(0.,1.,0.)) ;
#43885=DIRECTION('',(-1.,0.,0.)) ;
#43886=DIRECTION('center_axis',(0.,0.,1.)) ;
#43887=DIRECTION('ref_axis',(-0.793390388649525,-0.608713143605883,0.)) ;
#43888=DIRECTION('',(0.,0.,1.)) ;
#43889=DIRECTION('center_axis',(0.,0.,-1.)) ;
#43890=DIRECTION('ref_axis',(0.,-1.,0.)) ;
#43891=DIRECTION('',(0.,0.,-1.)) ;
#43892=DIRECTION('center_axis',(0.,-1.,0.)) ;
#43893=DIRECTION('ref_axis',(0.,0.,-1.)) ;
#43894=DIRECTION('',(-1.,0.,0.)) ;
#43895=DIRECTION('',(0.0942752822069817,0.,-0.995546167269401)) ;
#43896=DIRECTION('center_axis',(0.,1.,0.)) ;
#43897=DIRECTION('ref_axis',(-0.371772155637639,0.,0.928324008249568)) ;
#43898=DIRECTION('center_axis',(-0.431213875666459,-0.456273348170838,0.778376017861345)) ;
#43899=DIRECTION('ref_axis',(-0.726783280612687,0.686866845190435,-1.43341183094753E-17)) ;
#43900=DIRECTION('center_axis',(-0.784162512359631,-0.38251410409158,0.48864313602142)) ;
#43901=DIRECTION('ref_axis',(-0.438419748448937,0.898770340059111,-2.46822861618048E-16)) ;
#43902=DIRECTION('center_axis',(-0.998769717110462,-5.59362982373437E-11,
0.0495888312333393)) ;
#43903=DIRECTION('ref_axis',(-5.6005200477216E-11,1.,-3.39348476170366E-27)) ;
#43904=DIRECTION('center_axis',(-1.,2.22044604925031E-14,-1.11022302462516E-14)) ;
#43905=DIRECTION('ref_axis',(2.22044604925031E-14,1.,1.68155815718967E-44)) ;
#43906=DIRECTION('center_axis',(0.186904608536329,0.982127159191646,0.0222015874663972)) ;
#43907=DIRECTION('ref_axis',(0.982190613371512,-0.187262692646365,0.0153063041824444)) ;
#43908=DIRECTION('center_axis',(5.36677285303109E-14,-1.,2.16337548812628E-12)) ;
#43909=DIRECTION('ref_axis',(0.999909707696494,2.45917157912175E-14,-0.0134378738761801)) ;
#43910=DIRECTION('center_axis',(1.,-1.11022302462516E-14,-1.04454171887006E-14)) ;
#43911=DIRECTION('ref_axis',(1.27702679854493E-29,0.685234561324431,-0.728322453290103)) ;
#43912=DIRECTION('',(-0.999999978906491,-1.27145189198587E-8,-0.000205394783225332)) ;
#43913=DIRECTION('center_axis',(1.,0.,-1.85128860010521E-14)) ;
#43914=DIRECTION('ref_axis',(-1.66533453693773E-14,0.436809046170802,-0.899554254719166)) ;
#43915=DIRECTION('',(-1.,0.,0.)) ;
#43916=DIRECTION('',(-1.,-2.86503102337282E-14,0.)) ;
#43917=DIRECTION('center_axis',(0.202274762387575,-0.979328811227899,0.)) ;
#43918=DIRECTION('ref_axis',(0.81902520534733,0.169164969825965,0.548252611475353)) ;
#43919=DIRECTION('center_axis',(0.,2.3968590984082E-16,1.)) ;
#43920=DIRECTION('ref_axis',(1.,0.,0.)) ;
#43921=DIRECTION('center_axis',(0.,0.,-1.)) ;
#43922=DIRECTION('ref_axis',(1.,2.63677968348475E-16,0.)) ;
#43923=DIRECTION('center_axis',(0.186904608537136,-0.982127159191002,0.0222015874881292)) ;
#43924=DIRECTION('ref_axis',(0.982190613046714,0.187262692968013,0.0153063210892889)) ;
#43925=DIRECTION('center_axis',(-0.202274762386252,-0.979328811228172,-1.87854811391648E-12)) ;
#43926=DIRECTION('ref_axis',(0.819025205347352,-0.169164969825868,0.54825261147535)) ;
#43927=DIRECTION('center_axis',(-0.431213875666327,0.45627334817079,0.778376017861446)) ;
#43928=DIRECTION('ref_axis',(-0.813949131457668,0.175495689147714,-0.553794252850169)) ;
#43929=DIRECTION('center_axis',(-0.784162512362691,0.382514104089345,0.488643136018258)) ;
#43930=DIRECTION('ref_axis',(-0.490111180257797,0.101229659940977,-0.865761853476199)) ;
#43931=DIRECTION('center_axis',(-0.998769717110461,5.59418425230248E-11,
0.0495888312333449)) ;
#43932=DIRECTION('ref_axis',(-0.0495862470879959,0.0102088265337349,-0.998717669794889)) ;
#43933=DIRECTION('center_axis',(-1.,-5.55111512312579E-15,1.64313007644522E-12)) ;
#43934=DIRECTION('ref_axis',(-1.64313007644523E-12,1.5709655798446E-12,
-1.)) ;
#43935=DIRECTION('center_axis',(0.,1.,0.)) ;
#43936=DIRECTION('ref_axis',(0.999909707872585,0.,-0.0134378607732635)) ;
#43937=DIRECTION('',(0.999999978565477,-1.29200364901908E-8,0.000207048412283444)) ;
#43938=DIRECTION('center_axis',(1.,1.11022302462514E-14,6.57724049867568E-14)) ;
#43939=DIRECTION('ref_axis',(1.11022302462514E-14,-1.,1.17986696570242E-44)) ;
#43940=DIRECTION('',(1.,0.,0.)) ;
#43941=DIRECTION('center_axis',(1.,0.,-1.23419240007014E-14)) ;
#43942=DIRECTION('ref_axis',(0.,-1.,0.)) ;
#43943=DIRECTION('',(1.,0.,0.)) ;
#43944=DIRECTION('center_axis',(0.,0.,-1.)) ;
#43945=DIRECTION('ref_axis',(0.793390388649528,0.608713143605879,0.)) ;
#43946=DIRECTION('',(0.,0.,1.)) ;
#43947=DIRECTION('center_axis',(0.,0.,1.)) ;
#43948=DIRECTION('ref_axis',(0.965894315163092,-0.258936617602883,0.)) ;
#43949=DIRECTION('',(0.,0.,-1.)) ;
#43950=DIRECTION('center_axis',(0.,-1.,0.)) ;
#43951=DIRECTION('ref_axis',(0.,0.,-1.)) ;
#43952=DIRECTION('',(1.,0.,0.)) ;
#43953=DIRECTION('',(-0.0942752822069811,0.,-0.995546167269401)) ;
#43954=DIRECTION('center_axis',(0.,-1.,0.)) ;
#43955=DIRECTION('ref_axis',(0.371772155637639,0.,0.928324008249568)) ;
#43956=DIRECTION('center_axis',(0.,-1.,0.)) ;
#43957=DIRECTION('ref_axis',(0.525950052779709,0.,-0.850515456638515)) ;
#43958=DIRECTION('center_axis',(-0.087142648404439,0.0173337504938603,-0.996045029063886)) ;
#43959=DIRECTION('ref_axis',(-0.996194698091746,2.77416503886704E-15,0.0871557427476577)) ;
#43960=DIRECTION('center_axis',(0.0140688745303331,0.999901028487045,-1.40716591575854E-15)) ;
#43961=DIRECTION('ref_axis',(0.999901028487045,-0.0140688745303331,-6.81169755687964E-34)) ;
#43962=DIRECTION('center_axis',(-0.369647612382762,-0.929172019950947,3.84741834623491E-16)) ;
#43963=DIRECTION('ref_axis',(0.929172019950947,-0.369647612382762,4.43338045572624E-34)) ;
#43964=DIRECTION('center_axis',(0.0871426484044392,-0.0173337504938598,
0.996045029063886)) ;
#43965=DIRECTION('ref_axis',(-0.976906303124667,0.194318745462638,0.0888498738160223)) ;
#43966=DIRECTION('',(0.0871426484044392,-0.0173337504938598,0.996045029063886)) ;
#43967=DIRECTION('center_axis',(-0.0871426484044391,0.0173337504938307,
-0.996045029063886)) ;
#43968=DIRECTION('ref_axis',(-0.996194698091746,2.77283728287811E-15,0.0871557427476578)) ;
#43969=DIRECTION('',(-0.0871426484044392,0.0173337504938598,-0.996045029063886)) ;
#43970=DIRECTION('center_axis',(0.,0.,1.)) ;
#43971=DIRECTION('ref_axis',(-0.686061634431369,-0.727543423969566,0.)) ;
#43972=DIRECTION('center_axis',(0.0198801512493583,0.973637907857952,0.227231168566933)) ;
#43973=DIRECTION('ref_axis',(0.0848581350266343,-0.228099154715644,0.969932921669231)) ;
#43974=DIRECTION('center_axis',(-0.390791367470215,-0.90489803427529,-0.168646537691927)) ;
#43975=DIRECTION('ref_axis',(0.0145744118599508,-0.189275895687504,0.981815777949524)) ;
#43976=DIRECTION('center_axis',(-0.996194698091746,3.51997520523845E-15,
0.0871557427476579)) ;
#43977=DIRECTION('ref_axis',(0.0871557427476578,-2.56289665819841E-31,0.996194698091746)) ;
#43978=DIRECTION('center_axis',(0.996194698091746,-3.51997520523845E-15,
-0.0871557427476579)) ;
#43979=DIRECTION('ref_axis',(0.082689266929588,-0.316018771704214,0.945142645882201)) ;
#43980=DIRECTION('center_axis',(-0.996194698091746,3.51997520523845E-15,
0.0871557427476579)) ;
#43981=DIRECTION('ref_axis',(0.082689266929588,-0.316018771704214,0.945142645882201)) ;
#43982=DIRECTION('center_axis',(-0.996194698091746,3.51997520523845E-15,
0.0871557427476579)) ;
#43983=DIRECTION('ref_axis',(0.0871557427476579,3.7050998642496E-32,0.996194698091746)) ;
#43984=DIRECTION('',(3.53342093867907E-15,1.,0.)) ;
#43985=DIRECTION('center_axis',(-0.996194698091748,-6.11235790402882E-14,
0.0871557427476263)) ;
#43986=DIRECTION('ref_axis',(0.0827617664630686,-0.31351037143038,0.945971319341923)) ;
#43987=DIRECTION('center_axis',(3.53342093867907E-15,1.,0.)) ;
#43988=DIRECTION('ref_axis',(0.675590207615657,-2.3871445855557E-15,-0.737277336810127)) ;
#43989=DIRECTION('',(-3.53342093867907E-15,-1.,0.)) ;
#43990=DIRECTION('center_axis',(3.53342093867907E-15,1.,0.)) ;
#43991=DIRECTION('ref_axis',(0.675590207615657,-2.3871445855557E-15,-0.737277336810127)) ;
#43992=DIRECTION('center_axis',(-0.0796183978310997,0.406796813220287,-0.910042451471704)) ;
#43993=DIRECTION('ref_axis',(0.996194698091747,-1.11289992857909E-14,-0.0871557427476466)) ;
#43994=DIRECTION('center_axis',(-0.0844345745997023,0.247929423057006,-0.965091603836023)) ;
#43995=DIRECTION('ref_axis',(0.996194698091746,-5.54415204842811E-15,-0.0871557427476577)) ;
#43996=DIRECTION('center_axis',(0.969995299381892,-0.171397325086558,-0.17242991657542)) ;
#43997=DIRECTION('ref_axis',(-0.130771520122756,0.230075936076955,-0.96434634502501)) ;
#43998=DIRECTION('center_axis',(-0.0844006560103685,0.249445165551562,-0.964703912424933)) ;
#43999=DIRECTION('ref_axis',(0.996194698090483,-8.3278891326026E-15,-0.0871557427620906)) ;
#44000=DIRECTION('center_axis',(-0.307221196694479,-0.877837780004883,0.367445190875743)) ;
#44001=DIRECTION('ref_axis',(0.563077209994445,-0.478958069141859,-0.673456177927542)) ;
#44002=DIRECTION('center_axis',(-0.991017446008435,-0.133732650115511,0.)) ;
#44003=DIRECTION('ref_axis',(-0.133732650115511,0.991017446008435,0.)) ;
#44004=DIRECTION('center_axis',(0.307221196683632,-0.877837780010281,0.367445190871915)) ;
#44005=DIRECTION('ref_axis',(-0.563077209989657,-0.478958069131965,-0.673456177938582)) ;
#44006=DIRECTION('center_axis',(-0.0844006559966543,-0.249445165539995,
0.964703912429124)) ;
#44007=DIRECTION('ref_axis',(-0.996194698091746,2.76022795169697E-15,-0.0871557427476577)) ;
#44008=DIRECTION('center_axis',(0.991017446008434,-0.13373265011552,0.)) ;
#44009=DIRECTION('ref_axis',(0.13373265011552,0.991017446008434,0.)) ;
#44010=DIRECTION('center_axis',(6.61271392193231E-15,1.,0.)) ;
#44011=DIRECTION('ref_axis',(-0.675590207615657,4.46748477142119E-15,-0.737277336810127)) ;
#44012=DIRECTION('center_axis',(-0.0844345745997158,-0.247929423057003,
0.965091603836023)) ;
#44013=DIRECTION('ref_axis',(-0.996194698091745,5.56571981562619E-15,-0.0871557427476687)) ;
#44014=DIRECTION('center_axis',(-0.0796183978311047,-0.406796813220276,
0.910042451471708)) ;
#44015=DIRECTION('ref_axis',(-0.996194698091747,1.23978847396904E-17,-0.0871557427476467)) ;
#44016=DIRECTION('center_axis',(-0.969995299381675,-0.171397325087362,-0.172429916575841)) ;
#44017=DIRECTION('ref_axis',(0.130771521154601,0.23007593125536,-0.964346346035433)) ;
#44018=DIRECTION('center_axis',(0.99619469809175,-1.09010204657839E-13,
0.0871557427476121)) ;
#44019=DIRECTION('ref_axis',(0.0827617664618814,0.31351037147169,-0.945971319328336)) ;
#44020=DIRECTION('center_axis',(0.996194698091746,-6.58755054902644E-15,
0.0871557427476584)) ;
#44021=DIRECTION('ref_axis',(0.0871557427476584,-3.66128094028344E-32,-0.996194698091746)) ;
#44022=DIRECTION('center_axis',(-0.996194698091746,6.58755054902644E-15,
-0.0871557427476584)) ;
#44023=DIRECTION('ref_axis',(-0.0826892669295917,-0.316018771704213,0.945142645882201)) ;
#44024=DIRECTION('center_axis',(-0.0198801512493482,0.973637907857952,0.22723116856693)) ;
#44025=DIRECTION('ref_axis',(-0.0848581350266373,-0.22809915471564,0.969932921669232)) ;
#44026=DIRECTION('center_axis',(0.996194698091746,-6.58755054902644E-15,
0.0871557427476584)) ;
#44027=DIRECTION('ref_axis',(-0.0826892669295917,-0.316018771704213,0.945142645882201)) ;
#44028=DIRECTION('center_axis',(0.996194698091746,-6.58755054902644E-15,
0.0871557427476584)) ;
#44029=DIRECTION('ref_axis',(0.0871557427476584,-3.34096417774836E-32,-0.996194698091746)) ;
#44030=DIRECTION('',(-6.61271392193231E-15,-1.,0.)) ;
#44031=DIRECTION('',(0.0871426484044398,0.0173337504938583,-0.996045029063886)) ;
#44032=DIRECTION('center_axis',(-6.61271392193231E-15,-1.,0.)) ;
#44033=DIRECTION('ref_axis',(-0.675590207615657,4.46748477142119E-15,-0.737277336810127)) ;
#44034=DIRECTION('',(6.61271392193231E-15,1.,0.)) ;
#44035=DIRECTION('center_axis',(0.369647612382746,-0.929172019950953,2.5649455641565E-16)) ;
#44036=DIRECTION('ref_axis',(-0.929172019950953,-0.369647612382746,4.94162803730509E-33)) ;
#44037=DIRECTION('center_axis',(0.0871426484044391,0.0173337504938598,-0.996045029063886)) ;
#44038=DIRECTION('ref_axis',(0.92036389196323,0.381227206369641,0.0871557427476579)) ;
#44039=DIRECTION('center_axis',(-0.0140688745303202,0.999901028487045,1.39740367298719E-15)) ;
#44040=DIRECTION('ref_axis',(-0.999901028487045,-0.0140688745303202,2.97151128565353E-34)) ;
#44041=DIRECTION('center_axis',(-0.0871426484044398,-0.0173337504938583,
0.996045029063886)) ;
#44042=DIRECTION('ref_axis',(0.976906303124669,0.194318745462627,0.0888498738160226)) ;
#44043=DIRECTION('',(-0.0871426484044398,-0.0173337504938583,0.996045029063886)) ;
#44044=DIRECTION('center_axis',(0.0871426484044392,0.0173337504938592,-0.996045029063886)) ;
#44045=DIRECTION('ref_axis',(0.920363891963231,0.381227206369638,0.0871557427476578)) ;
#44046=DIRECTION('center_axis',(0.,0.,1.)) ;
#44047=DIRECTION('ref_axis',(1.,0.,0.)) ;
#44048=DIRECTION('center_axis',(0.390791367470204,-0.904898034275296,-0.168646537691924)) ;
#44049=DIRECTION('ref_axis',(-0.0145744118599547,-0.189275895687501,0.981815777949525)) ;
#44050=DIRECTION('center_axis',(0.92036389196323,0.381227206369639,0.087155742747658)) ;
#44051=DIRECTION('ref_axis',(-0.382683432365075,0.923879532511293,-6.02752148941637E-17)) ;
#44052=DIRECTION('',(0.382683432365075,-0.923879532511293,0.)) ;
#44053=DIRECTION('',(0.0666626913468331,0.066662691346831,-0.995546167269401)) ;
#44054=DIRECTION('center_axis',(0.92036389196323,0.381227206369639,0.087155742747658)) ;
#44055=DIRECTION('ref_axis',(0.391063046541469,-0.897215317273461,-0.205120374608636)) ;
#44056=DIRECTION('',(0.0942752822069809,-5.29059027656374E-18,-0.995546167269401)) ;
#44057=DIRECTION('center_axis',(-0.92036389196323,-0.381227206369639,-0.087155742747658)) ;
#44058=DIRECTION('ref_axis',(-0.0315995086952045,-0.149641293808218,0.988235272714764)) ;
#44059=DIRECTION('center_axis',(0.382683432365075,-0.923879532511293,0.)) ;
#44060=DIRECTION('ref_axis',(-0.62416396518116,-0.258537179522593,-0.737277336810128)) ;
#44061=DIRECTION('',(-0.382683432365075,0.923879532511293,0.)) ;
#44062=DIRECTION('center_axis',(0.884086155524837,-0.467323945041674,-3.24271127339954E-16)) ;
#44063=DIRECTION('ref_axis',(-0.467323945041674,-0.884086155524837,3.63079830694576E-33)) ;
#44064=DIRECTION('center_axis',(-0.307221196683633,-0.877837780010277,-0.367445190871924)) ;
#44065=DIRECTION('ref_axis',(-0.56307720998965,0.478958069131973,-0.673456177938582)) ;
#44066=DIRECTION('center_axis',(-0.0844006559966506,0.249445165540006,0.964703912429121)) ;
#44067=DIRECTION('ref_axis',(-0.129175820564643,0.957249345402581,-0.258819045102521)) ;
#44068=DIRECTION('center_axis',(-1.04325044166935E-14,-1.,0.)) ;
#44069=DIRECTION('ref_axis',(-0.675590207615657,7.04809782482522E-15,-0.737277336810127)) ;
#44070=DIRECTION('center_axis',(0.991017446008437,0.133732650115502,0.)) ;
#44071=DIRECTION('ref_axis',(0.133732650115502,-0.991017446008437,0.)) ;
#44072=DIRECTION('center_axis',(-0.0844345745996896,0.247929423057007,0.965091603836024)) ;
#44073=DIRECTION('ref_axis',(-0.162387929710607,0.952177957199453,-0.25881904510252)) ;
#44074=DIRECTION('center_axis',(-0.969995299381661,0.171397325087379,-0.172429916575904)) ;
#44075=DIRECTION('ref_axis',(-0.130771520584849,0.230075933918614,0.96434634547729)) ;
#44076=DIRECTION('center_axis',(-0.079618397831098,0.406796813220277,0.910042451471708)) ;
#44077=DIRECTION('ref_axis',(-0.15336115832627,0.89707261674463,-0.414416548177999)) ;
#44078=DIRECTION('center_axis',(0.99619469809175,1.08620882498388E-13,0.0871557427476121)) ;
#44079=DIRECTION('ref_axis',(0.0827617664602934,-0.31351037152687,-0.945971319310187)) ;
#44080=DIRECTION('center_axis',(0.,0.,1.)) ;
#44081=DIRECTION('ref_axis',(1.,0.,0.)) ;
#44082=DIRECTION('center_axis',(0.,0.,-1.)) ;
#44083=DIRECTION('ref_axis',(6.99440505513848E-15,1.,0.)) ;
#44084=DIRECTION('center_axis',(0.969995299381302,0.171397325089019,-0.172429916576296)) ;
#44085=DIRECTION('ref_axis',(0.130771520826673,0.230075932788573,0.964346345714104)) ;
#44086=DIRECTION('center_axis',(0.,0.,1.)) ;
#44087=DIRECTION('ref_axis',(7.04419501764363E-15,1.,0.)) ;
#44088=DIRECTION('center_axis',(0.,0.,1.)) ;
#44089=DIRECTION('ref_axis',(1.,0.,0.)) ;
#44090=DIRECTION('center_axis',(0.,0.,1.)) ;
#44091=DIRECTION('ref_axis',(7.21644966006352E-15,1.,0.)) ;
#44092=DIRECTION('center_axis',(0.,0.,1.)) ;
#44093=DIRECTION('ref_axis',(1.,0.,0.)) ;
#44094=DIRECTION('center_axis',(0.,0.,-1.)) ;
#44095=DIRECTION('ref_axis',(7.16665969755837E-15,1.,0.)) ;
#44096=DIRECTION('center_axis',(-0.991017446008435,0.133732650115516,0.)) ;
#44097=DIRECTION('ref_axis',(-0.133732650115516,-0.991017446008435,0.)) ;
#44098=DIRECTION('center_axis',(-1.04325044166935E-14,-1.,0.)) ;
#44099=DIRECTION('ref_axis',(-0.675590207615657,7.04809782482522E-15,-0.737277336810127)) ;
#44100=DIRECTION('',(-1.04325044166935E-14,-1.,0.)) ;
#44101=DIRECTION('center_axis',(0.369647612382771,0.929172019950944,0.)) ;
#44102=DIRECTION('ref_axis',(-0.929172019950944,0.369647612382771,0.)) ;
#44103=DIRECTION('',(1.04325044166935E-14,1.,0.)) ;
#44104=DIRECTION('center_axis',(0.307221196683631,-0.877837780010281,-0.367445190871915)) ;
#44105=DIRECTION('ref_axis',(0.563077209989657,0.478958069131965,-0.673456177938583)) ;
#44106=DIRECTION('center_axis',(0.0844006559966532,0.249445165540006,0.964703912429121)) ;
#44107=DIRECTION('ref_axis',(0.996194698091746,-8.28110794162546E-18,-0.0871557427476575)) ;
#44108=DIRECTION('center_axis',(2.86369556082085E-16,-1.,0.)) ;
#44109=DIRECTION('ref_axis',(0.675590207615657,1.93468467848299E-16,-0.737277336810127)) ;
#44110=DIRECTION('center_axis',(0.0844345745997038,0.247929423057005,0.965091603836023)) ;
#44111=DIRECTION('ref_axis',(0.996194698091746,-3.65481143962558E-17,-0.0871557427476578)) ;
#44112=DIRECTION('center_axis',(0.0796183978311159,0.406796813220274,0.910042451471708)) ;
#44113=DIRECTION('ref_axis',(0.996194698091746,-2.8097871293113E-15,-0.0871557427476576)) ;
#44114=DIRECTION('center_axis',(-0.996194698091746,-2.45272960483312E-14,
0.0871557427476522)) ;
#44115=DIRECTION('ref_axis',(0.0827617664579715,0.313510371607444,0.945971319283687)) ;
#44116=DIRECTION('center_axis',(-0.996194698091746,-2.8527983346386E-16,
0.0871557427476584)) ;
#44117=DIRECTION('ref_axis',(0.0871557427476583,1.94505549952558E-32,0.996194698091746)) ;
#44118=DIRECTION('center_axis',(0.996194698091746,2.8527983346386E-16,-0.0871557427476584)) ;
#44119=DIRECTION('ref_axis',(0.0826892669295895,0.316018771704214,0.945142645882201)) ;
#44120=DIRECTION('center_axis',(0.0198801512493551,-0.973637907857952,0.227231168566931)) ;
#44121=DIRECTION('ref_axis',(0.0848581350266359,0.228099154715642,0.969932921669231)) ;
#44122=DIRECTION('center_axis',(-0.996194698091746,-2.8527983346386E-16,
0.0871557427476584)) ;
#44123=DIRECTION('ref_axis',(0.0826892669295895,0.316018771704214,0.945142645882201)) ;
#44124=DIRECTION('center_axis',(-0.996194698091746,-2.8527983346386E-16,
0.0871557427476584)) ;
#44125=DIRECTION('ref_axis',(0.0871557427476584,-7.26620746443239E-33,0.996194698091746)) ;
#44126=DIRECTION('',(-2.86369556082085E-16,1.,0.)) ;
#44127=DIRECTION('',(-0.0871426484044397,-0.0173337504938598,-0.996045029063886)) ;
#44128=DIRECTION('center_axis',(-2.86369556082085E-16,1.,0.)) ;
#44129=DIRECTION('ref_axis',(0.675590207615657,1.93468467848299E-16,-0.737277336810127)) ;
#44130=DIRECTION('',(2.86369556082085E-16,-1.,0.)) ;
#44131=DIRECTION('center_axis',(-0.369647612382753,0.929172019950951,2.56494556415654E-16)) ;
#44132=DIRECTION('ref_axis',(0.929172019950951,0.369647612382753,4.719839717894E-33)) ;
#44133=DIRECTION('center_axis',(-0.087142648404439,-0.0173337504938604,
-0.996045029063886)) ;
#44134=DIRECTION('ref_axis',(-0.920363891963227,-0.381227206369647,0.0871557427476579)) ;
#44135=DIRECTION('center_axis',(0.0140688745303267,-0.999901028487045,-1.39252255160153E-15)) ;
#44136=DIRECTION('ref_axis',(0.999901028487045,0.0140688745303267,-5.60930068162866E-33)) ;
#44137=DIRECTION('center_axis',(0.0871426484044397,0.0173337504938598,0.996045029063886)) ;
#44138=DIRECTION('ref_axis',(-0.976906303124668,-0.194318745462633,0.0888498738160228)) ;
#44139=DIRECTION('',(0.0871426484044397,0.0173337504938598,0.996045029063886)) ;
#44140=DIRECTION('center_axis',(-0.0871426484044391,-0.0173337504938592,
-0.996045029063886)) ;
#44141=DIRECTION('ref_axis',(-0.920363891963228,-0.381227206369644,0.0871557427476575)) ;
#44142=DIRECTION('center_axis',(0.,0.,1.)) ;
#44143=DIRECTION('ref_axis',(-0.686061634431343,0.72754342396959,0.)) ;
#44144=DIRECTION('center_axis',(-0.39079136747021,0.904898034275293,-0.168646537691926)) ;
#44145=DIRECTION('ref_axis',(0.0145744118599526,0.189275895687503,0.981815777949524)) ;
#44146=DIRECTION('center_axis',(-0.920363891963228,-0.381227206369645,0.0871557427476583)) ;
#44147=DIRECTION('ref_axis',(0.382683432365081,-0.92387953251129,8.03599596472331E-17)) ;
#44148=DIRECTION('',(-0.382683432365082,0.92387953251129,0.)) ;
#44149=DIRECTION('',(-0.0666626913468326,-0.0666626913468325,-0.995546167269401)) ;
#44150=DIRECTION('center_axis',(-0.920363891963228,-0.381227206369645,0.0871557427476583)) ;
#44151=DIRECTION('ref_axis',(-0.391063046541475,0.897215317273459,-0.205120374608633)) ;
#44152=DIRECTION('',(-0.0942752822069815,-5.29059027656383E-18,-0.995546167269401)) ;
#44153=DIRECTION('center_axis',(0.920363891963228,0.381227206369645,-0.0871557427476583)) ;
#44154=DIRECTION('ref_axis',(0.0315995086952039,0.149641293808218,0.988235272714764)) ;
#44155=DIRECTION('center_axis',(-0.382683432365082,0.92387953251129,0.)) ;
#44156=DIRECTION('ref_axis',(0.624163965181158,0.258537179522598,-0.737277336810128)) ;
#44157=DIRECTION('',(0.382683432365082,-0.92387953251129,0.)) ;
#44158=DIRECTION('center_axis',(-0.884086155524841,0.467323945041666,-6.13458003510009E-16)) ;
#44159=DIRECTION('ref_axis',(0.467323945041666,0.884086155524841,-3.60419358345438E-32)) ;
#44160=DIRECTION('center_axis',(0.087142648404439,-0.0173337504938606,-0.996045029063886)) ;
#44161=DIRECTION('ref_axis',(0.996194698091746,-9.7139919131807E-15,0.0871557427476578)) ;
#44162=DIRECTION('center_axis',(-0.0140688745303435,-0.999901028487045,
-1.38764143021586E-15)) ;
#44163=DIRECTION('ref_axis',(-0.999901028487044,0.0140688745303435,-4.34518124734398E-32)) ;
#44164=DIRECTION('center_axis',(-0.087142648404439,0.0173337504938613,0.996045029063886)) ;
#44165=DIRECTION('ref_axis',(0.976906303124666,-0.194318745462644,0.0888498738160224)) ;
#44166=DIRECTION('',(-0.087142648404439,0.0173337504938612,0.996045029063886)) ;
#44167=DIRECTION('center_axis',(0.087142648404439,-0.0173337504937438,-0.996045029063888)) ;
#44168=DIRECTION('ref_axis',(0.996194698091746,-8.32583325170817E-15,0.0871557427476576)) ;
#44169=DIRECTION('',(0.087142648404439,-0.0173337504938613,-0.996045029063886)) ;
#44170=DIRECTION('center_axis',(0.,0.,1.)) ;
#44171=DIRECTION('ref_axis',(1.,0.,0.)) ;
#44172=DIRECTION('center_axis',(-0.0198801512493651,-0.973637907857951,
0.227231168566934)) ;
#44173=DIRECTION('ref_axis',(-0.084858135026633,0.228099154715646,0.969932921669231)) ;
#44174=DIRECTION('center_axis',(0.390791367470222,0.904898034275287,-0.168646537691928)) ;
#44175=DIRECTION('ref_axis',(-0.0145744118599494,0.189275895687505,0.981815777949524)) ;
#44176=DIRECTION('center_axis',(0.996194698091746,-1.03928055877287E-14,
0.0871557427476579)) ;
#44177=DIRECTION('ref_axis',(0.0871557427476579,2.06998122833165E-31,-0.996194698091746)) ;
#44178=DIRECTION('center_axis',(-0.996194698091746,1.03928055877287E-14,
-0.0871557427476579)) ;
#44179=DIRECTION('ref_axis',(-0.0826892669295858,0.316018771704216,0.9451426458822)) ;
#44180=DIRECTION('center_axis',(-0.382683432365094,-0.923879532511285,0.)) ;
#44181=DIRECTION('ref_axis',(-0.624163965181155,0.258537179522606,-0.737277336810127)) ;
#44182=DIRECTION('',(-0.382683432365094,-0.923879532511285,0.)) ;
#44183=DIRECTION('center_axis',(0.884086155524847,0.467323945041655,-3.24271127339941E-16)) ;
#44184=DIRECTION('ref_axis',(-0.467323945041655,0.884086155524847,-7.36160927852353E-33)) ;
#44185=DIRECTION('',(0.382683432365094,0.923879532511285,0.)) ;
#44186=DIRECTION('center_axis',(-2.25344562200783E-7,0.00122104690338566,
0.999999254521927)) ;
#44187=DIRECTION('ref_axis',(0.880239547026216,0.474529244989194,-0.000579224539763828)) ;
#44188=DIRECTION('center_axis',(3.49420756930928E-5,-0.000974753633340996,
0.99999952431709)) ;
#44189=DIRECTION('ref_axis',(-0.117733043599258,0.993044805378454,0.00097208833143988)) ;
#44190=DIRECTION('center_axis',(0.,0.,1.)) ;
#44191=DIRECTION('ref_axis',(1.,0.,0.)) ;
#44192=DIRECTION('center_axis',(0.,0.,-1.)) ;
#44193=DIRECTION('ref_axis',(0.38268343236509,0.923879532511287,0.)) ;
#44194=DIRECTION('center_axis',(2.83928856810258E-5,3.29420197351069E-5,
0.999999999054334)) ;
#44195=DIRECTION('ref_axis',(0.96762709105351,0.252384253428295,-3.57877724692542E-5)) ;
#44196=DIRECTION('center_axis',(-5.19405847738775E-5,2.97673798315385E-5,
0.999999998208039)) ;
#44197=DIRECTION('ref_axis',(0.690866054023378,-0.722982774416375,5.74052898069753E-5)) ;
#44198=DIRECTION('center_axis',(0.,0.,-1.)) ;
#44199=DIRECTION('ref_axis',(-1.,0.,0.)) ;
#44200=DIRECTION('center_axis',(0.218991760123564,0.252536654884624,-0.942479626802441)) ;
#44201=DIRECTION('ref_axis',(-1.36744941626268E-14,-0.965925826289036,-0.258819045102642)) ;
#44202=DIRECTION('center_axis',(0.939992844931799,-0.341133990269129,0.00640719596122297)) ;
#44203=DIRECTION('ref_axis',(0.337451616258958,0.932291946017575,0.130223400642821)) ;
#44204=DIRECTION('center_axis',(0.942424992012689,-0.333801508271347,0.0202900839243436)) ;
#44205=DIRECTION('ref_axis',(0.334410493611304,0.940273089931856,-0.0636878176156427)) ;
#44206=DIRECTION('center_axis',(0.943545137525121,-0.327692396729339,0.0483763018272643)) ;
#44207=DIRECTION('ref_axis',(0.331217944158533,0.935186145148194,-0.12538559482754)) ;
#44208=DIRECTION('',(-0.328003666919281,-0.944669970289995,0.00349881691496844)) ;
#44209=DIRECTION('',(0.846577478048041,0.532254029430749,-0.00349597147443212)) ;
#44210=DIRECTION('center_axis',(-0.53049404449562,0.844439101982528,-0.0741530295916526)) ;
#44211=DIRECTION('ref_axis',(0.847670234963863,0.527872145314473,-0.0529733041956474)) ;
#44212=DIRECTION('center_axis',(-0.523158578258209,0.851633793864804,-0.0320153579128746)) ;
#44213=DIRECTION('ref_axis',(0.851857027606319,0.521437987961937,-0.0494168921314753)) ;
#44214=DIRECTION('center_axis',(-0.512178225761606,0.858833907404777,-0.00881955483771457)) ;
#44215=DIRECTION('ref_axis',(0.849520309205079,0.508082285339014,0.142012800735676)) ;
#44216=DIRECTION('center_axis',(0.249199500799499,0.0844061683157321,-0.964766918769263)) ;
#44217=DIRECTION('ref_axis',(-1.08248674634472E-13,-0.996194698093663,-0.0871557427257419)) ;
#44218=DIRECTION('center_axis',(0.95602568240079,0.13742503062509,0.259093140680714)) ;
#44219=DIRECTION('ref_axis',(0.256281665748432,0.038083835396144,-0.965851608313994)) ;
#44220=DIRECTION('center_axis',(-0.852367862727417,-0.245048083800581,-0.461974526586865)) ;
#44221=DIRECTION('ref_axis',(0.501019754926551,-0.129565454350722,-0.855682182946583)) ;
#44222=DIRECTION('',(0.249320710565386,0.0844034492993762,-0.964735840025413)) ;
#44223=DIRECTION('center_axis',(0.249445165540006,0.084400655996652,-0.964703912429121)) ;
#44224=DIRECTION('ref_axis',(-5.51682469897799E-15,-0.996194698091746,-0.0871557427476577)) ;
#44225=DIRECTION('',(-0.248916559555376,-0.0870782764297481,0.964602467420201)) ;
#44226=DIRECTION('center_axis',(0.3263419315863,-0.82640429306137,0.458864781932826)) ;
#44227=DIRECTION('ref_axis',(-0.478958069131965,-0.563077209989657,-0.673456177938582)) ;
#44228=DIRECTION('center_axis',(1.,-6.98296267768627E-15,0.)) ;
#44229=DIRECTION('ref_axis',(-4.71762120519045E-15,-0.675590207615657,-0.737277336810127)) ;
#44230=DIRECTION('center_axis',(-0.133732650115508,0.991017446008436,0.)) ;
#44231=DIRECTION('ref_axis',(0.991017446008436,0.133732650115508,0.)) ;
#44232=DIRECTION('center_axis',(6.9563903964836E-15,0.996194698091746,0.0871557427476574)) ;
#44233=DIRECTION('ref_axis',(-6.40601855134593E-32,-0.0871557427476574,
0.996194698091746)) ;
#44234=DIRECTION('',(-1.,6.98296267768627E-15,0.)) ;
#44235=DIRECTION('',(-0.0173337504938605,-0.0871426484044386,0.996045029063886)) ;
#44236=DIRECTION('',(1.,-6.98296267768627E-15,0.)) ;
#44237=DIRECTION('center_axis',(1.,-6.98296267768627E-15,0.)) ;
#44238=DIRECTION('ref_axis',(4.7176212051905E-15,0.675590207615663,0.737277336810121)) ;
#44239=DIRECTION('',(1.,-6.98296267768627E-15,0.)) ;
#44240=DIRECTION('center_axis',(1.,-1.67169584432416E-14,0.)) ;
#44241=DIRECTION('ref_axis',(0.,0.,1.)) ;
#44242=DIRECTION('center_axis',(0.,0.,1.)) ;
#44243=DIRECTION('ref_axis',(-1.,9.64749793678664E-15,0.)) ;
#44244=DIRECTION('center_axis',(0.,0.,-1.)) ;
#44245=DIRECTION('ref_axis',(-1.,8.00610789814445E-15,0.)) ;
#44246=DIRECTION('center_axis',(0.,0.,1.)) ;
#44247=DIRECTION('ref_axis',(-1.,8.1410746989025E-15,0.)) ;
#44248=DIRECTION('center_axis',(-0.326341931586305,-0.826404293061363,-0.458864781932835)) ;
#44249=DIRECTION('ref_axis',(-0.478958069131954,0.563077209989667,-0.673456177938582)) ;
#44250=DIRECTION('center_axis',(-0.249445165539996,0.084400655996657,0.964703912429124)) ;
#44251=DIRECTION('ref_axis',(1.12665838577891E-14,0.996194698091745,-0.0871557427476582)) ;
#44252=DIRECTION('center_axis',(-0.133732650115524,-0.991017446008434,0.)) ;
#44253=DIRECTION('ref_axis',(0.991017446008434,-0.133732650115524,0.)) ;
#44254=DIRECTION('center_axis',(1.,-1.01461348606114E-14,0.)) ;
#44255=DIRECTION('ref_axis',(6.85462935697691E-15,0.675590207615657,-0.737277336810127)) ;
#44256=DIRECTION('center_axis',(-0.249199500798557,0.0844061683219424,0.964766918768963)) ;
#44257=DIRECTION('ref_axis',(5.52024668591357E-15,0.996194698093106,-0.0871557427321035)) ;
#44258=DIRECTION('',(0.248916559555379,-0.0870782764297426,-0.9646024674202)) ;
#44259=DIRECTION('',(-0.249320710565346,0.0844034492993872,0.964735840025422)) ;
#44260=DIRECTION('center_axis',(-0.852367862729301,0.245048083794489,-0.461974526586621)) ;
#44261=DIRECTION('ref_axis',(0.5010197546446,0.129565452553711,-0.855682183383771)) ;
#44262=DIRECTION('center_axis',(-0.218991760123583,0.252536654884511,0.942479626802467)) ;
#44263=DIRECTION('ref_axis',(1.66369913122973E-14,0.965925826289068,-0.258819045102521)) ;
#44264=DIRECTION('center_axis',(0.956025682401039,-0.137425030623654,0.259093140680558)) ;
#44265=DIRECTION('ref_axis',(0.256281665662312,-0.0380838359928184,-0.965851608313318)) ;
#44266=DIRECTION('center_axis',(-1.,1.01461348606114E-14,0.)) ;
#44267=DIRECTION('ref_axis',(-6.85462935697698E-15,-0.675590207615664,0.737277336810121)) ;
#44268=DIRECTION('',(1.,-1.01461348606114E-14,0.)) ;
#44269=DIRECTION('center_axis',(1.,-9.20200038935782E-15,2.22044604925031E-14)) ;
#44270=DIRECTION('ref_axis',(-1.11022302462516E-14,-0.996194698091746,0.0871557427476575)) ;
#44271=DIRECTION('',(-1.,1.01461348606114E-14,0.)) ;
#44272=DIRECTION('center_axis',(-1.01075257542649E-14,-0.996194698091746,
0.0871557427476588)) ;
#44273=DIRECTION('ref_axis',(9.3268358271731E-31,-0.0871557427476588,-0.996194698091745)) ;
#44274=DIRECTION('',(-1.,1.01461348606114E-14,0.)) ;
#44275=DIRECTION('',(0.0173337504938584,-0.0871426484044403,-0.996045029063886)) ;
#44276=DIRECTION('center_axis',(-1.,1.01461348606114E-14,0.)) ;
#44277=DIRECTION('ref_axis',(6.85462935697691E-15,0.675590207615657,-0.737277336810127)) ;
#44278=DIRECTION('',(1.,-1.01461348606114E-14,0.)) ;
#44279=DIRECTION('center_axis',(-0.929172019950953,-0.369647612382748,5.12989112831302E-16)) ;
#44280=DIRECTION('ref_axis',(-0.369647612382748,0.929172019950953,3.80280772654386E-32)) ;
#44281=DIRECTION('center_axis',(0.,0.,-1.)) ;
#44282=DIRECTION('ref_axis',(-1.,0.,0.)) ;
#44283=DIRECTION('',(-0.923879532511294,-0.382683432365072,0.)) ;
#44284=DIRECTION('',(1.,0.,0.)) ;
#44285=DIRECTION('',(-1.,0.,0.)) ;
#44286=DIRECTION('',(0.923879532511287,-0.38268343236509,0.)) ;
#44287=DIRECTION('center_axis',(0.0666626913468315,-0.0666626913468327,
-0.995546167269401)) ;
#44288=DIRECTION('ref_axis',(0.920363891963223,-0.381227206369657,0.0871557427476578)) ;
#44289=DIRECTION('center_axis',(-0.467323945041676,-0.884086155524836,6.13458003510006E-16)) ;
#44290=DIRECTION('ref_axis',(-0.884086155524836,0.467323945041676,9.23656027967999E-33)) ;
#44291=DIRECTION('center_axis',(-0.0666626913468313,0.0666626913468338,
0.995546167269401)) ;
#44292=DIRECTION('ref_axis',(0.703957445860461,-0.703957445860479,0.0942752822069821)) ;
#44293=DIRECTION('center_axis',(0.0666626913468288,-0.0666626913468385,
-0.995546167269401)) ;
#44294=DIRECTION('ref_axis',(0.920363891963223,-0.381227206369658,0.0871557427476576)) ;
#44295=DIRECTION('',(0.0666626913468313,-0.0666626913468338,-0.995546167269401)) ;
#44296=DIRECTION('',(-0.0666626913468313,0.0666626913468338,0.995546167269401)) ;
#44297=DIRECTION('center_axis',(0.382648721133683,0.923893810008795,0.000429001387020652)) ;
#44298=DIRECTION('ref_axis',(3.3887587197891E-9,-0.000464341932836984,0.999999892193279)) ;
#44299=DIRECTION('center_axis',(0.920363891963223,-0.381227206369657,0.0871557427476581)) ;
#44300=DIRECTION('ref_axis',(0.391063046541487,0.897215317273456,-0.205120374608625)) ;
#44301=DIRECTION('center_axis',(0.0942752822069813,0.,-0.995546167269401)) ;
#44302=DIRECTION('ref_axis',(0.920363891963223,-0.381227206369657,0.0871557427476577)) ;
#44303=DIRECTION('center_axis',(-0.762014168288054,0.631273206450739,-0.144320983040126)) ;
#44304=DIRECTION('ref_axis',(0.647560350336759,0.742848333944369,-0.169829165421638)) ;
#44305=DIRECTION('center_axis',(-0.0942752822069817,0.,0.995546167269401)) ;
#44306=DIRECTION('ref_axis',(0.55374779771692,-0.831031649929668,0.0524382812345561)) ;
#44307=DIRECTION('center_axis',(0.0942752822069761,-1.10527827697982E-14,
-0.995546167269401)) ;
#44308=DIRECTION('ref_axis',(0.920363891963223,-0.381227206369657,0.0871557427476571)) ;
#44309=DIRECTION('',(-0.0942752822069817,0.,0.995546167269401)) ;
#44310=DIRECTION('center_axis',(1.,0.,0.)) ;
#44311=DIRECTION('ref_axis',(0.,-1.,0.)) ;
#44312=DIRECTION('center_axis',(-0.388740138376909,-0.916141414187395,0.0978060019907851)) ;
#44313=DIRECTION('ref_axis',(-0.0425606765102603,0.123898048145669,0.991381794507385)) ;
#44314=DIRECTION('center_axis',(0.990117129665866,0.,0.140242894801221)) ;
#44315=DIRECTION('ref_axis',(-0.140242894801221,0.,0.990117129665866)) ;
#44316=DIRECTION('center_axis',(1.,0.,0.)) ;
#44317=DIRECTION('ref_axis',(0.,-1.,0.)) ;
#44318=DIRECTION('center_axis',(0.923873568388754,0.382697789457833,0.000177698394351369)) ;
#44319=DIRECTION('ref_axis',(7.78311851840014E-16,-0.000464330811650805,
0.999999892198443)) ;
#44320=DIRECTION('center_axis',(-0.923879532511294,-0.382683432365072,0.)) ;
#44321=DIRECTION('ref_axis',(-0.258537179522591,0.624163965181161,-0.737277336810127)) ;
#44322=DIRECTION('',(-0.923879532511294,-0.382683432365072,0.)) ;
#44323=DIRECTION('center_axis',(0.999901028487045,0.0140688745303215,-1.41204703714418E-15)) ;
#44324=DIRECTION('ref_axis',(-0.0140688745303215,0.999901028487045,-6.14044914489112E-33)) ;
#44325=DIRECTION('',(0.923879532511294,0.382683432365072,0.)) ;
#44326=DIRECTION('center_axis',(0.381227206369636,-0.920363891963232,0.0871557427476586)) ;
#44327=DIRECTION('ref_axis',(0.923879532511294,0.382683432365072,2.41666793745239E-17)) ;
#44328=DIRECTION('',(0.923879532511294,0.382683432365072,0.)) ;
#44329=DIRECTION('',(-0.0173337504938584,0.0871426484044403,0.996045029063886)) ;
#44330=DIRECTION('center_axis',(1.,0.,0.)) ;
#44331=DIRECTION('ref_axis',(0.,0.707106781186548,-0.707106781186548)) ;
#44332=DIRECTION('center_axis',(-0.98591981532733,-0.142582648849442,0.0873630699552131)) ;
#44333=DIRECTION('ref_axis',(0.16721877210685,-0.840665536837555,0.515091581593703)) ;
#44334=DIRECTION('center_axis',(-0.017333750493859,0.0871426484044392,0.996045029063886)) ;
#44335=DIRECTION('ref_axis',(0.381227206369635,-0.920363891963232,0.0871557427476577)) ;
#44336=DIRECTION('center_axis',(-0.92387953251129,-0.382683432365083,6.19072153925554E-15)) ;
#44337=DIRECTION('ref_axis',(5.55111512312578E-15,2.77555756156289E-15,
1.)) ;
#44338=DIRECTION('center_axis',(-0.923879532511294,-0.382683432365072,0.)) ;
#44339=DIRECTION('ref_axis',(0.258537179522595,-0.62416396518117,0.737277336810118)) ;
#44340=DIRECTION('center_axis',(-0.0173337504938584,0.0871426484044403,
0.996045029063886)) ;
#44341=DIRECTION('ref_axis',(0.194318745462623,-0.97690630312467,0.0888498738160231)) ;
#44342=DIRECTION('center_axis',(-0.0173337504938614,0.0871426484044502,
0.996045029063885)) ;
#44343=DIRECTION('ref_axis',(-9.71372357808658E-15,-0.996194698091745,0.0871557427476687)) ;
#44344=DIRECTION('center_axis',(0.0942752822069805,1.3083323619903E-16,
-0.995546167269401)) ;
#44345=DIRECTION('ref_axis',(-1.38777878078144E-15,1.,4.3924990864866E-31)) ;
#44346=DIRECTION('center_axis',(0.382648720419747,-0.923893810300393,0.000429010201431217)) ;
#44347=DIRECTION('ref_axis',(0.920363891963229,0.381227206369639,0.0871557427476688)) ;
#44348=DIRECTION('center_axis',(-0.762014168288071,-0.631273206450718,-0.144320983040128)) ;
#44349=DIRECTION('ref_axis',(0.647560350336739,-0.742848333944383,-0.169829165421651)) ;
#44350=DIRECTION('center_axis',(-0.0942752822069809,0.,0.995546167269401)) ;
#44351=DIRECTION('ref_axis',(0.553747797716925,0.831031649929665,0.0524382812345561)) ;
#44352=DIRECTION('center_axis',(0.0942752822069809,0.,-0.995546167269401)) ;
#44353=DIRECTION('ref_axis',(0.,1.,0.)) ;
#44354=DIRECTION('',(-0.0942752822069809,0.,0.995546167269401)) ;
#44355=DIRECTION('center_axis',(1.,0.,0.)) ;
#44356=DIRECTION('ref_axis',(0.,0.653011882880021,0.757347661789148)) ;
#44357=DIRECTION('center_axis',(0.990117129665866,0.,0.140242894801223)) ;
#44358=DIRECTION('ref_axis',(-0.140242894801223,7.9794965316409E-17,0.990117129665866)) ;
#44359=DIRECTION('center_axis',(-0.388740138376891,0.916141414187403,0.0978060019907881)) ;
#44360=DIRECTION('ref_axis',(-0.042560676510261,-0.12389804814567,0.991381794507385)) ;
#44361=DIRECTION('center_axis',(-0.0666626913468331,-0.066662691346831,
0.995546167269401)) ;
#44362=DIRECTION('ref_axis',(0.703957445860476,0.703957445860465,0.0942752822069814)) ;
#44363=DIRECTION('center_axis',(0.0666626913468211,0.0666626913468305,-0.995546167269402)) ;
#44364=DIRECTION('ref_axis',(0.381227219735143,0.920363886377725,0.0871557432686075)) ;
#44365=DIRECTION('center_axis',(-0.0666626913468326,-0.0666626913468315,
0.995546167269401)) ;
#44366=DIRECTION('ref_axis',(0.92036389196323,0.381227206369639,0.0871557427476577)) ;
#44367=DIRECTION('',(-0.0666626913468331,-0.066662691346831,0.995546167269401)) ;
#44368=DIRECTION('center_axis',(-0.467323945041656,0.884086155524847,6.13458003510013E-16)) ;
#44369=DIRECTION('ref_axis',(-0.884086155524847,-0.467323945041656,-8.62742891290345E-32)) ;
#44370=DIRECTION('center_axis',(1.,0.,0.)) ;
#44371=DIRECTION('ref_axis',(0.,-1.,0.)) ;
#44372=DIRECTION('center_axis',(0.923873568388748,-0.382697789457847,0.000177698394306731)) ;
#44373=DIRECTION('ref_axis',(0.381227206369654,0.920363891963224,0.0871557427476576)) ;
#44374=DIRECTION('center_axis',(0.92036389196323,0.381227206369639,0.087155742747658)) ;
#44375=DIRECTION('ref_axis',(0.0942752822069809,1.55365773163449E-17,-0.995546167269401)) ;
#44376=DIRECTION('center_axis',(0.92036389196323,0.381227206369639,0.087155742747658)) ;
#44377=DIRECTION('ref_axis',(-0.0315995086952045,-0.149641293808218,0.988235272714764)) ;
#44378=DIRECTION('center_axis',(0.,1.,0.)) ;
#44379=DIRECTION('ref_axis',(0.,0.,1.)) ;
#44380=DIRECTION('center_axis',(0.,-1.,0.)) ;
#44381=DIRECTION('ref_axis',(-0.37177215563764,0.,0.928324008249567)) ;
#44382=DIRECTION('center_axis',(-0.807964101600016,1.34553052300038E-14,
-0.589231712084201)) ;
#44383=DIRECTION('ref_axis',(-0.581351145863386,-0.163002279992783,0.797158141099043)) ;
#44384=DIRECTION('center_axis',(0.,1.,0.)) ;
#44385=DIRECTION('ref_axis',(-0.37177215563764,0.,0.928324008249567)) ;
#44386=DIRECTION('center_axis',(0.,-1.,0.)) ;
#44387=DIRECTION('ref_axis',(0.,0.,-1.)) ;
#44388=DIRECTION('',(0.,0.,-1.)) ;
#44389=DIRECTION('center_axis',(0.,-1.,0.)) ;
#44390=DIRECTION('ref_axis',(-0.525952960008619,0.,-0.850513658831046)) ;
#44391=DIRECTION('',(1.,0.,0.)) ;
#44392=DIRECTION('center_axis',(1.,0.,0.)) ;
#44393=DIRECTION('ref_axis',(0.,-0.707106781186548,-0.707106781186548)) ;
#44394=DIRECTION('center_axis',(0.381227206369654,0.920363891963224,0.0871557427476574)) ;
#44395=DIRECTION('ref_axis',(-0.923879532511287,0.38268343236509,8.02781664235613E-17)) ;
#44396=DIRECTION('',(0.923879532511287,-0.38268343236509,4.83811561633781E-18)) ;
#44397=DIRECTION('',(0.0173337504938605,0.0871426484044386,-0.996045029063886)) ;
#44398=DIRECTION('',(-0.923879532511287,0.38268343236509,-4.83811561633781E-18)) ;
#44399=DIRECTION('center_axis',(-0.985919815327329,0.142582648849448,0.0873630699552218)) ;
#44400=DIRECTION('ref_axis',(0.167218772106861,0.840665536837553,0.515091581593703)) ;
#44401=DIRECTION('center_axis',(-0.0173337504938585,-0.0871426484044279,
0.996045029063887)) ;
#44402=DIRECTION('ref_axis',(6.93831543720529E-15,0.996194698091747,0.0871557427476467)) ;
#44403=DIRECTION('center_axis',(-0.923879532511282,0.382683432365101,1.13192831841253E-14)) ;
#44404=DIRECTION('ref_axis',(0.381227206369666,0.920363891963219,0.0871557427476574)) ;
#44405=DIRECTION('center_axis',(0.923879532511286,-0.382683432365091,0.)) ;
#44406=DIRECTION('ref_axis',(0.258537179522607,0.624163965181163,0.73727733681012)) ;
#44407=DIRECTION('center_axis',(-0.0173337504938605,-0.0871426484044386,
0.996045029063886)) ;
#44408=DIRECTION('ref_axis',(0.194318745462641,0.976906303124666,0.0888498738160219)) ;
#44409=DIRECTION('center_axis',(-0.0173337504938607,-0.0871426484044388,
0.996045029063886)) ;
#44410=DIRECTION('ref_axis',(0.381227206369655,0.920363891963224,0.0871557427476577)) ;
#44411=DIRECTION('center_axis',(0.999901028487045,-0.0140688745303409,2.76552061766038E-15)) ;
#44412=DIRECTION('ref_axis',(-0.0140688745303409,-0.999901028487045,1.27304684468474E-32)) ;
#44413=DIRECTION('center_axis',(-0.929172019950944,0.369647612382769,1.28247278207833E-16)) ;
#44414=DIRECTION('ref_axis',(-0.369647612382769,-0.929172019950944,-9.94337188479288E-33)) ;
#44415=DIRECTION('center_axis',(1.,-6.98296267768627E-15,0.)) ;
#44416=DIRECTION('ref_axis',(-4.71762120519044E-15,-0.675590207615656,-0.737277336810128)) ;
#44417=DIRECTION('',(-1.,6.98296267768627E-15,0.)) ;
#44418=DIRECTION('center_axis',(0.923879532511286,-0.382683432365091,0.)) ;
#44419=DIRECTION('ref_axis',(-0.258537179522604,-0.624163965181156,-0.737277336810127)) ;
#44420=DIRECTION('',(-0.923879532511287,0.38268343236509,0.)) ;
#44421=DIRECTION('center_axis',(1.,0.,0.)) ;
#44422=DIRECTION('ref_axis',(0.,0.707106781186548,-0.707106781186548)) ;
#44423=DIRECTION('',(1.,0.,0.)) ;
#44424=DIRECTION('',(-1.,0.,0.)) ;
#44425=DIRECTION('center_axis',(0.762014168288065,0.631273206450725,-0.144320983040127)) ;
#44426=DIRECTION('ref_axis',(-0.647560350336745,0.742848333944378,-0.169829165421649)) ;
#44427=DIRECTION('center_axis',(-0.218991760123586,-0.252536654884508,-0.942479626802467)) ;
#44428=DIRECTION('ref_axis',(-2.81914239016188E-15,0.965925826289068,-0.258819045102521)) ;
#44429=DIRECTION('center_axis',(-0.939992844966884,0.341133990171559,0.00640719600867651)) ;
#44430=DIRECTION('ref_axis',(0.337451616159548,0.93229194606199,-0.130223400582445)) ;
#44431=DIRECTION('center_axis',(-0.942424992002713,0.333801508312564,0.0202900837096207)) ;
#44432=DIRECTION('ref_axis',(0.334410493637827,0.940273089914465,0.0636878177331398)) ;
#44433=DIRECTION('center_axis',(-0.943545137507695,0.327692396888825,0.0483763010868215)) ;
#44434=DIRECTION('ref_axis',(0.331217944217424,0.935186145117652,0.12538559489977)) ;
#44435=DIRECTION('',(0.328003666872713,0.944669970306165,0.00349881691470218)) ;
#44436=DIRECTION('',(-0.846577478023147,-0.532254029470342,-0.00349597147476316)) ;
#44437=DIRECTION('center_axis',(0.530494044393499,-0.844439102113116,-0.0741530288351211)) ;
#44438=DIRECTION('ref_axis',(0.847670235028008,0.527872145264436,0.0529733036678171)) ;
#44439=DIRECTION('center_axis',(0.523158578227078,-0.851633793891756,-0.0320153577046641)) ;
#44440=DIRECTION('ref_axis',(0.851857027623571,0.521437987939093,0.049416892075135)) ;
#44441=DIRECTION('center_axis',(0.51217822584914,-0.858833907352119,-0.00881955488214049)) ;
#44442=DIRECTION('ref_axis',(0.849520309139197,0.508082285425671,-0.142012800819747)) ;
#44443=DIRECTION('center_axis',(-0.249199500799459,-0.0844061683159849,
-0.964766918769251)) ;
#44444=DIRECTION('ref_axis',(2.76101386392502E-15,0.996194698093643,-0.087155742725975)) ;
#44445=DIRECTION('center_axis',(-0.956025682401338,-0.137425030622013,0.259093140680327)) ;
#44446=DIRECTION('ref_axis',(0.25628166568836,0.0380838358104107,0.965851608313599)) ;
#44447=DIRECTION('center_axis',(0.852367862728953,0.245048083795463,-0.461974526586746)) ;
#44448=DIRECTION('ref_axis',(0.501019755025973,-0.129565454997057,0.855682182790503)) ;
#44449=DIRECTION('',(-0.249320710565382,-0.0844034492993914,-0.964735840025412)) ;
#44450=DIRECTION('center_axis',(-0.249445165543295,-0.0844006560005468,
-0.96470391242793)) ;
#44451=DIRECTION('ref_axis',(-4.51830490057156E-18,0.996194698091387,-0.0871557427517545)) ;
#44452=DIRECTION('',(0.248916559555392,0.0870782764297379,0.964602467420198)) ;
#44453=DIRECTION('center_axis',(0.326341931589371,-0.826404293060443,-0.458864781932311)) ;
#44454=DIRECTION('ref_axis',(0.478958069134772,0.563077209991019,-0.673456177935448)) ;
#44455=DIRECTION('center_axis',(-1.,0.,0.)) ;
#44456=DIRECTION('ref_axis',(0.,0.675590207615657,-0.737277336810127)) ;
#44457=DIRECTION('center_axis',(0.133732650115514,-0.991017446008435,0.)) ;
#44458=DIRECTION('ref_axis',(-0.991017446008435,-0.133732650115514,0.)) ;
#44459=DIRECTION('center_axis',(0.,-0.996194698091746,0.0871557427476584)) ;
#44460=DIRECTION('ref_axis',(0.,-0.0871557427476584,-0.996194698091746)) ;
#44461=DIRECTION('',(1.,0.,0.)) ;
#44462=DIRECTION('',(0.0173337504938599,0.0871426484044397,0.996045029063886)) ;
#44463=DIRECTION('',(-1.,0.,0.)) ;
#44464=DIRECTION('center_axis',(-1.,0.,0.)) ;
#44465=DIRECTION('ref_axis',(0.,-0.675590207615663,0.737277336810121)) ;
#44466=DIRECTION('',(-1.,0.,0.)) ;
#44467=DIRECTION('center_axis',(-1.,0.,0.)) ;
#44468=DIRECTION('ref_axis',(0.,0.,1.)) ;
#44469=DIRECTION('center_axis',(0.,0.,1.)) ;
#44470=DIRECTION('ref_axis',(1.,0.,0.)) ;
#44471=DIRECTION('center_axis',(0.,0.,-1.)) ;
#44472=DIRECTION('ref_axis',(1.,-1.67349113601944E-15,0.)) ;
#44473=DIRECTION('center_axis',(0.,0.,1.)) ;
#44474=DIRECTION('ref_axis',(1.,-1.69309011255336E-15,0.)) ;
#44475=DIRECTION('center_axis',(-0.326341931586302,-0.826404293061369,0.458864781932826)) ;
#44476=DIRECTION('ref_axis',(0.478958069131963,-0.563077209989659,-0.673456177938582)) ;
#44477=DIRECTION('center_axis',(0.249445165540005,-0.084400655996654,0.964703912429121)) ;
#44478=DIRECTION('ref_axis',(-5.38268147788269E-15,-0.996194698091746,-0.087155742747657)) ;
#44479=DIRECTION('center_axis',(0.133732650115517,0.991017446008435,0.)) ;
#44480=DIRECTION('ref_axis',(-0.991017446008435,0.133732650115517,0.)) ;
#44481=DIRECTION('center_axis',(-1.,3.16317218292511E-15,0.)) ;
#44482=DIRECTION('ref_axis',(-2.13700815178645E-15,-0.675590207615657,-0.737277336810127)) ;
#44483=DIRECTION('center_axis',(0.249199500798546,-0.0844061683219426,0.964766918768965)) ;
#44484=DIRECTION('ref_axis',(-5.55075920992131E-15,-0.996194698093106,-0.0871557427321035)) ;
#44485=DIRECTION('',(-0.248916559555379,0.0870782764297428,-0.9646024674202)) ;
#44486=DIRECTION('',(0.249320710565346,-0.0844034492993872,0.964735840025422)) ;
#44487=DIRECTION('center_axis',(0.852367862729215,-0.245048083794411,-0.461974526586821)) ;
#44488=DIRECTION('ref_axis',(0.501019754798628,0.129565453540298,0.855682183144197)) ;
#44489=DIRECTION('center_axis',(0.218991760123595,-0.252536654884593,0.942479626802442)) ;
#44490=DIRECTION('ref_axis',(-1.77417912264492E-16,-0.965925826289044,-0.258819045102609)) ;
#44491=DIRECTION('center_axis',(-0.956025682401085,0.137425030623292,0.259093140680579)) ;
#44492=DIRECTION('ref_axis',(0.256281665788873,-0.0380838351145112,0.965851608314368)) ;
#44493=DIRECTION('center_axis',(1.,-3.16317218292511E-15,0.)) ;
#44494=DIRECTION('ref_axis',(2.13700815178647E-15,0.675590207615663,0.737277336810121)) ;
#44495=DIRECTION('',(-1.,3.16317218292511E-15,0.)) ;
#44496=DIRECTION('center_axis',(-1.,6.05797912428137E-15,-5.55111512312578E-15)) ;
#44497=DIRECTION('ref_axis',(5.55111512312579E-15,0.996194698091746,0.0871557427476578)) ;
#44498=DIRECTION('',(1.,-3.16317218292511E-15,0.)) ;
#44499=DIRECTION('center_axis',(3.15113535778129E-15,0.996194698091746,
0.0871557427476579)) ;
#44500=DIRECTION('ref_axis',(-1.82466814306167E-33,-0.0871557427476579,
0.996194698091746)) ;
#44501=DIRECTION('',(1.,-3.16317218292511E-15,0.)) ;
#44502=DIRECTION('',(-0.0173337504938591,0.0871426484044392,-0.996045029063886)) ;
#44503=DIRECTION('center_axis',(1.,-3.16317218292511E-15,0.)) ;
#44504=DIRECTION('ref_axis',(-2.13700815178645E-15,-0.675590207615657,-0.737277336810127)) ;
#44505=DIRECTION('',(-1.,3.16317218292511E-15,0.)) ;
#44506=DIRECTION('center_axis',(0.929172019950952,0.369647612382751,2.56494556415653E-16)) ;
#44507=DIRECTION('ref_axis',(0.369647612382751,-0.929172019950952,9.32329065219925E-33)) ;
#44508=DIRECTION('center_axis',(0.,0.,-1.)) ;
#44509=DIRECTION('ref_axis',(-1.,0.,0.)) ;
#44510=DIRECTION('',(-0.923879532511289,0.382683432365084,0.)) ;
#44511=DIRECTION('',(0.923879532511292,0.382683432365078,0.)) ;
#44512=DIRECTION('',(-1.,0.,0.)) ;
#44513=DIRECTION('center_axis',(0.0666626913468318,-0.0666626913468324,
0.995546167269401)) ;
#44514=DIRECTION('ref_axis',(-0.703957445860467,0.703957445860474,0.0942752822069815)) ;
#44515=DIRECTION('center_axis',(-0.0666626913468308,0.0666626913468347,
-0.995546167269401)) ;
#44516=DIRECTION('ref_axis',(-0.920363891963225,0.381227206369651,0.0871557427476577)) ;
#44517=DIRECTION('',(-0.0666626913468318,0.0666626913468324,-0.995546167269401)) ;
#44518=DIRECTION('center_axis',(0.0666626913468317,-0.0666626913468324,
0.995546167269401)) ;
#44519=DIRECTION('ref_axis',(-0.381227206369643,0.920363891963229,0.0871557427476577)) ;
#44520=DIRECTION('',(0.0666626913468317,-0.0666626913468324,0.995546167269401)) ;
#44521=DIRECTION('center_axis',(0.467323945041671,0.884086155524839,-6.48542254679904E-16)) ;
#44522=DIRECTION('ref_axis',(0.884086155524839,-0.467323945041671,5.72532255921785E-31)) ;
#44523=DIRECTION('center_axis',(-0.884086155524845,-0.467323945041659,-6.13458003510012E-16)) ;
#44524=DIRECTION('ref_axis',(0.467323945041659,-0.884086155524845,8.11346111104324E-33)) ;
#44525=DIRECTION('center_axis',(-0.382648721138496,-0.923893810006829,0.000429001327519702)) ;
#44526=DIRECTION('ref_axis',(-3.36632111294574E-9,0.000464341859142652,
0.999999892193313)) ;
#44527=DIRECTION('center_axis',(-0.920363891963225,0.381227206369651,0.0871557427476577)) ;
#44528=DIRECTION('ref_axis',(-0.391063046541481,-0.897215317273458,-0.205120374608628)) ;
#44529=DIRECTION('center_axis',(-0.0942752822069765,1.10527827697982E-14,
-0.995546167269401)) ;
#44530=DIRECTION('ref_axis',(-0.920363891963225,0.381227206369651,0.0871557427476577)) ;
#44531=DIRECTION('center_axis',(0.762014168288059,-0.631273206450732,-0.144320983040126)) ;
#44532=DIRECTION('ref_axis',(-0.647560350336752,-0.742848333944374,-0.16982916542164)) ;
#44533=DIRECTION('center_axis',(-0.0942752822069811,0.,-0.995546167269401)) ;
#44534=DIRECTION('ref_axis',(-0.55374779771692,0.831031649929668,0.0524382812345557)) ;
#44535=DIRECTION('center_axis',(-0.0942752822069763,1.11836160059972E-14,
-0.995546167269401)) ;
#44536=DIRECTION('ref_axis',(-0.920363891963225,0.381227206369652,0.0871557427476575)) ;
#44537=DIRECTION('',(0.0942752822069811,0.,0.995546167269401)) ;
#44538=DIRECTION('center_axis',(1.,0.,0.)) ;
#44539=DIRECTION('ref_axis',(0.,0.653011882880003,0.757347661789164)) ;
#44540=DIRECTION('center_axis',(0.388740138376903,0.916141414187398,0.0978060019907864)) ;
#44541=DIRECTION('ref_axis',(0.04256067651026,-0.123898048145669,0.991381794507385)) ;
#44542=DIRECTION('center_axis',(-0.990117129665866,0.,0.140242894801221)) ;
#44543=DIRECTION('ref_axis',(0.140242894801221,0.,0.990117129665866)) ;
#44544=DIRECTION('center_axis',(1.,0.,0.)) ;
#44545=DIRECTION('ref_axis',(0.,-1.,0.)) ;
#44546=DIRECTION('center_axis',(-0.923873568388752,-0.382697789457837,0.000177698394329629)) ;
#44547=DIRECTION('ref_axis',(-4.6023382439147E-16,0.000464330811593225,
0.999999892198443)) ;
#44548=DIRECTION('center_axis',(0.382683432365087,0.923879532511288,0.)) ;
#44549=DIRECTION('ref_axis',(0.624163965181156,-0.258537179522601,-0.737277336810128)) ;
#44550=DIRECTION('',(0.382683432365087,0.923879532511288,0.)) ;
#44551=DIRECTION('',(-0.382683432365087,-0.923879532511288,0.)) ;
#44552=DIRECTION('center_axis',(0.923879532511292,0.382683432365078,0.)) ;
#44553=DIRECTION('ref_axis',(0.258537179522595,-0.624163965181159,-0.737277336810128)) ;
#44554=DIRECTION('',(0.923879532511292,0.382683432365078,0.)) ;
#44555=DIRECTION('center_axis',(-0.999901028487045,-0.0140688745303254,
1.3827603088302E-15)) ;
#44556=DIRECTION('ref_axis',(0.0140688745303254,-0.999901028487045,3.77607068720447E-33)) ;
#44557=DIRECTION('',(-0.923879532511292,-0.382683432365078,0.)) ;
#44558=DIRECTION('center_axis',(-0.381227206369642,0.920363891963229,0.0871557427476577)) ;
#44559=DIRECTION('ref_axis',(-0.923879532511292,-0.382683432365078,-6.24302505454772E-17)) ;
#44560=DIRECTION('',(-0.923879532511292,-0.382683432365078,0.)) ;
#44561=DIRECTION('',(0.0173337504938591,-0.0871426484044392,0.996045029063886)) ;
#44562=DIRECTION('center_axis',(1.,0.,0.)) ;
#44563=DIRECTION('ref_axis',(0.,-0.707106781186548,-0.707106781186548)) ;
#44564=DIRECTION('center_axis',(-0.985919815327333,-0.142582648849427,-0.0873630699552041)) ;
#44565=DIRECTION('ref_axis',(-0.167218772106832,0.840665536837554,0.515091581593712)) ;
#44566=DIRECTION('center_axis',(0.0173337504938596,-0.0871426484044392,
0.996045029063886)) ;
#44567=DIRECTION('ref_axis',(-0.381227206369643,0.920363891963229,0.0871557427476578)) ;
#44568=DIRECTION('center_axis',(0.923879532511292,0.382683432365077,0.)) ;
#44569=DIRECTION('ref_axis',(0.,0.,1.)) ;
#44570=DIRECTION('center_axis',(0.923879532511292,0.382683432365078,0.)) ;
#44571=DIRECTION('ref_axis',(-0.258537179522597,0.624163965181164,0.737277336810123)) ;
#44572=DIRECTION('center_axis',(-0.0173337504938596,0.0871426484044391,
-0.996045029063886)) ;
#44573=DIRECTION('ref_axis',(-0.381227206369642,0.920363891963229,0.0871557427476578)) ;
#44574=DIRECTION('center_axis',(0.0173337504938591,-0.0871426484044393,
0.996045029063886)) ;
#44575=DIRECTION('ref_axis',(-0.194318745462631,0.976906303124668,0.0888498738160223)) ;
#44576=DIRECTION('center_axis',(-0.920363891963225,0.381227206369651,0.0871557427476577)) ;
#44577=DIRECTION('ref_axis',(-0.382683432365087,-0.923879532511288,6.71680456512626E-17)) ;
#44578=DIRECTION('center_axis',(0.920363891963225,-0.381227206369651,-0.0871557427476577)) ;
#44579=DIRECTION('ref_axis',(0.0315995086952024,-0.149641293808218,0.988235272714764)) ;
#44580=DIRECTION('center_axis',(-0.0942752822069733,1.09219495335991E-14,
-0.995546167269402)) ;
#44581=DIRECTION('ref_axis',(1.38777878078145E-15,-1.,-1.11022302462515E-14)) ;
#44582=DIRECTION('center_axis',(-0.382648720419749,0.923893810300391,0.000429010201481)) ;
#44583=DIRECTION('ref_axis',(-0.920363891963227,-0.381227206369645,0.0871557427476687)) ;
#44584=DIRECTION('center_axis',(-0.0942752822069815,0.,-0.995546167269401)) ;
#44585=DIRECTION('ref_axis',(-0.553747797716923,-0.831031649929666,0.0524382812345562)) ;
#44586=DIRECTION('center_axis',(-0.0942752822069688,-1.30833236199014E-16,
-0.995546167269402)) ;
#44587=DIRECTION('ref_axis',(1.38777878078145E-15,-1.,-2.81120891065768E-31)) ;
#44588=DIRECTION('',(0.0942752822069815,0.,0.995546167269401)) ;
#44589=DIRECTION('center_axis',(1.,0.,0.)) ;
#44590=DIRECTION('ref_axis',(0.,-1.,0.)) ;
#44591=DIRECTION('center_axis',(-0.990117129665866,0.,0.140242894801223)) ;
#44592=DIRECTION('ref_axis',(0.140242894801223,-7.9794965316409E-17,0.990117129665866)) ;
#44593=DIRECTION('center_axis',(0.388740138376897,-0.9161414141874,0.0978060019907868)) ;
#44594=DIRECTION('ref_axis',(0.0425606765102615,0.12389804814567,0.991381794507385)) ;
#44595=DIRECTION('center_axis',(0.0666626913468326,0.0666626913468325,0.995546167269401)) ;
#44596=DIRECTION('ref_axis',(-0.703957445860472,-0.703957445860469,0.0942752822069821)) ;
#44597=DIRECTION('center_axis',(-0.0666626913468289,-0.0666626913468395,
-0.995546167269401)) ;
#44598=DIRECTION('ref_axis',(-0.381227219735137,-0.920363886377726,0.0871557432686186)) ;
#44599=DIRECTION('center_axis',(0.0666626913468406,0.0666626913468404,0.9955461672694)) ;
#44600=DIRECTION('ref_axis',(-0.920363891963227,-0.381227206369644,0.0871557427476687)) ;
#44601=DIRECTION('',(0.0666626913468326,0.0666626913468325,0.995546167269401)) ;
#44602=DIRECTION('center_axis',(0.467323945041663,-0.884086155524843,-6.1345800351001E-16)) ;
#44603=DIRECTION('ref_axis',(0.884086155524843,0.467323945041663,-1.13677469639285E-32)) ;
#44604=DIRECTION('center_axis',(1.,0.,0.)) ;
#44605=DIRECTION('ref_axis',(0.,-1.,0.)) ;
#44606=DIRECTION('center_axis',(-0.92387356838875,0.382697789457843,0.000177698394328006)) ;
#44607=DIRECTION('ref_axis',(-0.381227206369648,-0.920363891963226,0.0871557427476688)) ;
#44608=DIRECTION('center_axis',(-0.920363891963228,-0.381227206369645,0.0871557427476583)) ;
#44609=DIRECTION('ref_axis',(0.0942752822069815,-1.5536577316345E-17,0.995546167269401)) ;
#44610=DIRECTION('center_axis',(-0.920363891963228,-0.381227206369645,0.0871557427476583)) ;
#44611=DIRECTION('ref_axis',(0.0315995086952039,0.149641293808218,0.988235272714764)) ;
#44612=DIRECTION('center_axis',(0.,1.,0.)) ;
#44613=DIRECTION('ref_axis',(0.,0.,1.)) ;
#44614=DIRECTION('center_axis',(0.,1.,0.)) ;
#44615=DIRECTION('ref_axis',(0.37177215563764,0.,0.928324008249567)) ;
#44616=DIRECTION('center_axis',(-0.807964101600017,0.,0.5892317120842)) ;
#44617=DIRECTION('ref_axis',(0.,-1.,0.)) ;
#44618=DIRECTION('center_axis',(0.,-1.,0.)) ;
#44619=DIRECTION('ref_axis',(0.37177215563764,0.,0.928324008249567)) ;
#44620=DIRECTION('center_axis',(0.,-1.,0.)) ;
#44621=DIRECTION('ref_axis',(0.,0.,-1.)) ;
#44622=DIRECTION('',(0.,0.,-1.)) ;
#44623=DIRECTION('center_axis',(-0.381227206369648,-0.920363891963227,0.0871557427476583)) ;
#44624=DIRECTION('ref_axis',(0.923879532511289,-0.382683432365084,3.0103033140203E-19)) ;
#44625=DIRECTION('',(-0.923879532511289,0.382683432365084,0.)) ;
#44626=DIRECTION('',(-0.0173337504938599,-0.0871426484044397,-0.996045029063886)) ;
#44627=DIRECTION('',(0.923879532511289,-0.382683432365084,0.)) ;
#44628=DIRECTION('center_axis',(-0.985919815327331,0.142582648849435,-0.087363069955213)) ;
#44629=DIRECTION('ref_axis',(-0.167218772106845,-0.840665536837551,0.515091581593712)) ;
#44630=DIRECTION('center_axis',(0.0173337504938597,0.087142648404439,0.996045029063886)) ;
#44631=DIRECTION('ref_axis',(2.15180843051778E-18,-0.996194698091746,0.0871557427476576)) ;
#44632=DIRECTION('center_axis',(0.923879532511289,-0.382683432365085,5.12856164486979E-15)) ;
#44633=DIRECTION('ref_axis',(-0.381227206369649,-0.920363891963226,0.0871557427476576)) ;
#44634=DIRECTION('center_axis',(-0.923879532511289,0.382683432365084,0.)) ;
#44635=DIRECTION('ref_axis',(-0.258537179522602,-0.624163965181165,0.73727733681012)) ;
#44636=DIRECTION('center_axis',(0.0173337504938599,0.0871426484044397,0.996045029063886)) ;
#44637=DIRECTION('ref_axis',(-0.194318745462635,-0.976906303124667,0.0888498738160228)) ;
#44638=DIRECTION('center_axis',(0.0173337504938597,0.087142648404439,0.996045029063886)) ;
#44639=DIRECTION('ref_axis',(-0.381227206369648,-0.920363891963227,0.0871557427476576)) ;
#44640=DIRECTION('center_axis',(-0.999901028487045,0.0140688745303331,1.40716591575854E-15)) ;
#44641=DIRECTION('ref_axis',(0.0140688745303331,0.999901028487045,-1.44407851814174E-34)) ;
#44642=DIRECTION('center_axis',(0.929172019950948,-0.36964761238276,0.)) ;
#44643=DIRECTION('ref_axis',(0.36964761238276,0.929172019950948,0.)) ;
#44644=DIRECTION('center_axis',(-1.,0.,0.)) ;
#44645=DIRECTION('ref_axis',(0.,0.675590207615656,-0.737277336810128)) ;
#44646=DIRECTION('',(1.,0.,0.)) ;
#44647=DIRECTION('center_axis',(-0.923879532511289,0.382683432365084,0.)) ;
#44648=DIRECTION('ref_axis',(0.258537179522599,0.624163965181158,-0.737277336810127)) ;
#44649=DIRECTION('',(0.923879532511289,-0.382683432365084,0.)) ;
#44650=DIRECTION('center_axis',(0.,0.,1.)) ;
#44651=DIRECTION('ref_axis',(-1.,7.87114109738639E-15,0.)) ;
#44652=DIRECTION('center_axis',(0.,0.,-1.)) ;
#44653=DIRECTION('ref_axis',(-1.,8.19721404385209E-15,0.)) ;
#44654=DIRECTION('center_axis',(6.03394327975752E-16,6.03394327975742E-16,
1.)) ;
#44655=DIRECTION('ref_axis',(-1.,8.03417757061924E-15,6.03394327975747E-16)) ;
#44656=DIRECTION('center_axis',(0.,0.,1.)) ;
#44657=DIRECTION('ref_axis',(1.,0.,0.)) ;
#44658=DIRECTION('center_axis',(0.,0.,-1.)) ;
#44659=DIRECTION('ref_axis',(-4.78181680548827E-15,-1.,0.)) ;
#44660=DIRECTION('center_axis',(-6.03394327975744E-16,6.0339432797575E-16,
1.)) ;
#44661=DIRECTION('ref_axis',(-4.55012211203708E-15,-1.,6.03394327975747E-16)) ;
#44662=DIRECTION('center_axis',(0.,0.,1.)) ;
#44663=DIRECTION('ref_axis',(1.,0.,0.)) ;
#44664=DIRECTION('center_axis',(0.,0.,-1.)) ;
#44665=DIRECTION('ref_axis',(1.,-1.73472347597681E-15,0.)) ;
#44666=DIRECTION('center_axis',(0.,0.,1.)) ;
#44667=DIRECTION('ref_axis',(1.,-1.69430781773116E-15,0.)) ;
#44668=DIRECTION('center_axis',(0.920363891963223,-0.381227206369657,0.0871557427476581)) ;
#44669=DIRECTION('ref_axis',(0.382683432365093,0.923879532511285,-6.76580195217738E-17)) ;
#44670=DIRECTION('center_axis',(-0.920363891963223,0.381227206369657,-0.0871557427476581)) ;
#44671=DIRECTION('ref_axis',(-0.0315995086952019,0.149641293808218,0.988235272714764)) ;
#44672=DIRECTION('center_axis',(0.,0.,1.)) ;
#44673=DIRECTION('ref_axis',(1.,0.,0.)) ;
#44674=DIRECTION('center_axis',(0.,0.,1.)) ;
#44675=DIRECTION('ref_axis',(1.,0.,0.)) ;
#44676=DIRECTION('center_axis',(0.,1.,0.)) ;
#44677=DIRECTION('ref_axis',(0.,0.,1.)) ;
#44678=DIRECTION('center_axis',(0.,1.,0.)) ;
#44679=DIRECTION('ref_axis',(0.371772155637639,0.,0.928324008249568)) ;
#44680=DIRECTION('center_axis',(-0.807964101600016,0.,0.589231712084202)) ;
#44681=DIRECTION('ref_axis',(0.581351145863385,-0.163002279992778,0.797158141099045)) ;
#44682=DIRECTION('center_axis',(-0.920363891963225,0.381227206369651,0.0871557427476577)) ;
#44683=DIRECTION('ref_axis',(0.0942752822069811,-1.03577182108966E-17,0.995546167269401)) ;
#44684=DIRECTION('center_axis',(-0.920363891963225,0.381227206369651,0.0871557427476577)) ;
#44685=DIRECTION('ref_axis',(0.0315995086952024,-0.149641293808218,0.988235272714764)) ;
#44686=DIRECTION('center_axis',(3.34743552557144E-30,9.58743639363279E-16,
1.)) ;
#44687=DIRECTION('ref_axis',(1.,0.,0.)) ;
#44688=DIRECTION('center_axis',(-5.38716036738172E-30,-1.00092047861322E-15,
-1.)) ;
#44689=DIRECTION('ref_axis',(-5.27809922139864E-15,-1.,1.00092047861322E-15)) ;
#44690=DIRECTION('center_axis',(3.34743552557144E-30,9.58743639363279E-16,
1.)) ;
#44691=DIRECTION('ref_axis',(-5.34959260451127E-15,-1.,9.58743639363279E-16)) ;
#44692=DIRECTION('center_axis',(0.,0.,1.)) ;
#44693=DIRECTION('ref_axis',(-0.793390388649525,0.608713143605883,0.)) ;
#44694=DIRECTION('',(0.,0.,1.)) ;
#44695=DIRECTION('center_axis',(0.,0.,-1.)) ;
#44696=DIRECTION('ref_axis',(-0.965894315163092,-0.258936617602884,0.)) ;
#44697=DIRECTION('center_axis',(1.,-1.83697019872103E-16,0.)) ;
#44698=DIRECTION('ref_axis',(-1.22464679914735E-16,-1.,4.94506671532915E-16)) ;
#44699=DIRECTION('center_axis',(0.,4.79371819681639E-16,1.)) ;
#44700=DIRECTION('ref_axis',(0.,-1.,4.79371819681639E-16)) ;
#44701=DIRECTION('center_axis',(0.,4.79371819681639E-16,1.)) ;
#44702=DIRECTION('ref_axis',(0.,-1.,5.18039323243001E-16)) ;
#44703=DIRECTION('center_axis',(0.,4.79371819681639E-16,1.)) ;
#44704=DIRECTION('ref_axis',(0.,-1.,4.79371819681639E-16)) ;
#44705=DIRECTION('center_axis',(0.,0.,-1.)) ;
#44706=DIRECTION('ref_axis',(-1.,0.,0.)) ;
#44707=DIRECTION('center_axis',(-0.807964101600022,-4.48510174333462E-15,
-0.589231712084193)) ;
#44708=DIRECTION('ref_axis',(5.55111512312579E-15,-1.,-3.90782375100986E-30)) ;
#44709=DIRECTION('center_axis',(0.,1.,0.)) ;
#44710=DIRECTION('ref_axis',(0.,0.,1.)) ;
#44711=DIRECTION('center_axis',(0.,-1.,0.)) ;
#44712=DIRECTION('ref_axis',(-0.371772155637639,0.,0.928324008249568)) ;
#44713=DIRECTION('center_axis',(0.920363891963223,-0.381227206369657,0.0871557427476581)) ;
#44714=DIRECTION('ref_axis',(0.0942752822069817,-4.14308728435866E-17,-0.995546167269401)) ;
#44715=DIRECTION('center_axis',(0.920363891963223,-0.381227206369657,0.0871557427476581)) ;
#44716=DIRECTION('ref_axis',(-0.0315995086952019,0.149641293808218,0.988235272714764)) ;
#44717=DIRECTION('center_axis',(0.996194698091746,-1.03928055877287E-14,
0.0871557427476579)) ;
#44718=DIRECTION('ref_axis',(0.0871557427476579,4.02740903431178E-31,-0.996194698091746)) ;
#44719=DIRECTION('center_axis',(0.996194698091746,-1.03928055877287E-14,
0.0871557427476579)) ;
#44720=DIRECTION('ref_axis',(-0.0826892669295858,0.316018771704216,0.9451426458822)) ;
#44721=DIRECTION('center_axis',(0.,0.,1.)) ;
#44722=DIRECTION('ref_axis',(5.55111512312579E-15,-1.,0.)) ;
#44723=DIRECTION('center_axis',(0.,0.,-1.)) ;
#44724=DIRECTION('ref_axis',(0.793390388649528,-0.608713143605879,0.)) ;
#44725=DIRECTION('',(0.,0.,1.)) ;
#44726=DIRECTION('center_axis',(1.,-1.83697019872103E-16,0.)) ;
#44727=DIRECTION('ref_axis',(-1.22464679914735E-16,-1.,4.94506671532915E-16)) ;
#44728=DIRECTION('center_axis',(0.,4.79371819681639E-16,1.)) ;
#44729=DIRECTION('ref_axis',(0.,-1.,4.79371819681639E-16)) ;
#44730=DIRECTION('center_axis',(0.,4.79371819681639E-16,1.)) ;
#44731=DIRECTION('ref_axis',(-1.22464679914735E-16,1.,-5.18039323243001E-16)) ;
#44732=DIRECTION('center_axis',(0.,4.79371819681639E-16,1.)) ;
#44733=DIRECTION('ref_axis',(0.,-1.,4.79371819681639E-16)) ;
#44734=DIRECTION('center_axis',(0.,0.,-1.)) ;
#44735=DIRECTION('ref_axis',(-1.,0.,0.)) ;
#44736=DIRECTION('center_axis',(0.,0.,1.)) ;
#44737=DIRECTION('ref_axis',(1.,0.,0.)) ;
#44738=DIRECTION('',(0.707106781186549,8.65956056235495E-17,-0.707106781186546)) ;
#44739=DIRECTION('center_axis',(0.,0.,-1.)) ;
#44740=DIRECTION('ref_axis',(1.,0.,0.)) ;
#44741=DIRECTION('center_axis',(3.34743552557144E-30,9.58743639363279E-16,
1.)) ;
#44742=DIRECTION('ref_axis',(7.70749845132874E-46,-1.,9.58743639363279E-16)) ;
#44743=DIRECTION('center_axis',(4.79371819681639E-16,4.79371819681634E-16,
1.)) ;
#44744=DIRECTION('ref_axis',(-1.,8.75931951708652E-15,4.79371819681635E-16)) ;
#44745=DIRECTION('center_axis',(0.,0.,1.)) ;
#44746=DIRECTION('ref_axis',(1.,0.,0.)) ;
#73261=CARTESIAN_POINT('',(0.,0.,0.)) ;
#73262=CARTESIAN_POINT('Origin',(3.10601593664312E-15,-2.12330153459561E-14,
-0.34726562499997)) ;
#73263=CARTESIAN_POINT('',(8.51359053417684E-13,-1.23704425180947,5.55625000000022)) ;
#73264=CARTESIAN_POINT('',(3.44719424660001E-14,-1.23704425180958,5.65546875)) ;
#73265=CARTESIAN_POINT('',(6.06053764494801E-15,-1.23704425180962,-0.347265624999939)) ;
#73266=CARTESIAN_POINT('',(-1.23064526020309,-0.123127494296425,6.16388000977423)) ;
#73267=CARTESIAN_POINT('Ctrl Pts',(1.63466462588189E-12,-1.23704425180947,
5.55625000000022)) ;
#73268=CARTESIAN_POINT('Ctrl Pts',(0.032410535193708,-1.23704425180947,
5.55938790945648)) ;
#73269=CARTESIAN_POINT('Ctrl Pts',(0.06485156327478,-1.23577059586982,5.56257984877948)) ;
#73270=CARTESIAN_POINT('Ctrl Pts',(0.261554273988151,-1.22025878337805,
5.58224620102718)) ;
#73271=CARTESIAN_POINT('Ctrl Pts',(0.421583054731985,-1.17459990755325,
5.59957086456626)) ;
#73272=CARTESIAN_POINT('Ctrl Pts',(0.709312921724199,-1.02590447288471,
5.63339132862922)) ;
#73273=CARTESIAN_POINT('Ctrl Pts',(0.835234563292027,-0.926268012883034,
5.64889464075713)) ;
#73274=CARTESIAN_POINT('Ctrl Pts',(1.0461788342556,-0.680415129648602,5.68115705137086)) ;
#73275=CARTESIAN_POINT('Ctrl Pts',(1.12741507524917,-0.535130549153963,
5.69848098170242)) ;
#73276=CARTESIAN_POINT('Ctrl Pts',(1.22646116995911,-0.226717318521629,
5.73231286381708)) ;
#73277=CARTESIAN_POINT('Ctrl Pts',(1.24541854129917,-0.0672584313812708,
5.74783986629028)) ;
#73278=CARTESIAN_POINT('Ctrl Pts',(1.22147882786804,0.255844813611181,5.78008199728177)) ;
#73279=CARTESIAN_POINT('Ctrl Pts',(1.17654329196774,0.416157461096852,5.797405135899)) ;
#73280=CARTESIAN_POINT('Ctrl Pts',(1.02911988768562,0.704643939698382,5.83124784083467)) ;
#73281=CARTESIAN_POINT('Ctrl Pts',(0.930044054170639,0.831030132889457,
5.84679794267637)) ;
#73282=CARTESIAN_POINT('Ctrl Pts',(0.685083752317439,1.04313900555543,5.8790206399247)) ;
#73283=CARTESIAN_POINT('Ctrl Pts',(0.540097293143178,1.1250543206284,5.89634293988441)) ;
#73284=CARTESIAN_POINT('Ctrl Pts',(0.232033318192428,1.2254691170157,5.93019589716347)) ;
#73285=CARTESIAN_POINT('Ctrl Pts',(0.0726391820466259,1.24511793858861,
5.94576847016992)) ;
#73286=CARTESIAN_POINT('Ctrl Pts',(-0.2506458377757,1.22256553715424,5.97797256457448)) ;
#73287=CARTESIAN_POINT('Ctrl Pts',(-0.411213940163794,1.17828945821474,
5.99529398941272)) ;
#73288=CARTESIAN_POINT('Ctrl Pts',(-0.700386660668012,1.03202510449678,
6.02915665304384)) ;
#73289=CARTESIAN_POINT('Ctrl Pts',(-0.827195214883551,0.93345884249799,
6.04475103884394)) ;
#73290=CARTESIAN_POINT('Ctrl Pts',(-1.04036027204184,0.689311906417811,
6.07693734431807)) ;
#73291=CARTESIAN_POINT('Ctrl Pts',(-1.12289141919012,0.544598890120713,
6.09425786700923)) ;
#73292=CARTESIAN_POINT('Ctrl Pts',(-1.20198911794031,0.305149566984994,
6.1206128371872)) ;
#73293=CARTESIAN_POINT('Ctrl Pts',(-1.22052187953621,0.219605249836496,
6.12963825279501)) ;
#73294=CARTESIAN_POINT('Ctrl Pts',(-1.23907720793799,0.0477697380486169,
6.14701907770368)) ;
#73295=CARTESIAN_POINT('Ctrl Pts',(-1.2394166269485,-0.0379502076343803,
6.15514160739101)) ;
#73296=CARTESIAN_POINT('Ctrl Pts',(-1.23090852815641,-0.123055581940823,
6.1637225050298)) ;
#73297=CARTESIAN_POINT('',(-1.18366931688486,-0.359039527537319,6.28795132031109)) ;
#73298=CARTESIAN_POINT('Ctrl Pts',(-1.23090128330268,-0.123128029703915,
6.1637298109973)) ;
#73299=CARTESIAN_POINT('Ctrl Pts',(-1.22220034015823,-0.210110677832008,
6.17250309915399)) ;
#73300=CARTESIAN_POINT('Ctrl Pts',(-1.20583575204488,-0.280578131537651,
6.18520779853968)) ;
#73301=CARTESIAN_POINT('Ctrl Pts',(-1.18696998481902,-0.349039280868321,
6.20671103290821)) ;
#73302=CARTESIAN_POINT('Ctrl Pts',(-1.18180835795257,-0.365742807077991,
6.21365128674509)) ;
#73303=CARTESIAN_POINT('Ctrl Pts',(-1.17619838945325,-0.383234137286321,
6.22434464445792)) ;
#73304=CARTESIAN_POINT('Ctrl Pts',(-1.17433885136118,-0.388879457581289,
6.22846304369811)) ;
#73305=CARTESIAN_POINT('Ctrl Pts',(-1.17208930685934,-0.395590250986855,
6.23599150360299)) ;
#73306=CARTESIAN_POINT('Ctrl Pts',(-1.17136121561512,-0.39773526410404,
6.23910049969088)) ;
#73307=CARTESIAN_POINT('Ctrl Pts',(-1.17059733480713,-0.399976624072225,
6.24494531778126)) ;
#73308=CARTESIAN_POINT('Ctrl Pts',(-1.17042655012746,-0.400474933454289,
6.24743652302402)) ;
#73309=CARTESIAN_POINT('Ctrl Pts',(-1.17044238937348,-0.400428638657382,
6.25245242249197)) ;
#73310=CARTESIAN_POINT('Ctrl Pts',(-1.17060894530179,-0.399942487518192,
6.25480649215178)) ;
#73311=CARTESIAN_POINT('Ctrl Pts',(-1.17128204467748,-0.397967653749609,
6.2600343415439)) ;
#73312=CARTESIAN_POINT('Ctrl Pts',(-1.17186577386847,-0.39624915385918,
6.26274945420801)) ;
#73313=CARTESIAN_POINT('Ctrl Pts',(-1.17375333330537,-0.390635890342859,
6.26967799482782)) ;
#73314=CARTESIAN_POINT('Ctrl Pts',(-1.17535164607556,-0.385813073064476,
6.27358482212547)) ;
#73315=CARTESIAN_POINT('Ctrl Pts',(-1.17890754325678,-0.374831481607947,
6.28103038015207)) ;
#73316=CARTESIAN_POINT('Ctrl Pts',(-1.1811438609383,-0.367736459238746,
6.28473131480161)) ;
#73317=CARTESIAN_POINT('Ctrl Pts',(-1.1832560635873,-0.36080960203242,6.28787103703615)) ;
#73318=CARTESIAN_POINT('Ctrl Pts',(-1.51494228338223E-16,-1.23704425180958,
5.65546875)) ;
#73319=CARTESIAN_POINT('Ctrl Pts',(0.512400506355205,-1.23704425180958,
5.705078125)) ;
#73320=CARTESIAN_POINT('Ctrl Pts',(0.874722379082391,-0.874722379082391,
5.7546875)) ;
#73321=CARTESIAN_POINT('Ctrl Pts',(1.23704425180958,-0.512400506355206,
5.804296875)) ;
#73322=CARTESIAN_POINT('Ctrl Pts',(1.23704425180958,-2.27241342507335E-16,
5.85390625)) ;
#73323=CARTESIAN_POINT('Ctrl Pts',(1.23704425180958,0.512400506355206,5.903515625)) ;
#73324=CARTESIAN_POINT('Ctrl Pts',(0.874722379082391,0.874722379082391,
5.953125)) ;
#73325=CARTESIAN_POINT('Ctrl Pts',(0.512400506355206,1.23704425180958,6.002734375)) ;
#73326=CARTESIAN_POINT('Ctrl Pts',(0.,1.23704425180958,6.05234375)) ;
#73327=CARTESIAN_POINT('Ctrl Pts',(-0.512400506355205,1.23704425180958,
6.101953125)) ;
#73328=CARTESIAN_POINT('Ctrl Pts',(-0.874722379082391,0.874722379082391,
6.1515625)) ;
#73329=CARTESIAN_POINT('Ctrl Pts',(-1.23704425180958,0.512400506355205,
6.201171875)) ;
#73330=CARTESIAN_POINT('Ctrl Pts',(-1.23704425180958,7.57471141691116E-17,
6.25078125)) ;
#73331=CARTESIAN_POINT('Ctrl Pts',(-1.23704425180958,-0.183204766505095,
6.26851869141665)) ;
#73332=CARTESIAN_POINT('Ctrl Pts',(-1.18394409959329,-0.358545464304532,
6.28762423629624)) ;
#73333=CARTESIAN_POINT('Origin',(3.10601593664312E-15,-2.12330153459561E-14,
-0.34726562499997)) ;
#73334=CARTESIAN_POINT('',(9.19078401434668E-13,-1.23704425180949,4.76250000000022)) ;
#73335=CARTESIAN_POINT('',(4.35160472637051E-13,-1.23704425180949,4.86171875000003)) ;
#73336=CARTESIAN_POINT('',(6.06053764494801E-15,-1.23704425180962,-0.347265624999939)) ;
#73337=CARTESIAN_POINT('Ctrl Pts',(1.77843850757079E-12,-1.23704425180949,
4.76250000000022)) ;
#73338=CARTESIAN_POINT('Ctrl Pts',(0.0421386522123601,-1.23704425180949,
4.76657976216588)) ;
#73339=CARTESIAN_POINT('Ctrl Pts',(0.0843179104865776,-1.23489139653225,
4.77074979199699)) ;
#73340=CARTESIAN_POINT('Ctrl Pts',(0.289955684198697,-1.21377252576669,
4.79150607610251)) ;
#73341=CARTESIAN_POINT('Ctrl Pts',(0.448520280260818,-1.16452899411383,
4.80883273683123)) ;
#73342=CARTESIAN_POINT('Ctrl Pts',(0.732438679409685,-1.00951739173385,
4.84253748205696)) ;
#73343=CARTESIAN_POINT('Ctrl Pts',(0.85603735041666,-0.907074834681463,
4.85783713510419)) ;
#73344=CARTESIAN_POINT('Ctrl Pts',(1.06111293017096,-0.656791531698224,
4.890293135197)) ;
#73345=CARTESIAN_POINT('Ctrl Pts',(1.13892739263001,-0.510058436740854,
4.90762008307935)) ;
#73346=CARTESIAN_POINT('Ctrl Pts',(1.23110405460236,-0.199936799080401,
4.94134188310875)) ;
#73347=CARTESIAN_POINT('Ctrl Pts',(1.24658404004136,-0.0401507195947445,
4.95666762906366)) ;
#73348=CARTESIAN_POINT('Ctrl Pts',(1.2156625882264,0.281988156101469,4.98909638188065)) ;
#73349=CARTESIAN_POINT('Ctrl Pts',(1.16742238571045,0.440972297818764,5.00642342534077)) ;
#73350=CARTESIAN_POINT('Ctrl Pts',(1.01418089980775,0.725968107940733,5.04016149563328)) ;
#73351=CARTESIAN_POINT('Ctrl Pts',(0.912528610844644,0.850220582311041,
5.05551334297379)) ;
#73352=CARTESIAN_POINT('Ctrl Pts',(0.663486603667513,1.05695544741248,5.08791570638977)) ;
#73353=CARTESIAN_POINT('Ctrl Pts',(0.517153989968506,1.13573725453211,5.10524267421844)) ;
#73354=CARTESIAN_POINT('Ctrl Pts',(0.207506710452891,1.22985149951979,5.13899625123036)) ;
#73355=CARTESIAN_POINT('Ctrl Pts',(0.0478133168613316,1.24631356321518,
5.15437410194347)) ;
#73356=CARTESIAN_POINT('Ctrl Pts',(-0.274606409922473,1.21736453792499,
5.18675094555916)) ;
#73357=CARTESIAN_POINT('Ctrl Pts',(-0.433973118519662,1.17005549056148,
5.20407768595966)) ;
#73358=CARTESIAN_POINT('Ctrl Pts',(-0.719961390303868,1.01845516294561,
5.23784602836267)) ;
#73359=CARTESIAN_POINT('Ctrl Pts',(-0.844818078053866,0.917532851082596,
5.25324968710869)) ;
#73360=CARTESIAN_POINT('Ctrl Pts',(-1.05308115417194,0.669641964324695,
5.28560188791629)) ;
#73361=CARTESIAN_POINT('Ctrl Pts',(-1.13275399505154,0.523684505045508,
5.30292826746668)) ;
#73362=CARTESIAN_POINT('Ctrl Pts',(-1.22865598812913,0.214480137870498,
5.33671065711472)) ;
#73363=CARTESIAN_POINT('Ctrl Pts',(-1.24602329086207,0.0548719765320699,
5.35213984046059)) ;
#73364=CARTESIAN_POINT('Ctrl Pts',(-1.2188919644099,-0.267800701702066,
5.38446827876781)) ;
#73365=CARTESIAN_POINT('Ctrl Pts',(-1.172442762695,-0.427514916174963,5.4017941813232)) ;
#73366=CARTESIAN_POINT('Ctrl Pts',(-1.02235660958171,-0.714413388720673,
5.43558992398581)) ;
#73367=CARTESIAN_POINT('Ctrl Pts',(-0.922105525992712,-0.83982589633167,
5.45104426958003)) ;
#73368=CARTESIAN_POINT('Ctrl Pts',(-0.67527687879584,-1.04949031574621,
5.48334982521286)) ;
#73369=CARTESIAN_POINT('Ctrl Pts',(-0.52966876539888,-1.12998027012065,
5.50067515076929)) ;
#73370=CARTESIAN_POINT('Ctrl Pts',(-0.251874491965004,-1.21773217371334,
5.53108964699106)) ;
#73371=CARTESIAN_POINT('Ctrl Pts',(-0.126242819055568,-1.23704425180948,
5.54402747626354)) ;
#73372=CARTESIAN_POINT('Ctrl Pts',(1.6324094853637E-12,-1.23704425180947,
5.55625000000022)) ;
#73373=CARTESIAN_POINT('Ctrl Pts',(1.55431223447522E-12,-1.23704425180947,
5.65546875000009)) ;
#73374=CARTESIAN_POINT('Ctrl Pts',(-0.152484622127137,-1.23704425180965,
5.64070555849834)) ;
#73375=CARTESIAN_POINT('Ctrl Pts',(-0.303785698542382,-1.20885031199389,
5.62492628913784)) ;
#73376=CARTESIAN_POINT('Ctrl Pts',(-0.589144297891564,-1.09848368938504,
5.5928725116777)) ;
#73377=CARTESIAN_POINT('Ctrl Pts',(-0.720593565085903,-1.01711877777539,
5.57688292274652)) ;
#73378=CARTESIAN_POINT('Ctrl Pts',(-0.951469283805133,-0.80643673920516,
5.54608108124321)) ;
#73379=CARTESIAN_POINT('Ctrl Pts',(-1.04730480818369,-0.677363204564986,
5.53022106353388)) ;
#73380=CARTESIAN_POINT('Ctrl Pts',(-1.18731261688945,-0.38453773123282,
5.49625565641034)) ;
#73381=CARTESIAN_POINT('Ctrl Pts',(-1.22802379686505,-0.22264310855874,
5.47894876478225)) ;
#73382=CARTESIAN_POINT('Ctrl Pts',(-1.24310775880187,0.101564705464852,
5.44695483565233)) ;
#73383=CARTESIAN_POINT('Ctrl Pts',(-1.21973263319505,0.260611300944475,
5.43110524505445)) ;
#73384=CARTESIAN_POINT('Ctrl Pts',(-1.1119278562886,0.566738642807326,5.3971434263766)) ;
#73385=CARTESIAN_POINT('Ctrl Pts',(-1.02636294861819,0.71006129721331,5.37983585179094)) ;
#73386=CARTESIAN_POINT('Ctrl Pts',(-0.807993422942662,0.950145843994516,
5.34783414140409)) ;
#73387=CARTESIAN_POINT('Ctrl Pts',(-0.679088552550741,1.04618462062345,
5.33199553059705)) ;
#73388=CARTESIAN_POINT('Ctrl Pts',(-0.386533477579363,1.18666069086128,
5.29803752402347)) ;
#73389=CARTESIAN_POINT('Ctrl Pts',(-0.224735086010386,1.22763894321764,
5.28072923881316)) ;
#73390=CARTESIAN_POINT('Ctrl Pts',(0.0994070490296592,1.24328068929504,
5.24871929966044)) ;
#73391=CARTESIAN_POINT('Ctrl Pts',(0.258479555860714,1.22018413326961,5.23289224202295)) ;
#73392=CARTESIAN_POINT('Ctrl Pts',(0.56475485011669,1.11293256584222,5.19893828439744)) ;
#73393=CARTESIAN_POINT('Ctrl Pts',(0.708205206869946,1.0276398336734,5.18162926107586)) ;
#73394=CARTESIAN_POINT('Ctrl Pts',(0.948658049494458,0.809737369586976,
5.14961062382056)) ;
#73395=CARTESIAN_POINT('Ctrl Pts',(1.04492481020587,0.681021673583593,5.13379571305975)) ;
#73396=CARTESIAN_POINT('Ctrl Pts',(1.18592563438713,0.388770188997297,5.09984605508362)) ;
#73397=CARTESIAN_POINT('Ctrl Pts',(1.22720313449488,0.227080222725434,5.08253626656936)) ;
#73398=CARTESIAN_POINT('Ctrl Pts',(1.24347018371378,-0.096987662505879,
5.05050843947551)) ;
#73399=CARTESIAN_POINT('Ctrl Pts',(1.22068586068575,-0.256089223457063,
5.03470628906358)) ;
#73400=CARTESIAN_POINT('Ctrl Pts',(1.11405421863357,-0.562529739913569,
5.0007611959873)) ;
#73401=CARTESIAN_POINT('Ctrl Pts',(1.02906669016739,-0.706122595938415,
4.98345061586245)) ;
#73402=CARTESIAN_POINT('Ctrl Pts',(0.811687924735941,-0.94698751559422,
4.95141308427514)) ;
#73403=CARTESIAN_POINT('Ctrl Pts',(0.683184093978087,-1.04350962700163,
4.93562432666935)) ;
#73404=CARTESIAN_POINT('Ctrl Pts',(0.391273003367663,-1.18509758235805,
4.90168407900147)) ;
#73405=CARTESIAN_POINT('Ctrl Pts',(0.229705083936882,-1.22670984317707,
4.88437268180648)) ;
#73406=CARTESIAN_POINT('Ctrl Pts',(0.0431281364359357,-1.2364808339211,
4.86591690646213)) ;
#73407=CARTESIAN_POINT('Ctrl Pts',(0.0215559159419141,-1.23704425180949,
4.86380574153132)) ;
#73408=CARTESIAN_POINT('Ctrl Pts',(8.09560751768692E-13,-1.23704425180949,
4.86171875000003)) ;
#73409=CARTESIAN_POINT('Origin',(3.10601593664312E-15,-2.12330153459561E-14,
-0.34726562499997)) ;
#73410=CARTESIAN_POINT('',(5.32647143441161E-13,-1.23704425180951,3.96875000000014)) ;
#73411=CARTESIAN_POINT('',(6.23963519277181E-13,-1.23704425180951,4.06796875000008)) ;
#73412=CARTESIAN_POINT('',(6.06053764494801E-15,-1.23704425180962,-0.347265624999939)) ;
#73413=CARTESIAN_POINT('Ctrl Pts',(1.0139111772387E-12,-1.23704425180951,
3.96875000000014)) ;
#73414=CARTESIAN_POINT('Ctrl Pts',(0.0551038756713428,-1.23704425180951,
3.97408502367433)) ;
#73415=CARTESIAN_POINT('Ctrl Pts',(0.110249673505602,-1.23336321992724,
3.97957172713591)) ;
#73416=CARTESIAN_POINT('Ctrl Pts',(0.327554666791744,-1.20410203287067,
4.00178413571668)) ;
#73417=CARTESIAN_POINT('Ctrl Pts',(0.484045790880615,-1.15014797873887,
4.01909895471897)) ;
#73418=CARTESIAN_POINT('Ctrl Pts',(0.762789740117514,-0.986797807279728,
4.05263712515903)) ;
#73419=CARTESIAN_POINT('Ctrl Pts',(0.883277688017725,-0.880589329049968,
4.06774382098912)) ;
#73420=CARTESIAN_POINT('Ctrl Pts',(1.08038014525501,-0.624463865032571,
4.1004456975994)) ;
#73421=CARTESIAN_POINT('Ctrl Pts',(1.15354966053906,-0.475904993799031,
4.11776313568763)) ;
#73422=CARTESIAN_POINT('Ctrl Pts',(1.2364656378473,-0.163597807609727,4.15132515257324)) ;
#73423=CARTESIAN_POINT('Ctrl Pts',(1.24723638954917,-0.00336380386512913,
4.16645308780335)) ;
#73424=CARTESIAN_POINT('Ctrl Pts',(1.20685407023023,0.317335284596847,4.19912185452807)) ;
#73425=CARTESIAN_POINT('Ctrl Pts',(1.15417636174644,0.474405368821141,4.21644154156241)) ;
#73426=CARTESIAN_POINT('Ctrl Pts',(0.993090564161647,0.754570831146914,
4.25002653092196)) ;
#73427=CARTESIAN_POINT('Ctrl Pts',(0.887912031932113,0.875908694415663,
4.26517683476727)) ;
#73428=CARTESIAN_POINT('Ctrl Pts',(0.633372016242751,1.07520220942914,4.29781308043887)) ;
#73429=CARTESIAN_POINT('Ctrl Pts',(0.485298711297695,1.14964745804084,4.31513466810497)) ;
#73430=CARTESIAN_POINT('Ctrl Pts',(0.173576773798556,1.23510024408959,4.34874175666028)) ;
#73431=CARTESIAN_POINT('Ctrl Pts',(0.0134663297023445,1.24716370540185,
4.36391540060311)) ;
#73432=CARTESIAN_POINT('Ctrl Pts',(-0.307643328469588,1.20937850104566,
4.39651976519306)) ;
#73433=CARTESIAN_POINT('Ctrl Pts',(-0.465251840947688,1.15791401095084,
4.41384292766305)) ;
#73434=CARTESIAN_POINT('Ctrl Pts',(-0.746754901463488,0.998977011960021,
4.44747124643818)) ;
#73435=CARTESIAN_POINT('Ctrl Pts',(-0.868895668647008,0.894770740285789,
4.46266904680359)) ;
#73436=CARTESIAN_POINT('Ctrl Pts',(-1.07025040888213,0.641736004836289,
4.49524221652169)) ;
#73437=CARTESIAN_POINT('Ctrl Pts',(-1.14589635909296,0.494130644689081,
4.51256665082678)) ;
#73438=CARTESIAN_POINT('Ctrl Pts',(-1.2337411814112,0.182969856561674,4.54621533845682)) ;
#73439=CARTESIAN_POINT('Ctrl Pts',(-1.24702165966823,0.0229753121996063,
4.56143796044876)) ;
#73440=CARTESIAN_POINT('Ctrl Pts',(-1.21168159833801,-0.298510265502198,
4.59398066271132)) ;
#73441=CARTESIAN_POINT('Ctrl Pts',(-1.16136280242387,-0.456616720778517,
4.61130608884694)) ;
#73442=CARTESIAN_POINT('Ctrl Pts',(-1.00445201492435,-0.739371046092404,
4.64497429457722)) ;
#73443=CARTESIAN_POINT('Ctrl Pts',(-0.90115810133007,-0.862265756220849,
4.66022225759696)) ;
#73444=CARTESIAN_POINT('Ctrl Pts',(-0.649543364335466,-1.06554826071117,
4.69273525593167)) ;
#73445=CARTESIAN_POINT('Ctrl Pts',(-0.502385483457626,-1.14231757247314,
4.7100614167188)) ;
#73446=CARTESIAN_POINT('Ctrl Pts',(-0.232372718583162,-1.22062577891459,
4.7393438041112)) ;
#73447=CARTESIAN_POINT('Ctrl Pts',(-0.116404738713934,-1.2370442518095,
4.75122997535534)) ;
#73448=CARTESIAN_POINT('Ctrl Pts',(1.7786640216233E-12,-1.23704425180949,
4.76250000000022)) ;
#73449=CARTESIAN_POINT('Ctrl Pts',(8.09612793473136E-13,-1.23704425180949,
4.86171875000003)) ;
#73450=CARTESIAN_POINT('Ctrl Pts',(-0.137336915342943,-1.23704425180949,
4.8484221227521)) ;
#73451=CARTESIAN_POINT('Ctrl Pts',(-0.273837360267966,-1.21418534140677,
4.83428976615802)) ;
#73452=CARTESIAN_POINT('Ctrl Pts',(-0.560037656867374,-1.11530384903455,
4.80261508754638)) ;
#73453=CARTESIAN_POINT('Ctrl Pts',(-0.703789186902301,-1.03065804248177,
4.7853028491147)) ;
#73454=CARTESIAN_POINT('Ctrl Pts',(-0.945114351967411,-0.813865590204942,
4.75324427068868)) ;
#73455=CARTESIAN_POINT('Ctrl Pts',(-1.04192199729811,-0.685598645235772,
4.73748426662642)) ;
#73456=CARTESIAN_POINT('Ctrl Pts',(-1.18416571355528,-0.39406863303059,
4.70355461596626)) ;
#73457=CARTESIAN_POINT('Ctrl Pts',(-1.22615178933585,-0.232637942704037,
4.6862415138019)) ;
#73458=CARTESIAN_POINT('Ctrl Pts',(-1.24390083882174,0.0912513448628287,
4.65417154521747)) ;
#73459=CARTESIAN_POINT('Ctrl Pts',(-1.22185629281801,0.250421796258092,
4.63842693364645)) ;
#73460=CARTESIAN_POINT('Ctrl Pts',(-1.11669285766411,0.557251204171017,
4.60450306876804)) ;
#73461=CARTESIAN_POINT('Ctrl Pts',(-1.03242901230166,0.701179000912871,
4.58718908246915)) ;
#73462=CARTESIAN_POINT('Ctrl Pts',(-0.816291860310908,0.943017192844111,
4.5551071136332)) ;
#73463=CARTESIAN_POINT('Ctrl Pts',(-0.68828928793283,1.0401435395084,4.53937858989549)) ;
#73464=CARTESIAN_POINT('Ctrl Pts',(-0.397185174831524,1.18311822243788,
4.50546085968587)) ;
#73465=CARTESIAN_POINT('Ctrl Pts',(-0.23590859250982,1.22552088559737,4.48814597141756)) ;
#73466=CARTESIAN_POINT('Ctrl Pts',(0.0878738572500918,1.24414215332276,
4.45605136790905)) ;
#73467=CARTESIAN_POINT('Ctrl Pts',(0.247084876853158,1.22253285185974,4.44033963824566)) ;
#73468=CARTESIAN_POINT('Ctrl Pts',(0.554141397167057,1.11823283162416,4.40642841055572)) ;
#73469=CARTESIAN_POINT('Ctrl Pts',(0.69826448734219,1.03439511621537,4.38911260557476)) ;
#73470=CARTESIAN_POINT('Ctrl Pts',(0.94067327944826,0.818988981154981,4.35700470869683)) ;
#73471=CARTESIAN_POINT('Ctrl Pts',(1.03815462345547,0.691280851097263,4.34131048759468)) ;
#73472=CARTESIAN_POINT('Ctrl Pts',(1.18194231219858,0.400651824203295,4.30740614998345)) ;
#73473=CARTESIAN_POINT('Ctrl Pts',(1.22480819038543,0.23954806056204,4.29008941721771)) ;
#73474=CARTESIAN_POINT('Ctrl Pts',(1.24440011555374,-0.0841139884145471,
4.25796754419715)) ;
#73475=CARTESIAN_POINT('Ctrl Pts',(1.22327506160333,-0.243370178118099,
4.24229155132392)) ;
#73476=CARTESIAN_POINT('Ctrl Pts',(1.11993530837595,-0.550677908791383,
4.20839451179072)) ;
#73477=CARTESIAN_POINT('Ctrl Pts',(1.03657199420482,-0.695016737891022,
4.19107684447547)) ;
#73478=CARTESIAN_POINT('Ctrl Pts',(0.821979619332609,-0.938058608442367,
4.15894028882639)) ;
#73479=CARTESIAN_POINT('Ctrl Pts',(0.694598672019677,-1.03593448500254,
4.14328324552636)) ;
#73480=CARTESIAN_POINT('Ctrl Pts',(0.404498475654644,-1.18062421707747,
4.10939393322327)) ;
#73481=CARTESIAN_POINT('Ctrl Pts',(0.243588203023662,-1.22400387511481,
4.09207532959614)) ;
#73482=CARTESIAN_POINT('Ctrl Pts',(0.052584724229101,-1.23620676325144,
4.07309346146815)) ;
#73483=CARTESIAN_POINT('Ctrl Pts',(0.026281115687445,-1.23704425180951,
4.07051322391713)) ;
#73484=CARTESIAN_POINT('Ctrl Pts',(1.19550203070388E-12,-1.23704425180951,
4.06796875000008)) ;
#73485=CARTESIAN_POINT('Origin',(3.10601593664312E-15,-2.12330153459561E-14,
-0.34726562499997)) ;
#73486=CARTESIAN_POINT('',(8.58475084835609E-14,-1.23704425180953,3.17500000000004)) ;
#73487=CARTESIAN_POINT('',(8.50687621102125E-13,-1.23704425180953,3.27421875000013)) ;
#73488=CARTESIAN_POINT('',(6.06053764494801E-15,-1.23704425180962,-0.347265624999939)) ;
#73489=CARTESIAN_POINT('Ctrl Pts',(1.28647092978432E-13,-1.23704425180953,
3.17500000000004)) ;
#73490=CARTESIAN_POINT('Ctrl Pts',(0.0708155775454666,-1.23704425180953,
3.18185619256565)) ;
#73491=CARTESIAN_POINT('Ctrl Pts',(0.141641158011715,-1.23096580307423,
3.18895711854993)) ;
#73492=CARTESIAN_POINT('Ctrl Pts',(0.37265237290927,-1.19083439746923,3.21293246032262)) ;
#73493=CARTESIAN_POINT('Ctrl Pts',(0.526449006731497,-1.13128370789566,
3.23021084803643)) ;
#73494=CARTESIAN_POINT('Ctrl Pts',(0.798776567960535,-0.9579519766928,3.26352809136088)) ;
#73495=CARTESIAN_POINT('Ctrl Pts',(0.915468185958332,-0.847133187399626,
3.27852390399491)) ;
#73496=CARTESIAN_POINT('Ctrl Pts',(1.10267389299613,-0.584031316057481,
3.31150432856375)) ;
#73497=CARTESIAN_POINT('Ctrl Pts',(1.1700919079108,-0.433429567785851,3.32878889975524)) ;
#73498=CARTESIAN_POINT('Ctrl Pts',(1.24162311102855,-0.118621376363251,
3.3621364925631)) ;
#73499=CARTESIAN_POINT('Ctrl Pts',(1.24656360713669,0.0421759060016317,
3.37713911282345)) ;
#73500=CARTESIAN_POINT('Ctrl Pts',(1.19447652746202,0.360879175517894,3.41008404699193)) ;
#73501=CARTESIAN_POINT('Ctrl Pts',(1.136381222018,0.515401389867704,3.42737431816112)) ;
#73502=CARTESIAN_POINT('Ctrl Pts',(0.965654131201204,0.789427315205592,
3.46075153868974)) ;
#73503=CARTESIAN_POINT('Ctrl Pts',(0.856049877773158,0.907117744817803,
3.475763232627)) ;
#73504=CARTESIAN_POINT('Ctrl Pts',(0.594766231382718,1.09694412949167,3.5086727184997)) ;
#73505=CARTESIAN_POINT('Ctrl Pts',(0.444681672071364,1.16588309277448,3.52596821153494)) ;
#73506=CARTESIAN_POINT('Ctrl Pts',(0.13051322723977,1.24041746774059,3.55937430228894)) ;
#73507=CARTESIAN_POINT('Ctrl Pts',(-0.0301340284081215,1.24690081458028,
3.57439722434183)) ;
#73508=CARTESIAN_POINT('Ctrl Pts',(-0.349388372826032,1.19790902522301,
3.6072713813451)) ;
#73509=CARTESIAN_POINT('Ctrl Pts',(-0.504603592915391,1.14123807328055,
3.62457162658369)) ;
#73510=CARTESIAN_POINT('Ctrl Pts',(-0.780270998401231,0.973053725356881,
3.65800579923392)) ;
#73511=CARTESIAN_POINT('Ctrl Pts',(-0.898930809787884,0.864627154576215,
3.67304197956894)) ;
#73512=CARTESIAN_POINT('Ctrl Pts',(-1.09128935018277,0.605120146751677,
3.70588100303067)) ;
#73513=CARTESIAN_POINT('Ctrl Pts',(-1.16169940902439,0.455551501636983,
3.72318554207434)) ;
#73514=CARTESIAN_POINT('Ctrl Pts',(-1.23914333848065,0.142016544828403,
3.75664698236262)) ;
#73515=CARTESIAN_POINT('Ctrl Pts',(-1.24711798196723,-0.0184863590425373,
3.77169831613014)) ;
#73516=CARTESIAN_POINT('Ctrl Pts',(-1.20111976828371,-0.338257695483038,
3.80450247522439)) ;
#73517=CARTESIAN_POINT('Ctrl Pts',(-1.14583216279305,-0.494130023229818,
3.82181086347906)) ;
#73518=CARTESIAN_POINT('Ctrl Pts',(-0.980111709808021,-0.771372658155629,
3.85529873606951)) ;
#73519=CARTESIAN_POINT('Ctrl Pts',(-0.872819008504264,-0.890966611339828,
3.87036697465867)) ;
#73520=CARTESIAN_POINT('Ctrl Pts',(-0.615034927641384,-1.08575441832947,
3.90313660975835)) ;
#73521=CARTESIAN_POINT('Ctrl Pts',(-0.465976295817607,-1.15757703751633,
3.92044841867519)) ;
#73522=CARTESIAN_POINT('Ctrl Pts',(-0.206659226669885,-1.2240756405299,
3.94822167239887)) ;
#73523=CARTESIAN_POINT('Ctrl Pts',(-0.103453804072554,-1.23704425180952,
3.95873385345504)) ;
#73524=CARTESIAN_POINT('Ctrl Pts',(1.01420608022984E-12,-1.23704425180951,
3.96875000000014)) ;
#73525=CARTESIAN_POINT('Ctrl Pts',(1.19626530903361E-12,-1.23704425180951,
4.06796875000008)) ;
#73526=CARTESIAN_POINT('Ctrl Pts',(-0.132492712536078,-1.23704425180951,
4.05514112672582)) ;
#73527=CARTESIAN_POINT('Ctrl Pts',(-0.264250786478305,-1.2157711313891,
4.04153151017354)) ;
#73528=CARTESIAN_POINT('Ctrl Pts',(-0.546829425379681,-1.1218114770952,
4.01040485290746)) ;
#73529=CARTESIAN_POINT('Ctrl Pts',(-0.691405803061307,-1.03897506036924,
3.99308531696321)) ;
#73530=CARTESIAN_POINT('Ctrl Pts',(-0.935148161467304,-0.825286427283299,
3.9609171846732)) ;
#73531=CARTESIAN_POINT('Ctrl Pts',(-1.03346140934947,-0.698268122235989,
3.94530019093328)) ;
#73532=CARTESIAN_POINT('Ctrl Pts',(-1.17914926345779,-0.408755192718701,
3.9114277085422)) ;
#73533=CARTESIAN_POINT('Ctrl Pts',(-1.22309721265908,-0.248061163883425,
3.89410725084768)) ;
#73534=CARTESIAN_POINT('Ctrl Pts',(-1.24496001774116,0.075313000626321,
3.8619221806586)) ;
#73535=CARTESIAN_POINT('Ctrl Pts',(-1.22496742029096,0.234674977830744,
3.84632626845864)) ;
#73536=CARTESIAN_POINT('Ctrl Pts',(-1.1238718134627,0.542564131407952,3.81246293431581)) ;
#73537=CARTESIAN_POINT('Ctrl Pts',(-1.04161906937166,0.687401129125714,
3.79514157288443)) ;
#73538=CARTESIAN_POINT('Ctrl Pts',(-0.828931494713476,0.931916231594316,
3.76293877098675)) ;
#73539=CARTESIAN_POINT('Ctrl Pts',(-0.702314007776924,1.03071299719022,
3.74736462375802)) ;
#73540=CARTESIAN_POINT('Ctrl Pts',(-0.41345153282745,1.17750198072219,3.71351095803971)) ;
#73541=CARTESIAN_POINT('Ctrl Pts',(-0.252998681415089,1.22207659623042,
3.69618871926384)) ;
#73542=CARTESIAN_POINT('Ctrl Pts',(0.0702044827112899,1.24525680135152,
3.66396737302194)) ;
#73543=CARTESIAN_POINT('Ctrl Pts',(0.22962791148717,1.22592090736459,3.64841565102641)) ;
#73544=CARTESIAN_POINT('Ctrl Pts',(0.537850340219543,1.12612564725782,3.61457219799452)) ;
#73545=CARTESIAN_POINT('Ctrl Pts',(0.682972132674095,1.04451759575679,3.59724911763267)) ;
#73546=CARTESIAN_POINT('Ctrl Pts',(0.928336862229866,0.83293567962328,3.5650083972929)) ;
#73547=CARTESIAN_POINT('Ctrl Pts',(1.02766652798706,0.706759836179155,3.54947973110837)) ;
#73548=CARTESIAN_POINT('Ctrl Pts',(1.17566627400191,0.418615717276284,3.51564705948802)) ;
#73549=CARTESIAN_POINT('Ctrl Pts',(1.22092959963284,0.258431230748975,3.49832318370233)) ;
#73550=CARTESIAN_POINT('Ctrl Pts',(1.24555959704839,-0.0645803549285124,
3.46606224437914)) ;
#73551=CARTESIAN_POINT('Ctrl Pts',(1.22694620073508,-0.224071489051609,
3.45055722787517)) ;
#73552=CARTESIAN_POINT('Ctrl Pts',(1.12858066702693,-0.532657284147546,
3.41673593112935)) ;
#73553=CARTESIAN_POINT('Ctrl Pts',(1.04768242874002,-0.678088926833233,
3.39941131756716)) ;
#73554=CARTESIAN_POINT('Ctrl Pts',(0.837317818847695,-0.924384412258899,
3.36712930151868)) ;
#73555=CARTESIAN_POINT('Ctrl Pts',(0.711626949645792,-1.02429943344021,
3.35164848434463)) ;
#73556=CARTESIAN_POINT('Ctrl Pts',(0.424273643956393,-1.17362567149252,
3.31783918082949)) ;
#73557=CARTESIAN_POINT('Ctrl Pts',(0.264386998566793,-1.21964309144324,
3.30051389974086)) ;
#73558=CARTESIAN_POINT('Ctrl Pts',(0.0667888724753224,-1.23569338185853,
3.28073926088402)) ;
#73559=CARTESIAN_POINT('Ctrl Pts',(0.0333785908521117,-1.23704425180953,
3.27745038425878)) ;
#73560=CARTESIAN_POINT('Ctrl Pts',(1.65728542000869E-12,-1.23704425180953,
3.27421875000013)) ;
#73561=CARTESIAN_POINT('Origin',(3.10601593664312E-15,-2.12330153459561E-14,
-0.34726562499997)) ;
#73562=CARTESIAN_POINT('',(-3.53216841023252E-15,-1.23704425180955,2.38125000000001)) ;
#73563=CARTESIAN_POINT('',(9.61945429429848E-13,-1.23704425180955,2.48046875000017)) ;
#73564=CARTESIAN_POINT('',(6.06053764494801E-15,-1.23704425180962,-0.347265624999939)) ;
#73565=CARTESIAN_POINT('Ctrl Pts',(-4.17770751542265E-14,-1.23704425180955,
2.38125000000001)) ;
#73566=CARTESIAN_POINT('Ctrl Pts',(0.087742059255656,-1.23704425180956,
2.38974497349614)) ;
#73567=CARTESIAN_POINT('Ctrl Pts',(0.175397924138452,-1.22771444679764,
2.39860575646061)) ;
#73568=CARTESIAN_POINT('Ctrl Pts',(0.421086846657427,-1.17456748660854,
2.42452412308534)) ;
#73569=CARTESIAN_POINT('Ctrl Pts',(0.572236413054084,-1.1088156553442,2.44179491348184)) ;
#73570=CARTESIAN_POINT('Ctrl Pts',(0.837308815849046,-0.924484441545288,
2.47485084388711)) ;
#73571=CARTESIAN_POINT('Ctrl Pts',(0.949454964634233,-0.808883391388236,
2.48984013351775)) ;
#73572=CARTESIAN_POINT('Ctrl Pts',(1.12561252818267,-0.538418100523992,
2.52309040112664)) ;
#73573=CARTESIAN_POINT('Ctrl Pts',(1.18673778075662,-0.385426693580367,
2.54035397366693)) ;
#73574=CARTESIAN_POINT('Ctrl Pts',(1.24545581479387,-0.06796089209204,2.57344502135837)) ;
#73575=CARTESIAN_POINT('Ctrl Pts',(1.24382461226767,0.0931604792678681,
2.58843515795435)) ;
#73576=CARTESIAN_POINT('Ctrl Pts',(1.17870954711358,0.409287181349732,2.6216530984053)) ;
#73577=CARTESIAN_POINT('Ctrl Pts',(1.11454847343287,0.560941616284452,2.63890897455499)) ;
#73578=CARTESIAN_POINT('Ctrl Pts',(0.93296551076449,0.827874944272307,2.67203486169088)) ;
#73579=CARTESIAN_POINT('Ctrl Pts',(0.818402498915292,0.941285688546151,
2.68702840287109)) ;
#73580=CARTESIAN_POINT('Ctrl Pts',(0.549717127143605,1.12011507343048,2.7202134914879)) ;
#73581=CARTESIAN_POINT('Ctrl Pts',(0.397504367741431,1.18272460810127,2.73746120165276)) ;
#73582=CARTESIAN_POINT('Ctrl Pts',(0.0806781569248627,1.24471548612111,
2.77062157708896)) ;
#73583=CARTESIAN_POINT('Ctrl Pts',(-0.0806045211311646,1.24472025715767,
2.78562110233823)) ;
#73584=CARTESIAN_POINT('Ctrl Pts',(-0.397356001307769,1.182763456008,2.81877287594506)) ;
#73585=CARTESIAN_POINT('Ctrl Pts',(-0.549502376681443,1.12020880515138,
2.8360119579552)) ;
#73586=CARTESIAN_POINT('Ctrl Pts',(-0.818295898471779,0.941404839217002,
2.86920649801463)) ;
#73587=CARTESIAN_POINT('Ctrl Pts',(-0.932980086154937,0.827888629057569,
2.88421439790037)) ;
#73588=CARTESIAN_POINT('Ctrl Pts',(-1.11448302604523,0.561002038877481,
2.9173325508293)) ;
#73589=CARTESIAN_POINT('Ctrl Pts',(-1.1785728542988,0.409585276593328,2.93456255892281)) ;
#73590=CARTESIAN_POINT('Ctrl Pts',(-1.2438453660056,0.0934176447806062,
2.96779077619432)) ;
#73591=CARTESIAN_POINT('Ctrl Pts',(-1.24549236720236,-0.0680239283704382,
2.98280961579441)) ;
#73592=CARTESIAN_POINT('Ctrl Pts',(-1.18669605779163,-0.385386507512381,
3.01589380883778)) ;
#73593=CARTESIAN_POINT('Ctrl Pts',(-1.12575095674432,-0.538007783822041,
3.03311432158302)) ;
#73594=CARTESIAN_POINT('Ctrl Pts',(-0.949994588684741,-0.808247851089063,
3.06632669438506)) ;
#73595=CARTESIAN_POINT('Ctrl Pts',(-0.837932363556729,-0.923917822393809,
3.08131606252068)) ;
#73596=CARTESIAN_POINT('Ctrl Pts',(-0.57298402990398,-1.1084310914558,3.11436728184243)) ;
#73597=CARTESIAN_POINT('Ctrl Pts',(-0.421868558518369,-1.17428838114891,
3.13163900045812)) ;
#73598=CARTESIAN_POINT('Ctrl Pts',(-0.175938483935532,-1.22765667322761,
3.1575895909478)) ;
#73599=CARTESIAN_POINT('Ctrl Pts',(-0.0880134335085121,-1.23704425180953,
3.16647875270654)) ;
#73600=CARTESIAN_POINT('Ctrl Pts',(1.28647092978432E-13,-1.23704425180953,
3.17500000000004)) ;
#73601=CARTESIAN_POINT('Ctrl Pts',(1.65839564303383E-12,-1.23704425180953,
3.27421875000013)) ;
#73602=CARTESIAN_POINT('Ctrl Pts',(-0.125259306880064,-1.23704425180953,
3.26209144752812)) ;
#73603=CARTESIAN_POINT('Ctrl Pts',(-0.249926036900973,-1.21803207403063,
3.24925906863424)) ;
#73604=CARTESIAN_POINT('Ctrl Pts',(-0.526956071082114,-1.1312423725868,
3.21895715154446)) ;
#73605=CARTESIAN_POINT('Ctrl Pts',(-0.672723207759457,-1.05112289247697,
3.2016312869256)) ;
#73606=CARTESIAN_POINT('Ctrl Pts',(-0.920034257456585,-0.842093826970192,
3.16930450594698)) ;
#73607=CARTESIAN_POINT('Ctrl Pts',(-1.02058989133647,-0.716933533450121,
3.15387351926058)) ;
#73608=CARTESIAN_POINT('Ctrl Pts',(-1.17136365853769,-0.430447751260752,
3.12009015678486)) ;
#73609=CARTESIAN_POINT('Ctrl Pts',(-1.21820341668262,-0.270890696784831,
3.10276380753511)) ;
#73610=CARTESIAN_POINT('Ctrl Pts',(-1.24615994228965,0.0516678432709414,
3.07041332672158)) ;
#73611=CARTESIAN_POINT('Ctrl Pts',(-1.22920362688226,0.211314677528755,
3.05500784135146)) ;
#73612=CARTESIAN_POINT('Ctrl Pts',(-1.13411349407752,0.520720804939624,
3.0212384759232)) ;
#73613=CARTESIAN_POINT('Ctrl Pts',(-1.05484511114142,0.666849301455023,
3.00391175700099)) ;
#73614=CARTESIAN_POINT('Ctrl Pts',(-0.847275704032822,0.915263631919053,
2.971536695957)) ;
#73615=CARTESIAN_POINT('Ctrl Pts',(-0.722693521263278,1.01651754484435,
2.95615700125366)) ;
#73616=CARTESIAN_POINT('Ctrl Pts',(-0.437155755641923,1.16886410870982,
2.92240234933873)) ;
#73617=CARTESIAN_POINT('Ctrl Pts',(-0.277962236505721,1.21659665948755,
2.90507539289976)) ;
#73618=CARTESIAN_POINT('Ctrl Pts',(0.0443306516715813,1.24644225330239,
2.87267487426566)) ;
#73619=CARTESIAN_POINT('Ctrl Pts',(0.204066149164751,1.23042661911412,2.85732117214245)) ;
#73620=CARTESIAN_POINT('Ctrl Pts',(0.513929854356582,1.13719340528694,2.82358197344859)) ;
#73621=CARTESIAN_POINT('Ctrl Pts',(0.660445358989949,1.05885124898515,2.80625492994689)) ;
#73622=CARTESIAN_POINT('Ctrl Pts',(0.912420921808995,0.850916104331233,
2.77352041178961)) ;
#73623=CARTESIAN_POINT('Ctrl Pts',(1.0159735026812,0.724138380107633,2.75788120679066)) ;
#73624=CARTESIAN_POINT('Ctrl Pts',(1.16792566570418,0.438487516909866,2.72413142175986)) ;
#73625=CARTESIAN_POINT('Ctrl Pts',(1.21512293691003,0.282521136875137,2.70713837550492)) ;
#73626=CARTESIAN_POINT('Ctrl Pts',(1.24699068652411,-0.0393940197984395,
2.67469333309582)) ;
#73627=CARTESIAN_POINT('Ctrl Pts',(1.23111986905087,-0.202210012834243,
2.65909118027089)) ;
#73628=CARTESIAN_POINT('Ctrl Pts',(1.13766332112956,-0.511919195941446,
2.62535798562932)) ;
#73629=CARTESIAN_POINT('Ctrl Pts',(1.06121309629516,-0.655885259419098,
2.60835364525798)) ;
#73630=CARTESIAN_POINT('Ctrl Pts',(0.85698298817807,-0.906688869553548,
2.57588117636637)) ;
#73631=CARTESIAN_POINT('Ctrl Pts',(0.731074505423473,-1.01096042603533,
2.56031628581112)) ;
#73632=CARTESIAN_POINT('Ctrl Pts',(0.446585037301406,-1.16486864609059,
2.5266005001818)) ;
#73633=CARTESIAN_POINT('Ctrl Pts',(0.29084157916395,-1.21317239258132,2.50958466353687)) ;
#73634=CARTESIAN_POINT('Ctrl Pts',(0.0868667757727215,-1.23475935950554,
2.48897061205492)) ;
#73635=CARTESIAN_POINT('Ctrl Pts',(0.0434117617253601,-1.23704425180955,
2.484671771543)) ;
#73636=CARTESIAN_POINT('Ctrl Pts',(1.88813622231907E-12,-1.23704425180955,
2.48046875000017)) ;
#73637=CARTESIAN_POINT('Origin',(3.10601593664312E-15,-2.12330153459561E-14,
-0.34726562499997)) ;
#73638=CARTESIAN_POINT('',(-4.44768360959499E-13,-1.23704425180957,1.58749999999992)) ;
#73639=CARTESIAN_POINT('',(5.0368059013805E-13,-1.23704425180957,1.68671875000009)) ;
#73640=CARTESIAN_POINT('',(6.06053764494801E-15,-1.23704425180962,-0.347265624999939)) ;
#73641=CARTESIAN_POINT('Ctrl Pts',(-9.15951342550514E-13,-1.23704425180957,
1.58749999999992)) ;
#73642=CARTESIAN_POINT('Ctrl Pts',(0.103213138457939,-1.23704425180965,
1.5974928458836)) ;
#73643=CARTESIAN_POINT('Ctrl Pts',(0.20618093125318,-1.22413589226724,1.6079796039136)) ;
#73644=CARTESIAN_POINT('Ctrl Pts',(0.465294526843657,-1.15784994931821,
1.63572462948155)) ;
#73645=CARTESIAN_POINT('Ctrl Pts',(0.614386971854366,-1.08611976088681,
1.65303600534444)) ;
#73646=CARTESIAN_POINT('Ctrl Pts',(0.872284307129058,-0.891490854380605,
1.68581023305133)) ;
#73647=CARTESIAN_POINT('Ctrl Pts',(0.979651300418265,-0.771958131624264,
1.70087611594015)) ;
#73648=CARTESIAN_POINT('Ctrl Pts',(1.1455336587961,-0.494818547234572,1.73436050434422)) ;
#73649=CARTESIAN_POINT('Ctrl Pts',(1.20091225741019,-0.338988964280692,
1.75166840326281)) ;
#73650=CARTESIAN_POINT('Ctrl Pts',(1.24710701030825,-0.019251089994797,
1.78447720447454)) ;
#73651=CARTESIAN_POINT('Ctrl Pts',(1.23923025432837,0.141261268995484,1.79952640806237)) ;
#73652=CARTESIAN_POINT('Ctrl Pts',(1.16197750256199,0.454838262952741,1.8329842514573)) ;
#73653=CARTESIAN_POINT('Ctrl Pts',(1.09166402678993,0.604441255179057,1.85028824261942)) ;
#73654=CARTESIAN_POINT('Ctrl Pts',(0.899471659306014,0.864065455998327,
1.88313194836513)) ;
#73655=CARTESIAN_POINT('Ctrl Pts',(0.780875597126371,0.972569441935872,
1.89816624369074)) ;
#73656=CARTESIAN_POINT('Ctrl Pts',(0.505315928503476,1.14092145152737,1.93159670928056)) ;
#73657=CARTESIAN_POINT('Ctrl Pts',(0.350145937766151,1.19768642569191,1.94889634611048)) ;
#73658=CARTESIAN_POINT('Ctrl Pts',(0.0309273791243574,1.24688212451289,
1.98177521583409)) ;
#73659=CARTESIAN_POINT('Ctrl Pts',(-0.129729735598369,1.24050038649072,
1.996796516646)) ;
#73660=CARTESIAN_POINT('Ctrl Pts',(-0.443940802185009,1.16616401538692,
2.03019879335581)) ;
#73661=CARTESIAN_POINT('Ctrl Pts',(-0.594059940236127,1.09732525431576,
2.04749361579619)) ;
#73662=CARTESIAN_POINT('Ctrl Pts',(-0.855463952527125,0.907671435081854,
2.08040783478537)) ;
#73663=CARTESIAN_POINT('Ctrl Pts',(-0.965148313080044,0.7900469122298,2.09541818852656)) ;
#73664=CARTESIAN_POINT('Ctrl Pts',(-1.13604775318347,0.516132835806172,
2.12879149186426)) ;
#73665=CARTESIAN_POINT('Ctrl Pts',(-1.19423947770742,0.361658141632641,
2.14608102895431)) ;
#73666=CARTESIAN_POINT('Ctrl Pts',(-1.24653657779848,0.0429928738521064,
2.17903070636778)) ;
#73667=CARTESIAN_POINT('Ctrl Pts',(-1.24170080478482,-0.117814616829579,
2.1940322831697)) ;
#73668=CARTESIAN_POINT('Ctrl Pts',(-1.17037318110268,-0.432665655153667,
2.22737586013345)) ;
#73669=CARTESIAN_POINT('Ctrl Pts',(-1.10305835532869,-0.5833018986499,2.24465963285908)) ;
#73670=CARTESIAN_POINT('Ctrl Pts',(-0.916030557171499,-0.846526450950797,
2.27764480039392)) ;
#73671=CARTESIAN_POINT('Ctrl Pts',(-0.799406585624652,-0.957427536954876,
2.29263988016888)) ;
#73672=CARTESIAN_POINT('Ctrl Pts',(-0.527194302150408,-1.13093510371108,
2.32595301414067)) ;
#73673=CARTESIAN_POINT('Ctrl Pts',(-0.373447225065235,-1.19058390611551,
2.3432305385252)) ;
#73674=CARTESIAN_POINT('Ctrl Pts',(-0.142197606895638,-1.23091787788555,
2.36723708546675)) ;
#73675=CARTESIAN_POINT('Ctrl Pts',(-0.0710943025950748,-1.23704425180955,
2.3743668219507)) ;
#73676=CARTESIAN_POINT('Ctrl Pts',(-4.17770751542265E-14,-1.23704425180955,
2.38125000000001)) ;
#73677=CARTESIAN_POINT('Ctrl Pts',(1.88718832228041E-12,-1.23704425180955,
2.48046875000017)) ;
#73678=CARTESIAN_POINT('Ctrl Pts',(-0.117854422562485,-1.23704425180955,
2.4690583704788)) ;
#73679=CARTESIAN_POINT('Ctrl Pts',(-0.235259954172443,-1.22021429663736,
2.45701651722142)) ;
#73680=CARTESIAN_POINT('Ctrl Pts',(-0.503742565535835,-1.14132347646503,
2.42785891093527)) ;
#73681=CARTESIAN_POINT('Ctrl Pts',(-0.648352051565075,-1.06584880147738,
2.41083139857694)) ;
#73682=CARTESIAN_POINT('Ctrl Pts',(-0.9005016509573,-0.863442817047236,
2.37830176737945)) ;
#73683=CARTESIAN_POINT('Ctrl Pts',(-1.00554098541687,-0.738463663602721,
2.36281152285193)) ;
#73684=CARTESIAN_POINT('Ctrl Pts',(-1.16153599988668,-0.45522443795177,
2.32913309563231)) ;
#73685=CARTESIAN_POINT('Ctrl Pts',(-1.21102257045409,-0.299728136240724,
2.31209375309849)) ;
#73686=CARTESIAN_POINT('Ctrl Pts',(-1.24737301964058,0.0215105103391086,
2.27953443836968)) ;
#73687=CARTESIAN_POINT('Ctrl Pts',(-1.23390184302536,0.184098066882936,
2.26408130090388)) ;
#73688=CARTESIAN_POINT('Ctrl Pts',(-1.14516389803635,0.494989647801575,
2.23042286022801)) ;
#73689=CARTESIAN_POINT('Ctrl Pts',(-1.07073590685864,0.640278380071665,
2.21337156021615)) ;
#73690=CARTESIAN_POINT('Ctrl Pts',(-0.870280527286828,0.893856283492051,
2.18078186949001)) ;
#73691=CARTESIAN_POINT('Ctrl Pts',(-0.746289475136698,0.999711062990307,
2.16536549722697)) ;
#73692=CARTESIAN_POINT('Ctrl Pts',(-0.464389285401086,1.15791979132683,
2.13172793531287)) ;
#73693=CARTESIAN_POINT('Ctrl Pts',(-0.309165785841783,1.20866374621666,
2.11466457974615)) ;
#73694=CARTESIAN_POINT('Ctrl Pts',(0.011687544531865,1.24747565459223,2.08204385812378)) ;
#73695=CARTESIAN_POINT('Ctrl Pts',(0.174149188670792,1.2353163190968,2.06666375212741)) ;
#73696=CARTESIAN_POINT('Ctrl Pts',(0.485671507308586,1.14916490674463,2.03304797306873)) ;
#73697=CARTESIAN_POINT('Ctrl Pts',(0.631672625126814,1.0758538699623,2.01597249500797)) ;
#73698=CARTESIAN_POINT('Ctrl Pts',(0.886757111752249,0.877472869550115,
1.98332012969277)) ;
#73699=CARTESIAN_POINT('Ctrl Pts',(0.993472981931957,0.754526248933447,
1.96797562842022)) ;
#73700=CARTESIAN_POINT('Ctrl Pts',(1.15401598399901,0.474052350699193,1.93438254485527)) ;
#73701=CARTESIAN_POINT('Ctrl Pts',(1.2060886249513,0.319128439609208,1.91729491021741)) ;
#73702=CARTESIAN_POINT('Ctrl Pts',(1.24750140441329,-0.00130710008280192,
1.8846103349448)) ;
#73703=CARTESIAN_POINT('Ctrl Pts',(1.2367238774351,-0.163635493877063,1.86930061010034)) ;
#73704=CARTESIAN_POINT('Ctrl Pts',(1.15330201587322,-0.47581012292618,1.83573113952197)) ;
#73705=CARTESIAN_POINT('Ctrl Pts',(1.08117603828055,-0.622553229007982,
1.81863134856616)) ;
#73706=CARTESIAN_POINT('Ctrl Pts',(0.884988109592906,-0.879216813977091,
1.78591404786803)) ;
#73707=CARTESIAN_POINT('Ctrl Pts',(0.763138611287406,-0.986836462633585,
1.77063810181685)) ;
#73708=CARTESIAN_POINT('Ctrl Pts',(0.484175066543603,-1.14982526943159,
1.73709316253432)) ;
#73709=CARTESIAN_POINT('Ctrl Pts',(0.329578303643328,-1.20329307532079,
1.71998125107816)) ;
#73710=CARTESIAN_POINT('Ctrl Pts',(0.112914723118742,-1.23318313648863,
1.6978057226914)) ;
#73711=CARTESIAN_POINT('Ctrl Pts',(0.0564359310574075,-1.23704425180957,
1.69218274004799)) ;
#73712=CARTESIAN_POINT('Ctrl Pts',(9.799417293904E-13,-1.23704425180957,
1.68671875000009)) ;
#73713=CARTESIAN_POINT('Origin',(3.10601593664312E-15,-2.12330153459561E-14,
-0.34726562499997)) ;
#73714=CARTESIAN_POINT('',(-8.39648792932172E-13,-1.23704425180959,0.793749999999827)) ;
#73715=CARTESIAN_POINT('',(5.29840382873746E-14,-1.23704425180959,0.892968750000012)) ;
#73716=CARTESIAN_POINT('',(6.06053764494801E-15,-1.23704425180962,-0.347265624999939)) ;
#73717=CARTESIAN_POINT('Ctrl Pts',(-1.69756569912138E-12,-1.23704425180959,
0.793749999999827)) ;
#73718=CARTESIAN_POINT('Ctrl Pts',(0.1162135096242,-1.23704425180975,0.805001510307853)) ;
#73719=CARTESIAN_POINT('Ctrl Pts',(0.231993391524348,-1.22067968586107,
0.816867308523916)) ;
#73720=CARTESIAN_POINT('Ctrl Pts',(0.501851918951939,-1.1425510323291,0.846127562382746)) ;
#73721=CARTESIAN_POINT('Ctrl Pts',(0.64903902066643,-1.06585436358931,0.863453639046213)) ;
#73722=CARTESIAN_POINT('Ctrl Pts',(0.900745927932724,-0.862696502043695,
0.895970562508104)) ;
#73723=CARTESIAN_POINT('Ctrl Pts',(1.00409892292396,-0.739850629398905,
0.911215113226969)) ;
#73724=CARTESIAN_POINT('Ctrl Pts',(1.16114120635477,-0.457177214677076,
0.944880758791297)) ;
#73725=CARTESIAN_POINT('Ctrl Pts',(1.21153440255779,-0.299102787427825,
0.962206067737137)) ;
#73726=CARTESIAN_POINT('Ctrl Pts',(1.24703303565389,0.0223587230185338,
0.994752799094146)) ;
#73727=CARTESIAN_POINT('Ctrl Pts',(1.23383148384927,0.182360771507888,1.0099720699921)) ;
#73728=CARTESIAN_POINT('Ctrl Pts',(1.14614189822723,0.493558250385675,1.04361808445064)) ;
#73729=CARTESIAN_POINT('Ctrl Pts',(1.07057380233359,0.641194275551678,1.06094236546491)) ;
#73730=CARTESIAN_POINT('Ctrl Pts',(0.869352688423176,0.894327003201699,
1.09351966371337)) ;
#73731=CARTESIAN_POINT('Ctrl Pts',(0.747264072761988,0.998596405999818,
1.1087141933317)) ;
#73732=CARTESIAN_POINT('Ctrl Pts',(0.465847736088978,1.15767326019276,1.14233972434915)) ;
#73733=CARTESIAN_POINT('Ctrl Pts',(0.308273942622746,1.20921677031023,1.15966269436063)) ;
#73734=CARTESIAN_POINT('Ctrl Pts',(-0.0128093674351517,1.24717088191047,
1.1922712817031)) ;
#73735=CARTESIAN_POINT('Ctrl Pts',(-0.172927832847755,1.23519149091611,
1.20744175516426)) ;
#73736=CARTESIAN_POINT('Ctrl Pts',(-0.484688169925139,1.14990381148094,
1.24104594017786)) ;
#73737=CARTESIAN_POINT('Ctrl Pts',(-0.632793413025101,1.07554152064093,
1.25836729315049)) ;
#73738=CARTESIAN_POINT('Ctrl Pts',(-0.887436959175382,0.876390450413255,
1.29100784990532)) ;
#73739=CARTESIAN_POINT('Ctrl Pts',(-0.992682559954528,0.755107952134886,
1.30615510407062)) ;
#73740=CARTESIAN_POINT('Ctrl Pts',(-1.15391618506924,0.475034915683939,
1.33973707333109)) ;
#73741=CARTESIAN_POINT('Ctrl Pts',(-1.20667728664983,0.31800226565451,1.35705648040355)) ;
#73742=CARTESIAN_POINT('Ctrl Pts',(-1.24723842912681,-0.00266812435902711,
1.38972963998657)) ;
#73743=CARTESIAN_POINT('Ctrl Pts',(-1.23655669159541,-0.162910653688068,
1.4048546673072)) ;
#73744=CARTESIAN_POINT('Ctrl Pts',(-1.15381523882729,-0.47525772953329,
1.43841354722827)) ;
#73745=CARTESIAN_POINT('Ctrl Pts',(-1.08073357594365,-0.623849600619874,
1.45573065712404)) ;
#73746=CARTESIAN_POINT('Ctrl Pts',(-0.883782048240159,-0.880083724520226,
1.48843700117062)) ;
#73747=CARTESIAN_POINT('Ctrl Pts',(-0.763352513880301,-0.986363018669953,
1.50354095205518)) ;
#73748=CARTESIAN_POINT('Ctrl Pts',(-0.484706471672932,-1.14986842699004,
1.53707586886158)) ;
#73749=CARTESIAN_POINT('Ctrl Pts',(-0.328255474692753,-1.20390989906769,
1.55439030858974)) ;
#73750=CARTESIAN_POINT('Ctrl Pts',(-0.11073495251392,-1.23333072827733,
1.57662998630918)) ;
#73751=CARTESIAN_POINT('Ctrl Pts',(-0.0553466012557314,-1.23704425180953,
1.58214147622296)) ;
#73752=CARTESIAN_POINT('Ctrl Pts',(-9.1591427459783E-13,-1.23704425180957,
1.58749999999992)) ;
#73753=CARTESIAN_POINT('Ctrl Pts',(9.77854949790746E-13,-1.23704425180957,
1.68671875000009)) ;
#73754=CARTESIAN_POINT('Ctrl Pts',(-0.10386256664325,-1.23704425180957,
1.67666302805362)) ;
#73755=CARTESIAN_POINT('Ctrl Pts',(-0.207478531013762,-1.22397292284966,
1.66610698003369)) ;
#73756=CARTESIAN_POINT('Ctrl Pts',(-0.465439188933171,-1.15754626523678,
1.63846793599463)) ;
#73757=CARTESIAN_POINT('Ctrl Pts',(-0.612949519067283,-1.08666986668399,
1.6213439763253)) ;
#73758=CARTESIAN_POINT('Ctrl Pts',(-0.871257204810473,-0.892786088060061,
1.58855990145816)) ;
#73759=CARTESIAN_POINT('Ctrl Pts',(-0.979819407915098,-0.772081537314303,
1.57334784025726)) ;
#73760=CARTESIAN_POINT('Ctrl Pts',(-1.14535382711181,-0.494707432630223,
1.53985469962491)) ;
#73761=CARTESIAN_POINT('Ctrl Pts',(-1.20027685322434,-0.340465686100379,
1.52271880107381)) ;
#73762=CARTESIAN_POINT('Ctrl Pts',(-1.24726986798919,-0.0209634197422772,
1.48990079803262)) ;
#73763=CARTESIAN_POINT('Ctrl Pts',(-1.23944258399302,0.141078963361431,
1.47471850741457)) ;
#73764=CARTESIAN_POINT('Ctrl Pts',(-1.16186482936867,0.454604495748239,
1.4412526127647)) ;
#73765=CARTESIAN_POINT('Ctrl Pts',(-1.09229745619761,0.602902154226948,
1.42410492191876)) ;
#73766=CARTESIAN_POINT('Ctrl Pts',(-0.900818692585104,0.862909739124637,
1.39125271562109)) ;
#73767=CARTESIAN_POINT('Ctrl Pts',(-0.781300846944657,0.972448427893816,
1.37609853100886)) ;
#73768=CARTESIAN_POINT('Ctrl Pts',(-0.505588448131426,1.14061394427051,
1.34266075741807)) ;
#73769=CARTESIAN_POINT('Ctrl Pts',(-0.351729338343704,1.19704425540707,
1.32550145794681)) ;
#73770=CARTESIAN_POINT('Ctrl Pts',(-0.0327411096781994,1.24698920659493,
1.29261484083076)) ;
#73771=CARTESIAN_POINT('Ctrl Pts',(0.129150239315594,1.24071495015846,1.27748694345738)) ;
#73772=CARTESIAN_POINT('Ctrl Pts',(0.443363792513356,1.16622189220983,1.24407814236331)) ;
#73773=CARTESIAN_POINT('Ctrl Pts',(0.592463098666166,1.09801641980495,1.22690745444761)) ;
#73774=CARTESIAN_POINT('Ctrl Pts',(0.854215627606005,0.909030767087041,
1.19398628850527)) ;
#73775=CARTESIAN_POINT('Ctrl Pts',(0.964759018890449,0.790734196106168,
1.17888271455525)) ;
#73776=CARTESIAN_POINT('Ctrl Pts',(1.13562442012412,0.516747116745544,1.14550370831607)) ;
#73777=CARTESIAN_POINT('Ctrl Pts',(1.19360463581005,0.363297383936295,1.12832188767215)) ;
#73778=CARTESIAN_POINT('Ctrl Pts',(1.2465863443891,0.04485264056338,1.09536610593822)) ;
#73779=CARTESIAN_POINT('Ctrl Pts',(1.2419044748859,-0.116883762470755,1.0802847577046)) ;
#73780=CARTESIAN_POINT('Ctrl Pts',(1.1705797531155,-0.431786062192727,1.0469363341123)) ;
#73781=CARTESIAN_POINT('Ctrl Pts',(1.10378105038461,-0.581695050705877,
1.02974367061268)) ;
#73782=CARTESIAN_POINT('Ctrl Pts',(0.917361446453772,-0.845225492784956,
0.996753278077057)) ;
#73783=CARTESIAN_POINT('Ctrl Pts',(0.800312552818451,-0.956795325894941,
0.981691937034111)) ;
#73784=CARTESIAN_POINT('Ctrl Pts',(0.528104024710194,-1.13041068455493,
0.948374843852459)) ;
#73785=CARTESIAN_POINT('Ctrl Pts',(0.375088845060119,-1.18997271695152,
0.931171659754383)) ;
#73786=CARTESIAN_POINT('Ctrl Pts',(0.143803632792016,-1.23077857977579,
0.907142742359252)) ;
#73787=CARTESIAN_POINT('Ctrl Pts',(0.0718982454565328,-1.23704425180959,
0.899929763848464)) ;
#73788=CARTESIAN_POINT('Ctrl Pts',(8.68838113439773E-14,-1.23704425180959,
0.892968750000012)) ;
#73789=CARTESIAN_POINT('Origin',(3.10601593664312E-15,-2.12330153459561E-14,
-0.34726562499997)) ;
#73790=CARTESIAN_POINT('',(1.05447087183509E-14,-1.23704425180961,0.079756751809301)) ;
#73791=CARTESIAN_POINT('',(-7.25126625797582E-14,-1.23704425180961,0.0992187500000007)) ;
#73792=CARTESIAN_POINT('',(6.06053764494801E-15,-1.23704425180962,-0.347265624999939)) ;
#73793=CARTESIAN_POINT('',(0.726199640324295,-1.00145522282725,0.0797567518095777)) ;
#73794=CARTESIAN_POINT('Origin',(-2.4980018054066E-14,3.26683124995952E-13,
0.0797567518098535)) ;
#73795=CARTESIAN_POINT('Ctrl Pts',(0.726199640323043,-1.0014552228282,0.0797567518093963)) ;
#73796=CARTESIAN_POINT('Ctrl Pts',(0.802662369413066,-0.946008703505574,
0.0893832681515186)) ;
#73797=CARTESIAN_POINT('Ctrl Pts',(0.872471815530275,-0.882035343570336,
0.0984204718097368)) ;
#73798=CARTESIAN_POINT('Ctrl Pts',(0.997224140199396,-0.738258844823923,
0.117343525487123)) ;
#73799=CARTESIAN_POINT('Ctrl Pts',(1.05143921430174,-0.658747762510608,
0.127215791163134)) ;
#73800=CARTESIAN_POINT('Ctrl Pts',(1.17229056528863,-0.427929940265304,
0.154409533454461)) ;
#73801=CARTESIAN_POINT('Ctrl Pts',(1.21879504238397,-0.268237899717561,
0.171735505901204)) ;
#73802=CARTESIAN_POINT('Ctrl Pts',(1.24604311601219,0.0544187008378128,
0.204067069536395)) ;
#73803=CARTESIAN_POINT('Ctrl Pts',(1.22873396164754,0.214032331477905,0.21949286037181)) ;
#73804=CARTESIAN_POINT('Ctrl Pts',(1.13294685474823,0.52326531264887,0.253273413059563)) ;
#73805=CARTESIAN_POINT('Ctrl Pts',(1.05333123000921,0.669247043075862,0.270599847935997)) ;
#73806=CARTESIAN_POINT('Ctrl Pts',(0.845166281544509,0.917212072143561,
0.302955291793988)) ;
#73807=CARTESIAN_POINT('Ctrl Pts',(0.720348450836969,1.01818131913425,0.318355515374318)) ;
#73808=CARTESIAN_POINT('Ctrl Pts',(0.434423910324296,1.16988734227459,0.352121926193887)) ;
#73809=CARTESIAN_POINT('Ctrl Pts',(0.275081654562437,1.21725638444016,0.369448705110878)) ;
#73810=CARTESIAN_POINT('Ctrl Pts',(-0.0473201945277858,1.24633236809541,
0.401828909282351)) ;
#73811=CARTESIAN_POINT('Ctrl Pts',(-0.207019547606109,1.22993352367641,
0.417203293416204)) ;
#73812=CARTESIAN_POINT('Ctrl Pts',(-0.516697555743524,1.13594406746541,
0.450954841075392)) ;
#73813=CARTESIAN_POINT('Ctrl Pts',(-0.663056154002597,1.05722451103384,
0.468281828217318)) ;
#73814=CARTESIAN_POINT('Ctrl Pts',(-0.912178303567051,0.850596417502907,
0.500687668948343)) ;
#73815=CARTESIAN_POINT('Ctrl Pts',(-1.01388151658769,0.726386083539357,
0.51603603077116)) ;
#73816=CARTESIAN_POINT('Ctrl Pts',(-1.16723727435572,0.441459608090348,
0.549771970910831)) ;
#73817=CARTESIAN_POINT('Ctrl Pts',(-1.21554227974159,0.282502333661602,
0.567099011944622)) ;
#73818=CARTESIAN_POINT('Ctrl Pts',(-1.24660115811779,-0.0396167266740036,
0.599531357524871)) ;
#73819=CARTESIAN_POINT('Ctrl Pts',(-1.23118959083217,-0.19940927205464,
0.6148536127307)) ;
#73820=CARTESIAN_POINT('Ctrl Pts',(-1.13914783753225,-0.509563718089096,
0.648573178924222)) ;
#73821=CARTESIAN_POINT('Ctrl Pts',(-1.06140079033295,-0.656324460188585,
0.66590009997139)) ;
#73822=CARTESIAN_POINT('Ctrl Pts',(-0.856440857683523,-0.906693947072086,
0.698359806366983)) ;
#73823=CARTESIAN_POINT('Ctrl Pts',(-0.732887669291429,-1.00919149521601,
0.713655978353038)) ;
#73824=CARTESIAN_POINT('Ctrl Pts',(-0.449044355490821,-1.16432601467632,
0.747358383359865)) ;
#73825=CARTESIAN_POINT('Ctrl Pts',(-0.290509159749249,-1.21363917762656,
0.764684990055389)) ;
#73826=CARTESIAN_POINT('Ctrl Pts',(-0.0846982434860556,-1.23487193179222,
0.785462604486457)) ;
#73827=CARTESIAN_POINT('Ctrl Pts',(-0.042328748373072,-1.23704425180953,
0.789651833184625)) ;
#73828=CARTESIAN_POINT('Ctrl Pts',(-1.69733995288825E-12,-1.23704425180959,
0.793749999999827)) ;
#73829=CARTESIAN_POINT('Ctrl Pts',(8.68838113439773E-14,-1.23704425180959,
0.892968750000012)) ;
#73830=CARTESIAN_POINT('Ctrl Pts',(-0.0875248041401834,-1.23704425180959,
0.884494810617548)) ;
#73831=CARTESIAN_POINT('Ctrl Pts',(-0.174966896078172,-1.22776054683028,
0.87565657338642)) ;
#73832=CARTESIAN_POINT('Ctrl Pts',(-0.41995018210912,-1.17490010146493,
0.849818014923812)) ;
#73833=CARTESIAN_POINT('Ctrl Pts',(-0.570670292727075,-1.10954373360727,
0.832604662724326)) ;
#73834=CARTESIAN_POINT('Ctrl Pts',(-0.835998524625215,-0.925745863761894,
0.799545352339523)) ;
#73835=CARTESIAN_POINT('Ctrl Pts',(-0.948609445250275,-0.809962101861421,
0.784516962607178)) ;
#73836=CARTESIAN_POINT('Ctrl Pts',(-1.12500457693874,-0.539573439929506,
0.75126458679419)) ;
#73837=CARTESIAN_POINT('Ctrl Pts',(-1.18616863733828,-0.387015722853597,
0.734041446739443)) ;
#73838=CARTESIAN_POINT('Ctrl Pts',(-1.24539471075493,-0.0697352935498187,
0.700947972352484)) ;
#73839=CARTESIAN_POINT('Ctrl Pts',(-1.24397131491542,0.0916846098798968,
0.685932365379448)) ;
#73840=CARTESIAN_POINT('Ctrl Pts',(-1.17914537419291,0.407942995498055,
0.652713270448955)) ;
#73841=CARTESIAN_POINT('Ctrl Pts',(-1.11525651939214,0.55946897649527,0.635480747733497)) ;
#73842=CARTESIAN_POINT('Ctrl Pts',(-0.934117137292666,0.826601135755457,
0.602353399215146)) ;
#73843=CARTESIAN_POINT('Ctrl Pts',(-0.819606476545795,0.940260261763549,
0.587348036170277)) ;
#73844=CARTESIAN_POINT('Ctrl Pts',(-0.551065827509422,1.1194437567851,0.554162758324779)) ;
#73845=CARTESIAN_POINT('Ctrl Pts',(-0.398985533121644,1.1822176944358,0.536921280023609)) ;
#73846=CARTESIAN_POINT('Ctrl Pts',(-0.0823183609100411,1.24460538594021,
0.503760388847658)) ;
#73847=CARTESIAN_POINT('Ctrl Pts',(0.0789422497001507,1.24482410271381,
0.488762749285042)) ;
#73848=CARTESIAN_POINT('Ctrl Pts',(0.39585691264359,1.18328008947396,0.455611730814931)) ;
#73849=CARTESIAN_POINT('Ctrl Pts',(0.548176881593565,1.12087276457155,0.438361750130771)) ;
#73850=CARTESIAN_POINT('Ctrl Pts',(0.817106163526264,0.942407848466602,
0.405167663070568)) ;
#73851=CARTESIAN_POINT('Ctrl Pts',(0.931811182096248,0.829170170116615,
0.390175304535352)) ;
#73852=CARTESIAN_POINT('Ctrl Pts',(1.11377079968785,0.562490560968091,0.357058876792354)) ;
#73853=CARTESIAN_POINT('Ctrl Pts',(1.17814975251798,0.410904233082254,0.339800856961119)) ;
#73854=CARTESIAN_POINT('Ctrl Pts',(1.2436934742221,0.0948635622913495,0.30657405537189)) ;
#73855=CARTESIAN_POINT('Ctrl Pts',(1.24554635127363,-0.066236004955523,
0.291584401546679)) ;
#73856=CARTESIAN_POINT('Ctrl Pts',(1.18727207947304,-0.383787057084025,
0.258502896359715)) ;
#73857=CARTESIAN_POINT('Ctrl Pts',(1.12634866084976,-0.53688286891284,0.241237309769291)) ;
#73858=CARTESIAN_POINT('Ctrl Pts',(0.950553801783562,-0.807588345240864,
0.207978333579274)) ;
#73859=CARTESIAN_POINT('Ctrl Pts',(0.838578599221216,-0.923329787010875,
0.192988836521312)) ;
#73860=CARTESIAN_POINT('Ctrl Pts',(0.573758990510375,-1.10803178977929,
0.159942511219614)) ;
#73861=CARTESIAN_POINT('Ctrl Pts',(0.422678950448764,-1.1739984166373,0.142669838213727)) ;
#73862=CARTESIAN_POINT('Ctrl Pts',(0.17651318645884,-1.22759348881469,0.116687334249879)) ;
#73863=CARTESIAN_POINT('Ctrl Pts',(0.0883103353827004,-1.23704425180962,
0.107768742613292)) ;
#73864=CARTESIAN_POINT('Ctrl Pts',(-1.55774404735361E-13,-1.23704425180961,
0.0992187500000006)) ;
#73865=CARTESIAN_POINT('Origin',(0.,0.,0.)) ;
#73866=CARTESIAN_POINT('',(-1.7526,3.24070050962596E-15,1.09140625)) ;
#73867=CARTESIAN_POINT('',(-1.7526,1.70165690542032E-13,0.992187499999977)) ;
#73868=CARTESIAN_POINT('',(-1.7526,-2.14631598018565E-16,0.)) ;
#73869=CARTESIAN_POINT('',(1.23927534470755,-1.23927534470755,0.595312499999997)) ;
#73870=CARTESIAN_POINT('Ctrl Pts',(-1.7526,5.55111512312578E-15,1.09140625)) ;
#73871=CARTESIAN_POINT('Ctrl Pts',(-1.7526,0.104547657359432,1.08426176482362)) ;
#73872=CARTESIAN_POINT('Ctrl Pts',(-1.74324717274818,0.209108727288083,
1.07685162045178)) ;
#73873=CARTESIAN_POINT('Ctrl Pts',(-1.68340069519565,0.539420779786685,
1.05258502413979)) ;
#73874=CARTESIAN_POINT('Ctrl Pts',(-1.59787269747691,0.75605024665108,1.03536022243484)) ;
#73875=CARTESIAN_POINT('Ctrl Pts',(-1.35066052761109,1.13936681186793,1.00216784753972)) ;
#73876=CARTESIAN_POINT('Ctrl Pts',(-1.19306628616519,1.30346997592726,0.987212602834704)) ;
#73877=CARTESIAN_POINT('Ctrl Pts',(-0.819924420582547,1.56608123915945,
0.954279648356355)) ;
#73878=CARTESIAN_POINT('Ctrl Pts',(-0.606768521826978,1.66033533629354,
0.937045217909976)) ;
#73879=CARTESIAN_POINT('Ctrl Pts',(-0.161546082820598,1.75962805345187,
0.90380940587192)) ;
#73880=CARTESIAN_POINT('Ctrl Pts',(0.0657712499739911,1.76580372195142,
0.888847879253041)) ;
#73881=CARTESIAN_POINT('Ctrl Pts',(0.515896453846038,1.69080176141891,0.855964604443078)) ;
#73882=CARTESIAN_POINT('Ctrl Pts',(0.733993601723274,1.60816871798398,0.838721450690954)) ;
#73883=CARTESIAN_POINT('Ctrl Pts',(1.12071257887363,1.36614209500329,0.805443347700574)) ;
#73884=CARTESIAN_POINT('Ctrl Pts',(1.28680628777948,1.21097938674294,0.790470917443707)) ;
#73885=CARTESIAN_POINT('Ctrl Pts',(1.55465981560029,0.841466028666496,0.757637536319184)) ;
#73886=CARTESIAN_POINT('Ctrl Pts',(1.65195907511392,0.629329368409463,0.740386560838467)) ;
#73887=CARTESIAN_POINT('Ctrl Pts',(1.7572524398515,0.185372758680501,0.707067396633006)) ;
#73888=CARTESIAN_POINT('Ctrl Pts',(1.76651236376204,-0.0416378121238857,
0.692079647673984)) ;
#73889=CARTESIAN_POINT('Ctrl Pts',(1.70441589556448,-0.448830076054136,
0.662495590997371)) ;
#73890=CARTESIAN_POINT('Ctrl Pts',(1.64693701205005,-0.627750772362418,
0.648641660541893)) ;
#73891=CARTESIAN_POINT('Ctrl Pts',(1.47869800081274,-0.958703636471365,
0.621263096675404)) ;
#73892=CARTESIAN_POINT('Ctrl Pts',(1.36965572949312,-1.10889495992211,0.607912887171705)) ;
#73893=CARTESIAN_POINT('Ctrl Pts',(1.23927534470684,-1.23927534470824,0.595312499999933)) ;
#73894=CARTESIAN_POINT('',(1.7526,0.,0.5953125)) ;
#73895=CARTESIAN_POINT('Origin',(0.,0.,0.5953125)) ;
#73896=CARTESIAN_POINT('Ctrl Pts',(1.7526,-2.15105711021124E-15,0.5953125)) ;
#73897=CARTESIAN_POINT('Ctrl Pts',(1.7526,0.21481984001363,0.609992667890278)) ;
#73898=CARTESIAN_POINT('Ctrl Pts',(1.71310447370405,0.427903785524575,0.625672176423836)) ;
#73899=CARTESIAN_POINT('Ctrl Pts',(1.55856129077335,0.830122835430236,0.657533189451965)) ;
#73900=CARTESIAN_POINT('Ctrl Pts',(1.44454049439502,1.01565121826221,0.673439154533952)) ;
#73901=CARTESIAN_POINT('Ctrl Pts',(1.1487270417631,1.34262606689925,0.704157014779829)) ;
#73902=CARTESIAN_POINT('Ctrl Pts',(0.967058618495535,1.47886687425541,0.71991567147517)) ;
#73903=CARTESIAN_POINT('Ctrl Pts',(0.554468507663844,1.67889396301424,0.75377288756523)) ;
#73904=CARTESIAN_POINT('Ctrl Pts',(0.326094855888817,1.73776089872563,0.771045580701419)) ;
#73905=CARTESIAN_POINT('Ctrl Pts',(-0.131750544532228,1.76205786107286,
0.803021167700791)) ;
#73906=CARTESIAN_POINT('Ctrl Pts',(-0.356611590657682,1.73062508679216,
0.818741832310748)) ;
#73907=CARTESIAN_POINT('Ctrl Pts',(-0.790158210912439,1.58168779748694,
0.852584999765607)) ;
#73908=CARTESIAN_POINT('Ctrl Pts',(-0.993577728078715,1.46250450419731,
0.869859723794248)) ;
#73909=CARTESIAN_POINT('Ctrl Pts',(-1.33540783531321,1.15709975956045,0.901864242180511)) ;
#73910=CARTESIAN_POINT('Ctrl Pts',(-1.4727465616134,0.9763392165215,0.917545719644801)) ;
#73911=CARTESIAN_POINT('Ctrl Pts',(-1.67528581774019,0.56521487114132,0.951373879364155)) ;
#73912=CARTESIAN_POINT('Ctrl Pts',(-1.73558543790577,0.337376226297066,
0.9686505654653)) ;
#73913=CARTESIAN_POINT('Ctrl Pts',(-1.75156455156437,0.0695968375627338,
0.987402143410981)) ;
#73914=CARTESIAN_POINT('Ctrl Pts',(-1.7526,0.0347828049418742,0.989810543494454)) ;
#73915=CARTESIAN_POINT('Ctrl Pts',(-1.7526,3.40546012682082E-13,0.992187499999977)) ;
#73916=CARTESIAN_POINT('Origin',(0.,0.,0.)) ;
#73917=CARTESIAN_POINT('',(-1.7526,-7.2430388732916E-14,1.88515625000001)) ;
#73918=CARTESIAN_POINT('',(-1.7526,2.85432335943383E-13,1.78593749999996)) ;
#73919=CARTESIAN_POINT('',(-1.7526,-2.14631598018565E-16,0.)) ;
#73920=CARTESIAN_POINT('Ctrl Pts',(-1.7526,-1.44155520853673E-13,1.88515625000001)) ;
#73921=CARTESIAN_POINT('Ctrl Pts',(-1.75260000000001,0.137894910250373,
1.87573290980218)) ;
#73922=CARTESIAN_POINT('Ctrl Pts',(-1.73633070266727,0.275582131070812,
1.86586324117668)) ;
#73923=CARTESIAN_POINT('Ctrl Pts',(-1.65021735313446,0.633251880812449,
1.83898358452446)) ;
#73924=CARTESIAN_POINT('Ctrl Pts',(-1.55325686201387,0.8435796286795,1.82186581412804)) ;
#73925=CARTESIAN_POINT('Ctrl Pts',(-1.28533606284546,1.21283083755785,1.78904844332966)) ;
#73926=CARTESIAN_POINT('Ctrl Pts',(-1.11779116886749,1.3687913098494,1.77396952247319)) ;
#73927=CARTESIAN_POINT('Ctrl Pts',(-0.73020747915963,1.6096874188709,1.74066432803057)) ;
#73928=CARTESIAN_POINT('Ctrl Pts',(-0.513326877073374,1.69138962506005,
1.72353065793429)) ;
#73929=CARTESIAN_POINT('Ctrl Pts',(-0.0633186871198124,1.76605389040637,
1.69066493837158)) ;
#73930=CARTESIAN_POINT('Ctrl Pts',(0.165276475839116,1.75944269119178,1.67561792294161)) ;
#73931=CARTESIAN_POINT('Ctrl Pts',(0.610355197234708,1.65886568423244,1.64235557883846)) ;
#73932=CARTESIAN_POINT('Ctrl Pts',(0.822287881901152,1.56467786568413,1.62520661540491)) ;
#73933=CARTESIAN_POINT('Ctrl Pts',(1.19504792379624,1.30181724091056,1.59229269518788)) ;
#73934=CARTESIAN_POINT('Ctrl Pts',(1.35302893168609,1.13674084899859,1.57727316131317)) ;
#73935=CARTESIAN_POINT('Ctrl Pts',(1.59934964349609,0.752676972049826,1.5440549510449)) ;
#73936=CARTESIAN_POINT('Ctrl Pts',(1.68417623655015,0.536652784648655,1.52689136646387)) ;
#73937=CARTESIAN_POINT('Ctrl Pts',(1.76495892013688,0.0877725403261723,
1.49392953852819)) ;
#73938=CARTESIAN_POINT('Ctrl Pts',(1.76154542959128,-0.140503534161234,
1.47893285472881)) ;
#73939=CARTESIAN_POINT('Ctrl Pts',(1.6673469914036,-0.586915339414595,1.44575996430666)) ;
#73940=CARTESIAN_POINT('Ctrl Pts',(1.57600910258148,-0.800445713521442,
1.4285824899529)) ;
#73941=CARTESIAN_POINT('Ctrl Pts',(1.31832327386051,-1.17674495475663,1.39557318966923)) ;
#73942=CARTESIAN_POINT('Ctrl Pts',(1.15574533167312,-1.33677126408857,1.38059456494248)) ;
#73943=CARTESIAN_POINT('Ctrl Pts',(0.775287903995105,-1.5885585898706,1.34746807016247)) ;
#73944=CARTESIAN_POINT('Ctrl Pts',(0.560176278440258,-1.67654203789935,
1.33027748898416)) ;
#73945=CARTESIAN_POINT('Ctrl Pts',(0.112478485471377,-1.76351335068776,
1.29722129003663)) ;
#73946=CARTESIAN_POINT('Ctrl Pts',(-0.11547683701007,-1.76331954554437,
1.28225582539335)) ;
#73947=CARTESIAN_POINT('Ctrl Pts',(-0.563182482720134,-1.67555649639276,
1.24917667879644)) ;
#73948=CARTESIAN_POINT('Ctrl Pts',(-0.77828442275198,-1.58711590168822,
1.23197381943213)) ;
#73949=CARTESIAN_POINT('Ctrl Pts',(-1.15811524055575,-1.33466516746216,
1.19887136681734)) ;
#73950=CARTESIAN_POINT('Ctrl Pts',(-1.3201894927846,-1.1745901086568,1.18391422887698)) ;
#73951=CARTESIAN_POINT('Ctrl Pts',(-1.57742656628545,-0.797786875386106,
1.15088318976893)) ;
#73952=CARTESIAN_POINT('Ctrl Pts',(-1.668564210659,-0.583635070404743,1.13366891677396)) ;
#73953=CARTESIAN_POINT('Ctrl Pts',(-1.74027492516994,-0.239971504707985,
1.10815408560011)) ;
#73954=CARTESIAN_POINT('Ctrl Pts',(-1.7526,-0.120018555030801,1.0996079716738)) ;
#73955=CARTESIAN_POINT('Ctrl Pts',(-1.7526,5.44703171456717E-15,1.09140625)) ;
#73956=CARTESIAN_POINT('Ctrl Pts',(-1.7526,3.37785355242204E-13,0.992187499999977)) ;
#73957=CARTESIAN_POINT('Ctrl Pts',(-1.7526,-0.189598109227915,1.005144087599)) ;
#73958=CARTESIAN_POINT('Ctrl Pts',(-1.7218412189295,-0.378150559501995,
1.01889988084353)) ;
#73959=CARTESIAN_POINT('Ctrl Pts',(-1.58698346716713,-0.77942035652952,
1.05013880571663)) ;
#73960=CARTESIAN_POINT('Ctrl Pts',(-1.46927136315343,-0.983505269936009,
1.06741735728579)) ;
#73961=CARTESIAN_POINT('Ctrl Pts',(-1.16639091096922,-1.32729172587642,
1.09948411387195)) ;
#73962=CARTESIAN_POINT('Ctrl Pts',(-0.986642304617752,-1.46585487001854,
1.11508405901835)) ;
#73963=CARTESIAN_POINT('Ctrl Pts',(-0.577158522321734,-1.67118546774369,
1.14887911955152)) ;
#73964=CARTESIAN_POINT('Ctrl Pts',(-0.349926086046935,-1.73307590322111,
1.16615940898039)) ;
#73965=CARTESIAN_POINT('Ctrl Pts',(0.107114628641963,-1.76371403859573,
1.1982595003338)) ;
#73966=CARTESIAN_POINT('Ctrl Pts',(0.332276422609993,-1.73544618249771,
1.21381737045474)) ;
#73967=CARTESIAN_POINT('Ctrl Pts',(0.767450699788526,-1.59278072451589,
1.24759423582901)) ;
#73968=CARTESIAN_POINT('Ctrl Pts',(0.972262664692636,-1.47670680677704,
1.26487610123737)) ;
#73969=CARTESIAN_POINT('Ctrl Pts',(1.31821032672548,-1.17663629117846,1.29701100989763)) ;
#73970=CARTESIAN_POINT('Ctrl Pts',(1.458131396676,-0.998009254994801,1.31252615256722)) ;
#73971=CARTESIAN_POINT('Ctrl Pts',(1.66654482904563,-0.590351992356521,
1.34628365722728)) ;
#73972=CARTESIAN_POINT('Ctrl Pts',(1.73019072282956,-0.363803485072845,
1.36356689920542)) ;
#73973=CARTESIAN_POINT('Ctrl Pts',(1.7645229382863,0.0927476684014285,1.39573810057802)) ;
#73974=CARTESIAN_POINT('Ctrl Pts',(1.73809700251126,0.318085361371882,1.41121005975164)) ;
#73975=CARTESIAN_POINT('Ctrl Pts',(1.59907663088538,0.754185070479275,1.44494698807761)) ;
#73976=CARTESIAN_POINT('Ctrl Pts',(1.48481611104004,0.95978494330198,1.46223136650934)) ;
#73977=CARTESIAN_POINT('Ctrl Pts',(1.18785527375227,1.30810418333975,1.494440318916)) ;
#73978=CARTESIAN_POINT('Ctrl Pts',(1.01046360803963,1.44952204637,1.50986886038149)) ;
#73979=CARTESIAN_POINT('Ctrl Pts',(0.604827973964349,1.66131763116995,1.54358394852591)) ;
#73980=CARTESIAN_POINT('Ctrl Pts',(0.379047263768518,1.72688742092612,1.56086917957305)) ;
#73981=CARTESIAN_POINT('Ctrl Pts',(-0.0769481266801126,1.76527924233848,
1.59311731355779)) ;
#73982=CARTESIAN_POINT('Ctrl Pts',(-0.302479780335044,1.74087622754771,
1.60850245019479)) ;
#73983=CARTESIAN_POINT('Ctrl Pts',(-0.7395773828631,1.60585438572068,1.64219438865525)) ;
#73984=CARTESIAN_POINT('Ctrl Pts',(-0.946023426504051,1.49358813022675,
1.65948014199397)) ;
#73985=CARTESIAN_POINT('Ctrl Pts',(-1.29692605138797,1.20004656583408,1.69176884898162)) ;
#73986=CARTESIAN_POINT('Ctrl Pts',(-1.4399827386388,1.02400637996451,1.70711086526757)) ;
#73987=CARTESIAN_POINT('Ctrl Pts',(-1.65546189751001,0.620593827557374,
1.74077830226157)) ;
#73988=CARTESIAN_POINT('Ctrl Pts',(-1.72312437828023,0.395670201913235,
1.75806419866947)) ;
#73989=CARTESIAN_POINT('Ctrl Pts',(-1.75003962953136,0.109450542229317,
1.77838549156683)) ;
#73990=CARTESIAN_POINT('Ctrl Pts',(-1.7526,0.0546965877173526,1.78219969305134)) ;
#73991=CARTESIAN_POINT('Ctrl Pts',(-1.7526,5.71079303484785E-13,1.78593749999996)) ;
#73992=CARTESIAN_POINT('Origin',(0.,0.,0.)) ;
#73993=CARTESIAN_POINT('',(-1.7526,-3.02963679535642E-13,2.67890625000005)) ;
#73994=CARTESIAN_POINT('',(-1.7526,1.12532367841355E-13,2.57968749999998)) ;
#73995=CARTESIAN_POINT('',(-1.7526,-2.14631598018565E-16,0.)) ;
#73996=CARTESIAN_POINT('Ctrl Pts',(-1.7526,-6.06112382506296E-13,2.67890625000005)) ;
#73997=CARTESIAN_POINT('Ctrl Pts',(-1.75260000000006,0.167794841835216,
2.66743963476974)) ;
#73998=CARTESIAN_POINT('Ctrl Pts',(-1.72851068177184,0.334990802640833,
2.65533206925858)) ;
#73999=CARTESIAN_POINT('Ctrl Pts',(-1.61613829516608,0.715405367443283,
2.62615480509768)) ;
#74000=CARTESIAN_POINT('Ctrl Pts',(-1.50932245410327,0.91960420272306,2.60917689979265)) ;
#74001=CARTESIAN_POINT('Ctrl Pts',(-1.22317845929475,1.27581509594749,2.5767348378504)) ;
#74002=CARTESIAN_POINT('Ctrl Pts',(-1.04652669095695,1.42430903244335,2.56127802021772)) ;
#74003=CARTESIAN_POINT('Ctrl Pts',(-0.646337776712737,1.64499658772374,
2.52768344765317)) ;
#74004=CARTESIAN_POINT('Ctrl Pts',(-0.426687637569999,1.71514464643388,
2.51068756892792)) ;
#74005=CARTESIAN_POINT('Ctrl Pts',(0.0271348749003668,1.76720867163961,
2.47820091557302)) ;
#74006=CARTESIAN_POINT('Ctrl Pts',(0.256915735402302,1.74864533134862,2.46279992862756)) ;
#74007=CARTESIAN_POINT('Ctrl Pts',(0.696591814856775,1.62437266580848,2.42923605239312)) ;
#74008=CARTESIAN_POINT('Ctrl Pts',(0.902246371267716,1.51980072118882,2.41222218339769)) ;
#74009=CARTESIAN_POINT('Ctrl Pts',(1.26150882860939,1.23784150397511,2.3796900413523)) ;
#74010=CARTESIAN_POINT('Ctrl Pts',(1.41174582860743,1.0633118822824,2.36434318780097)) ;
#74011=CARTESIAN_POINT('Ctrl Pts',(1.63716968880939,0.666006325112866,2.33081158893528)) ;
#74012=CARTESIAN_POINT('Ctrl Pts',(1.71001242012726,0.446946707454403,2.31377978891158)) ;
#74013=CARTESIAN_POINT('Ctrl Pts',(1.76734651524038,-0.00603574739972152,
2.28120136723079)) ;
#74014=CARTESIAN_POINT('Ctrl Pts',(1.75159138829553,-0.235540169200276,
2.26590656468891)) ;
#74015=CARTESIAN_POINT('Ctrl Pts',(1.63286262308617,-0.676544727005498,
2.23240883060458)) ;
#74016=CARTESIAN_POINT('Ctrl Pts',(1.53069027897643,-0.883715991510807,
2.21535923762982)) ;
#74017=CARTESIAN_POINT('Ctrl Pts',(1.25318188960883,-1.24618637556307,2.18273386097376)) ;
#74018=CARTESIAN_POINT('Ctrl Pts',(1.08088890457571,-1.39825791607344,2.16748864177913)) ;
#74019=CARTESIAN_POINT('Ctrl Pts',(0.686657935676051,-1.62865582263718,
2.13402635525318)) ;
#74020=CARTESIAN_POINT('Ctrl Pts',(0.468256765243388,-1.70433764044138,
2.1169591879779)) ;
#74021=CARTESIAN_POINT('Ctrl Pts',(0.0161917720505629,-1.7672238142356,
2.08428630495496)) ;
#74022=CARTESIAN_POINT('Ctrl Pts',(-0.21302102223957,-1.75441282183859,
2.06908782214896)) ;
#74023=CARTESIAN_POINT('Ctrl Pts',(-0.655379533562164,-1.64151270301104,
2.0356625493825)) ;
#74024=CARTESIAN_POINT('Ctrl Pts',(-0.864114072684682,-1.5418833009729,
2.01857810765572)) ;
#74025=CARTESIAN_POINT('Ctrl Pts',(-1.22992400629464,-1.26906584175147,
1.98585729803748)) ;
#74026=CARTESIAN_POINT('Ctrl Pts',(-1.38390861706332,-1.09910773855309,
1.97070233785842)) ;
#74027=CARTESIAN_POINT('Ctrl Pts',(-1.61947947451139,-0.708125235589788,
1.93731561574699)) ;
#74028=CARTESIAN_POINT('Ctrl Pts',(-1.69812325285362,-0.490450951286152,
1.92021428004477)) ;
#74029=CARTESIAN_POINT('Ctrl Pts',(-1.74595470399728,-0.176304466427567,
1.89739249122397)) ;
#74030=CARTESIAN_POINT('Ctrl Pts',(-1.75259999999999,-0.0881227360395467,
1.89117830345619)) ;
#74031=CARTESIAN_POINT('Ctrl Pts',(-1.7526,-1.44646145867813E-13,1.88515625000001)) ;
#74032=CARTESIAN_POINT('Ctrl Pts',(-1.7526,5.71079303484785E-13,1.78593749999996)) ;
#74033=CARTESIAN_POINT('Ctrl Pts',(-1.7526,-0.169339024401733,1.79750964021027)) ;
#74034=CARTESIAN_POINT('Ctrl Pts',(-1.72806515051229,-0.338033438283696,
1.80973221695903)) ;
#74035=CARTESIAN_POINT('Ctrl Pts',(-1.61308143750617,-0.72360540841447,
1.83933583993703)) ;
#74036=CARTESIAN_POINT('Ctrl Pts',(-1.50299263305593,-0.930951275487185,
1.85662144933578)) ;
#74037=CARTESIAN_POINT('Ctrl Pts',(-1.21318427577553,-1.28464560245755,
1.88899526043142)) ;
#74038=CARTESIAN_POINT('Ctrl Pts',(-1.03861168766202,-1.42948356470644,
1.90425308939975)) ;
#74039=CARTESIAN_POINT('Ctrl Pts',(-0.637626366345578,-1.64894294060327,
1.93786732108372)) ;
#74040=CARTESIAN_POINT('Ctrl Pts',(-0.413653382345688,-1.71886315472059,
1.95515216114529)) ;
#74041=CARTESIAN_POINT('Ctrl Pts',(0.0410093244316962,-1.76648056906025,
1.98757036447825)) ;
#74042=CARTESIAN_POINT('Ctrl Pts',(0.266984560954872,-1.74667118590977,
2.00278777632734)) ;
#74043=CARTESIAN_POINT('Ctrl Pts',(0.706276495114559,-1.6207083130571,2.03637324445863)) ;
#74044=CARTESIAN_POINT('Ctrl Pts',(0.914569087867585,-1.51297837596066,
2.05365677988273)) ;
#74045=CARTESIAN_POINT('Ctrl Pts',(1.27125430488095,-1.22721474999631,2.08612048896267)) ;
#74046=CARTESIAN_POINT('Ctrl Pts',(1.41801316077564,-1.054223186184,2.10129906156371)) ;
#74047=CARTESIAN_POINT('Ctrl Pts',(1.64173675890614,-0.655867477843011,
2.13485429684043)) ;
#74048=CARTESIAN_POINT('Ctrl Pts',(1.71407133525771,-0.432941345458989,
2.15213593940611)) ;
#74049=CARTESIAN_POINT('Ctrl Pts',(1.76683813655813,0.0209350447270955,
2.18464616750078)) ;
#74050=CARTESIAN_POINT('Ctrl Pts',(1.74959152333341,0.24715968621795,2.19978783806631)) ;
#74051=CARTESIAN_POINT('Ctrl Pts',(1.62866847251747,0.687632694870889,2.23331135941382)) ;
#74052=CARTESIAN_POINT('Ctrl Pts',(1.52347229531964,0.896910039075942,2.25059046889851)) ;
#74053=CARTESIAN_POINT('Ctrl Pts',(1.24205467761495,1.25677007786189,2.28314811733312)) ;
#74054=CARTESIAN_POINT('Ctrl Pts',(1.07075186180036,1.40558294859694,2.29825518800676)) ;
#74055=CARTESIAN_POINT('Ctrl Pts',(0.675221204033864,1.63383361824712,2.33174551148854)) ;
#74056=CARTESIAN_POINT('Ctrl Pts',(0.453438689242829,1.70872576533173,2.34902139753333)) ;
#74057=CARTESIAN_POINT('Ctrl Pts',(0.000432766936031767,1.76697209320413,
2.38162724471802)) ;
#74058=CARTESIAN_POINT('Ctrl Pts',(-0.226058764460174,1.75245236168843,
2.39670238262469)) ;
#74059=CARTESIAN_POINT('Ctrl Pts',(-0.667754664436714,1.63687944061578,
2.43015803121053)) ;
#74060=CARTESIAN_POINT('Ctrl Pts',(-0.878043964467795,1.5343801550739,2.44742995619069)) ;
#74061=CARTESIAN_POINT('Ctrl Pts',(-1.24124121035046,1.25759093278454,2.48008464762852)) ;
#74062=CARTESIAN_POINT('Ctrl Pts',(-1.39223079083935,1.08807569583888,2.49513087887956)) ;
#74063=CARTESIAN_POINT('Ctrl Pts',(-1.62524149301606,0.695552885592716,
2.52855039298208)) ;
#74064=CARTESIAN_POINT('Ctrl Pts',(-1.70281592843141,0.475008766544544,
2.54581757591695)) ;
#74065=CARTESIAN_POINT('Ctrl Pts',(-1.7468382272959,0.164173644723157,2.5683052532728)) ;
#74066=CARTESIAN_POINT('Ctrl Pts',(-1.7526,0.0820549291164976,2.57408010295708)) ;
#74067=CARTESIAN_POINT('Ctrl Pts',(-1.7526,2.25279367280728E-13,2.57968749999998)) ;
#74068=CARTESIAN_POINT('Origin',(0.,0.,0.)) ;
#74069=CARTESIAN_POINT('',(-1.7526,-2.09103334841134E-13,3.47265625000003)) ;
#74070=CARTESIAN_POINT('',(-1.7526,-5.06302198483948E-16,3.3734375)) ;
#74071=CARTESIAN_POINT('',(-1.7526,-2.14631598018565E-16,0.)) ;
#74072=CARTESIAN_POINT('Ctrl Pts',(-1.7526,-4.17513246198098E-13,3.47265625000003)) ;
#74073=CARTESIAN_POINT('Ctrl Pts',(-1.75260000000004,0.185210600655636,
3.45999949207434)) ;
#74074=CARTESIAN_POINT('Ctrl Pts',(-1.72324896284641,0.369470892755415,
3.44657686035593)) ;
#74075=CARTESIAN_POINT('Ctrl Pts',(-1.59279484445025,0.767421264017481,
3.41568942540778)) ;
#74076=CARTESIAN_POINT('Ctrl Pts',(-1.47672495305229,0.972234997958048,
3.39840755307882)) ;
#74077=CARTESIAN_POINT('Ctrl Pts',(-1.17301360568729,1.32239354269544,3.36588182688286)) ;
#74078=CARTESIAN_POINT('Ctrl Pts',(-0.989205491121332,1.4649837181463,3.34995951071369)) ;
#74079=CARTESIAN_POINT('Ctrl Pts',(-0.579538199999467,1.6695782840237,3.31617274395179)) ;
#74080=CARTESIAN_POINT('Ctrl Pts',(-0.358141571382955,1.73064028751114,
3.29931470650395)) ;
#74081=CARTESIAN_POINT('Ctrl Pts',(0.0982952795497277,1.7649160237594,3.26715291494664)) ;
#74082=CARTESIAN_POINT('Ctrl Pts',(0.328999802663575,1.73676904263517,3.25128773938596)) ;
#74083=CARTESIAN_POINT('Ctrl Pts',(0.763872713205693,1.5937059475115,3.21752021295754)) ;
#74084=CARTESIAN_POINT('Ctrl Pts',(0.964173820662061,1.48114590915186,3.20064607095859)) ;
#74085=CARTESIAN_POINT('Ctrl Pts',(1.31233058947525,1.18417961761153,3.16844806697758)) ;
#74086=CARTESIAN_POINT('Ctrl Pts',(1.45622838186895,1.00195149571405,3.15264086582667)) ;
#74087=CARTESIAN_POINT('Ctrl Pts',(1.66439213815404,0.594344213342975,3.11889384404487)) ;
#74088=CARTESIAN_POINT('Ctrl Pts',(1.72745943040643,0.373300780381277,3.10200318094529)) ;
#74089=CARTESIAN_POINT('Ctrl Pts',(1.76566483314572,-0.0825878733541528,
3.06976761783615)) ;
#74090=CARTESIAN_POINT('Ctrl Pts',(1.73964953909945,-0.313090227909846,
3.05401898960127)) ;
#74091=CARTESIAN_POINT('Ctrl Pts',(1.60074750475764,-0.749067292774356,
3.02029379210293)) ;
#74092=CARTESIAN_POINT('Ctrl Pts',(1.48993651937415,-0.950581907434876,
3.00338623149624)) ;
#74093=CARTESIAN_POINT('Ctrl Pts',(1.19628310005053,-1.30122937743768,2.97111179487327)) ;
#74094=CARTESIAN_POINT('Ctrl Pts',(1.01577567112777,-1.44654829596119,2.95542207613238)) ;
#74095=CARTESIAN_POINT('Ctrl Pts',(0.610432930541322,-1.65858863601416,
2.92172007540247)) ;
#74096=CARTESIAN_POINT('Ctrl Pts',(0.389794994609997,-1.72384046393432,
2.9047952869848)) ;
#74097=CARTESIAN_POINT('Ctrl Pts',(-0.0654779456713953,-1.76632390737681,
2.872480705054)) ;
#74098=CARTESIAN_POINT('Ctrl Pts',(-0.295758785991269,-1.74261971907228,
2.85684994471076)) ;
#74099=CARTESIAN_POINT('Ctrl Pts',(-0.732909890444729,-1.60824129178231,
2.82317256267759)) ;
#74100=CARTESIAN_POINT('Ctrl Pts',(-0.935725769901182,-1.49934475758604,
2.80623026815074)) ;
#74101=CARTESIAN_POINT('Ctrl Pts',(-1.28906055399697,-1.2092995320789,2.77387432234772)) ;
#74102=CARTESIAN_POINT('Ctrl Pts',(-1.43591283688306,-1.03065239366411,
2.75830225741605)) ;
#74103=CARTESIAN_POINT('Ctrl Pts',(-1.65213207633461,-0.62778258377614,
2.72465096104054)) ;
#74104=CARTESIAN_POINT('Ctrl Pts',(-1.71974616387183,-0.407607554591312,
2.70769093983665)) ;
#74105=CARTESIAN_POINT('Ctrl Pts',(-1.74949550562248,-0.120523582461612,
2.68723036010368)) ;
#74106=CARTESIAN_POINT('Ctrl Pts',(-1.75259999999998,-0.0602292128905996,
2.6830221405857)) ;
#74107=CARTESIAN_POINT('Ctrl Pts',(-1.7526,-6.05712727473265E-13,2.67890625000005)) ;
#74108=CARTESIAN_POINT('Ctrl Pts',(-1.7526,2.25279367280728E-13,2.57968749999998)) ;
#74109=CARTESIAN_POINT('Ctrl Pts',(-1.7526,-0.142024538270848,2.58939304705851)) ;
#74110=CARTESIAN_POINT('Ctrl Pts',(-1.73534182380825,-0.283790939099401,
2.59956946643582)) ;
#74111=CARTESIAN_POINT('Ctrl Pts',(-1.64524534444182,-0.6467636811424,2.62692426138539)) ;
#74112=CARTESIAN_POINT('Ctrl Pts',(-1.54558886698793,-0.858079736654223,
2.64418588289291)) ;
#74113=CARTESIAN_POINT('Ctrl Pts',(-1.27368250679245,-1.22474897706124,
2.6769396253434)) ;
#74114=CARTESIAN_POINT('Ctrl Pts',(-1.10604159088307,-1.37802354594454,
2.69193848892341)) ;
#74115=CARTESIAN_POINT('Ctrl Pts',(-0.716690851871007,-1.61598895300862,
2.7252814814989)) ;
#74116=CARTESIAN_POINT('Ctrl Pts',(-0.497475018079849,-1.69634711168952,
2.74253668976731)) ;
#74117=CARTESIAN_POINT('Ctrl Pts',(-0.0464636891190264,-1.76639663606009,
2.77534033536094)) ;
#74118=CARTESIAN_POINT('Ctrl Pts',(0.180608059176743,-1.75775315744277,
2.79032136742799)) ;
#74119=CARTESIAN_POINT('Ctrl Pts',(0.624821194156055,-1.6536608113385,2.82362406560381)) ;
#74120=CARTESIAN_POINT('Ctrl Pts',(0.837165348245854,-1.55697051100277,
2.84087198331866)) ;
#74121=CARTESIAN_POINT('Ctrl Pts',(1.20740840408138,-1.29016467261973,2.87372557381785)) ;
#74122=CARTESIAN_POINT('Ctrl Pts',(1.36305801487321,-1.12446972860818,2.8886930464671)) ;
#74123=CARTESIAN_POINT('Ctrl Pts',(1.60612704091343,-0.73843090146846,2.92195417639586)) ;
#74124=CARTESIAN_POINT('Ctrl Pts',(1.6893429308557,-0.520625246278682,2.93919390852514)) ;
#74125=CARTESIAN_POINT('Ctrl Pts',(1.76561778142678,-0.0707325453436116,
2.97209732538375)) ;
#74126=CARTESIAN_POINT('Ctrl Pts',(1.76007670662897,0.156648105524041,2.98705574259079)) ;
#74127=CARTESIAN_POINT('Ctrl Pts',(1.66201597291323,0.602125530862736,3.02027410693917)) ;
#74128=CARTESIAN_POINT('Ctrl Pts',(1.5683878464975,0.815485282051297,3.03750474924555)) ;
#74129=CARTESIAN_POINT('Ctrl Pts',(1.30685524541685,1.18936675820036,3.07045771379264)) ;
#74130=CARTESIAN_POINT('Ctrl Pts',(1.14316023010785,1.34745987301223,3.08541176804576)) ;
#74131=CARTESIAN_POINT('Ctrl Pts',(0.76054348947215,1.59572971971315,3.11858625771782)) ;
#74132=CARTESIAN_POINT('Ctrl Pts',(0.54421879935505,1.681846775671,3.13580690583587)) ;
#74133=CARTESIAN_POINT('Ctrl Pts',(0.0955173731444148,1.76448303712047,
3.16880898152834)) ;
#74134=CARTESIAN_POINT('Ctrl Pts',(-0.1321808781177,1.76211573038241,3.18376350595154)) ;
#74135=CARTESIAN_POINT('Ctrl Pts',(-0.578905685979277,1.67020212412462,
3.21689311125174)) ;
#74136=CARTESIAN_POINT('Ctrl Pts',(-0.793255034070076,1.57970086529386,
3.23410287014207)) ;
#74137=CARTESIAN_POINT('Ctrl Pts',(-1.17079956001474,1.32356249944587,3.26715346685808)) ;
#74138=CARTESIAN_POINT('Ctrl Pts',(-1.33138037898044,1.16190166375245,3.28211338383734)) ;
#74139=CARTESIAN_POINT('Ctrl Pts',(-1.58489259402161,0.782783166642962,
3.31519720495683)) ;
#74140=CARTESIAN_POINT('Ctrl Pts',(-1.67392181139128,0.567996248342534,
3.33239519829217)) ;
#74141=CARTESIAN_POINT('Ctrl Pts',(-1.74135782360205,0.22921502874541,3.35745538361937)) ;
#74142=CARTESIAN_POINT('Ctrl Pts',(-1.7526,0.114623761611832,3.36560444293893)) ;
#74143=CARTESIAN_POINT('Ctrl Pts',(-1.7526,-5.55111512312578E-16,3.3734375)) ;
#74144=CARTESIAN_POINT('Origin',(0.,0.,0.)) ;
#74145=CARTESIAN_POINT('',(-1.7526,-6.97032678444217E-14,4.26640625000002)) ;
#74146=CARTESIAN_POINT('',(-1.7526,-1.44575086878353E-13,4.16718750000002)) ;
#74147=CARTESIAN_POINT('',(-1.7526,-2.14631598018565E-16,0.)) ;
#74148=CARTESIAN_POINT('Ctrl Pts',(-1.7526,-1.3912482277334E-13,4.26640625000002)) ;
#74149=CARTESIAN_POINT('Ctrl Pts',(-1.75260000000002,0.20021035250331,4.25272445232278)) ;
#74150=CARTESIAN_POINT('Ctrl Pts',(-1.7182993432369,0.399124785467476,4.23816029418824)) ;
#74151=CARTESIAN_POINT('Ctrl Pts',(-1.57256716668258,0.808235012859114,
4.20607776373)) ;
#74152=CARTESIAN_POINT('Ctrl Pts',(-1.45090373646926,1.01050584252262,4.18881133453901)) ;
#74153=CARTESIAN_POINT('Ctrl Pts',(-1.14124126899642,1.34900413359057,4.15691398307249)) ;
#74154=CARTESIAN_POINT('Ctrl Pts',(-0.958764240846233,1.48426752674617,
4.14108339296375)) ;
#74155=CARTESIAN_POINT('Ctrl Pts',(-0.544873581032442,1.68205096011171,
4.10720081037692)) ;
#74156=CARTESIAN_POINT('Ctrl Pts',(-0.316030548027637,1.73963764710754,
4.08993228000637)) ;
#74157=CARTESIAN_POINT('Ctrl Pts',(0.142141141021597,1.76125722862828,4.05801018175233)) ;
#74158=CARTESIAN_POINT('Ctrl Pts',(0.366875607603623,1.72848677607019,4.04221497702927)) ;
#74159=CARTESIAN_POINT('Ctrl Pts',(0.799720006941358,1.57689574068337,4.0083446799656)) ;
#74160=CARTESIAN_POINT('Ctrl Pts',(1.00253640979324,1.45640111071015,3.99107405212338)) ;
#74161=CARTESIAN_POINT('Ctrl Pts',(1.34261020733303,1.14874555256045,3.95912584298678)) ;
#74162=CARTESIAN_POINT('Ctrl Pts',(1.47885343647802,0.967079132387764,3.94336736075693)) ;
#74163=CARTESIAN_POINT('Ctrl Pts',(1.67888607605626,0.554492249112647,3.90951020810639)) ;
#74164=CARTESIAN_POINT('Ctrl Pts',(1.73775617832987,0.326119768457322,3.89223750536792)) ;
#74165=CARTESIAN_POINT('Ctrl Pts',(1.76205976840444,-0.131724814356606,
3.86026178663595)) ;
#74166=CARTESIAN_POINT('Ctrl Pts',(1.73063030439237,-0.356586174100122,
3.8445413022737)) ;
#74167=CARTESIAN_POINT('Ctrl Pts',(1.58169958013592,-0.790134521566633,
3.81069820261749)) ;
#74168=CARTESIAN_POINT('Ctrl Pts',(1.46251953418115,-0.993555520508037,
3.7934234692482)) ;
#74169=CARTESIAN_POINT('Ctrl Pts',(1.15712036235999,-1.33538996225157,3.76141881239911)) ;
#74170=CARTESIAN_POINT('Ctrl Pts',(0.976362057983705,-1.47273139649564,
3.74573752054108)) ;
#74171=CARTESIAN_POINT('Ctrl Pts',(0.565241334081197,-1.67527683800978,
3.7119094332185)) ;
#74172=CARTESIAN_POINT('Ctrl Pts',(0.337404018862843,-1.73557998459742,
3.69463273816068)) ;
#74173=CARTESIAN_POINT('Ctrl Pts',(-0.12006516187297,-1.76288584741123,
3.66259769051253)) ;
#74174=CARTESIAN_POINT('Ctrl Pts',(-0.345068736274904,-1.73295537074502,
3.64695668443386)) ;
#74175=CARTESIAN_POINT('Ctrl Pts',(-0.779393877244594,-1.58699641468622,
3.61314462029586)) ;
#74176=CARTESIAN_POINT('Ctrl Pts',(-0.98348041604981,-1.4692879367239,3.59586606029122)) ;
#74177=CARTESIAN_POINT('Ctrl Pts',(-1.32727167564188,-1.1664137051595,3.56379915151923)) ;
#74178=CARTESIAN_POINT('Ctrl Pts',(-1.46583783176088,-0.986667587364208,
3.54819940101925)) ;
#74179=CARTESIAN_POINT('Ctrl Pts',(-1.67117528248908,-0.577187848274536,
3.51440442280493)) ;
#74180=CARTESIAN_POINT('Ctrl Pts',(-1.73306962205852,-0.349956915545484,
3.49712412561418)) ;
#74181=CARTESIAN_POINT('Ctrl Pts',(-1.75129362080061,-0.0781760192814626,
3.47803555211733)) ;
#74182=CARTESIAN_POINT('Ctrl Pts',(-1.75259999999999,-0.0390693720068885,
3.47532613812762)) ;
#74183=CARTESIAN_POINT('Ctrl Pts',(-1.7526,-4.1799203808425E-13,3.47265625000003)) ;
#74184=CARTESIAN_POINT('Ctrl Pts',(-1.7526,5.20417042793042E-16,3.3734375)) ;
#74185=CARTESIAN_POINT('Ctrl Pts',(-1.7526,-0.110290712389861,3.38097444898255)) ;
#74186=CARTESIAN_POINT('Ctrl Pts',(-1.74219157692512,-0.220571031733036,
3.38880531021715)) ;
#74187=CARTESIAN_POINT('Ctrl Pts',(-1.6781174386689,-0.555412544065956,
3.41350110557992)) ;
#74188=CARTESIAN_POINT('Ctrl Pts',(-1.59077377474029,-0.770712973034604,
3.4306864792079)) ;
#74189=CARTESIAN_POINT('Ctrl Pts',(-1.34036001264139,-1.15149977671283,
3.46379660228058)) ;
#74190=CARTESIAN_POINT('Ctrl Pts',(-1.18116471893329,-1.31429332825069,
3.47875083345804)) ;
#74191=CARTESIAN_POINT('Ctrl Pts',(-0.805655132204611,-1.57343913115523,
3.51174749729369)) ;
#74192=CARTESIAN_POINT('Ctrl Pts',(-0.591851390805269,-1.66568295798028,
3.5289692964048)) ;
#74193=CARTESIAN_POINT('Ctrl Pts',(-0.145816340827931,-1.7610209202741,
3.56214869600973)) ;
#74194=CARTESIAN_POINT('Ctrl Pts',(0.0817046468911821,-1.76515776908648,
3.57710299755285)) ;
#74195=CARTESIAN_POINT('Ctrl Pts',(0.531076123027321,-1.68606731810649,
3.61005049424702)) ;
#74196=CARTESIAN_POINT('Ctrl Pts',(0.748231261236104,-1.60156493198531,
3.62728218768916)) ;
#74197=CARTESIAN_POINT('Ctrl Pts',(1.13276017984804,-1.35619220140093,3.66050534385486)) ;
#74198=CARTESIAN_POINT('Ctrl Pts',(1.29757141623345,-1.19946318792092,3.67546453578996)) ;
#74199=CARTESIAN_POINT('Ctrl Pts',(1.56205098033292,-0.827608010919695,
3.70836244610627)) ;
#74200=CARTESIAN_POINT('Ctrl Pts',(1.65738980324903,-0.614809925134019,
3.72560312906785)) ;
#74201=CARTESIAN_POINT('Ctrl Pts',(1.75881857792582,-0.170033544249094,
3.75886892236587)) ;
#74202=CARTESIAN_POINT('Ctrl Pts',(1.76609340287348,0.0571742758199495,
3.77383767859007)) ;
#74203=CARTESIAN_POINT('Ctrl Pts',(1.69329679860401,0.507697700798713,3.80668574151523)) ;
#74204=CARTESIAN_POINT('Ctrl Pts',(1.6116753741927,0.726296042245817,3.82393451034011)) ;
#74205=CARTESIAN_POINT('Ctrl Pts',(1.3714561522033,1.11418980751476,3.85724173437944)) ;
#74206=CARTESIAN_POINT('Ctrl Pts',(1.21713546460311,1.28097332671082,3.8722245352361)) ;
#74207=CARTESIAN_POINT('Ctrl Pts',(0.848887625573543,1.55063619792425,3.9050226500038)) ;
#74208=CARTESIAN_POINT('Ctrl Pts',(0.637113785841988,1.64898751954791,3.92227861121472)) ;
#74209=CARTESIAN_POINT('Ctrl Pts',(0.193604384633389,1.75635710844691,3.95562598441266)) ;
#74210=CARTESIAN_POINT('Ctrl Pts',(-0.0333006902295665,1.7666817120298,
3.97062707387792)) ;
#74211=CARTESIAN_POINT('Ctrl Pts',(-0.4848992414616,1.70000772939862,4.00337529992421)) ;
#74212=CARTESIAN_POINT('Ctrl Pts',(-0.704863455468664,1.62120653484239,
4.02063757866201)) ;
#74213=CARTESIAN_POINT('Ctrl Pts',(-1.09599481138453,1.38601427493407,4.05402375631231)) ;
#74214=CARTESIAN_POINT('Ctrl Pts',(-1.26468653960243,1.23402108015127,4.06904710460958)) ;
#74215=CARTESIAN_POINT('Ctrl Pts',(-1.53933410450875,0.869294862158893,
4.10174565949343)) ;
#74216=CARTESIAN_POINT('Ctrl Pts',(-1.6405861752385,0.658550076098389,4.11901340721298)) ;
#74217=CARTESIAN_POINT('Ctrl Pts',(-1.73431865952934,0.292042822720498,
4.14671266180152)) ;
#74218=CARTESIAN_POINT('Ctrl Pts',(-1.75260000000002,0.146174356133978,
4.15719836636521)) ;
#74219=CARTESIAN_POINT('Ctrl Pts',(-1.7526,-2.89004931097736E-13,4.16718750000002)) ;
#74220=CARTESIAN_POINT('Origin',(0.,0.,0.)) ;
#74221=CARTESIAN_POINT('',(-1.7526,-2.15134495268842E-14,5.06015625000001)) ;
#74222=CARTESIAN_POINT('',(-1.7526,-2.79050850736062E-13,4.96093750000004)) ;
#74223=CARTESIAN_POINT('',(-1.7526,-2.14631598018565E-16,0.)) ;
#74224=CARTESIAN_POINT('Ctrl Pts',(-1.7526,-4.34374758384592E-14,5.06015625000001)) ;
#74225=CARTESIAN_POINT('Ctrl Pts',(-1.75260000000001,0.209553021544105,
5.04583600128375)) ;
#74226=CARTESIAN_POINT('Ctrl Pts',(-1.71502071246155,0.417566653426324,
5.03055722471029)) ;
#74227=CARTESIAN_POINT('Ctrl Pts',(-1.55945751550078,0.833354407293773,
4.99774009293334)) ;
#74228=CARTESIAN_POINT('Ctrl Pts',(-1.43434040293718,1.03396849796978,4.98048912002016)) ;
#74229=CARTESIAN_POINT('Ctrl Pts',(-1.11874264416212,1.36775444830488,4.94874579101757)) ;
#74230=CARTESIAN_POINT('Ctrl Pts',(-0.933851894800391,1.50010250410655,
4.93268272773915)) ;
#74231=CARTESIAN_POINT('Ctrl Pts',(-0.516107355713871,1.69115436333346,
4.89872732717594)) ;
#74232=CARTESIAN_POINT('Ctrl Pts',(-0.285903620642897,1.74489672691016,
4.88147462838478)) ;
#74233=CARTESIAN_POINT('Ctrl Pts',(0.173197292714659,1.75850207685975,4.84971588173976)) ;
#74234=CARTESIAN_POINT('Ctrl Pts',(0.39755401614597,1.72172171026321,4.83367701009703)) ;
#74235=CARTESIAN_POINT('Ctrl Pts',(0.828242469633597,1.56216698635971,4.79972862271391)) ;
#74236=CARTESIAN_POINT('Ctrl Pts',(1.02919949925927,1.43775341500248,4.78247412889219)) ;
#74237=CARTESIAN_POINT('Ctrl Pts',(1.3639523869677,1.1233654135263,4.75069896576308)) ;
#74238=CARTESIAN_POINT('Ctrl Pts',(1.49689684607618,0.938968663923053,4.7346856328411)) ;
#74239=CARTESIAN_POINT('Ctrl Pts',(1.68933053643342,0.522009368276059,4.70074477921605)) ;
#74240=CARTESIAN_POINT('Ctrl Pts',(1.74386238587,0.29207915162885,4.68348842457198)) ;
#74241=CARTESIAN_POINT('Ctrl Pts',(1.75911059422777,-0.166837054428321,
4.65169579727879)) ;
#74242=CARTESIAN_POINT('Ctrl Pts',(1.72315300195766,-0.391271092051124,
4.63570938136785)) ;
#74243=CARTESIAN_POINT('Ctrl Pts',(1.56523325401132,-0.822408145766662,
4.60177661782992)) ;
#74244=CARTESIAN_POINT('Ctrl Pts',(1.44162220607035,-1.023752946598,4.58451834119889)) ;
#74245=CARTESIAN_POINT('Ctrl Pts',(1.12861370694019,-1.35960440722033,4.55270715318068)) ;
#74246=CARTESIAN_POINT('Ctrl Pts',(0.944778996204964,-1.49322756830232,
4.53674905734208)) ;
#74247=CARTESIAN_POINT('Ctrl Pts',(0.528715304794354,-1.68723084035202,
4.5028249778962)) ;
#74248=CARTESIAN_POINT('Ctrl Pts',(0.299099398954512,-1.7426592494988,4.48556472418351)) ;
#74249=CARTESIAN_POINT('Ctrl Pts',(-0.159603232089813,-1.75977495358756,
4.45373383035843)) ;
#74250=CARTESIAN_POINT('Ctrl Pts',(-0.384125224424138,-1.72475213656398,
4.4378054746974)) ;
#74251=CARTESIAN_POINT('Ctrl Pts',(-0.815768038173584,-1.56868936870932,
4.40389071295291)) ;
#74252=CARTESIAN_POINT('Ctrl Pts',(-1.01754948783441,-1.44599111725407,
4.38662843476389)) ;
#74253=CARTESIAN_POINT('Ctrl Pts',(-1.35464482158062,-1.13455112137733,
4.35477664234939)) ;
#74254=CARTESIAN_POINT('Ctrl Pts',(-1.48903790883624,-0.95135381841529,
4.33887945488558)) ;
#74255=CARTESIAN_POINT('Ctrl Pts',(-1.68481791220455,-0.536308650653891,
4.30497468596644)) ;
#74256=CARTESIAN_POINT('Ctrl Pts',(-1.74126092919167,-0.307053205314894,
4.2877103454328)) ;
#74257=CARTESIAN_POINT('Ctrl Pts',(-1.75208741637621,-0.0489626096197369,
4.26976672270769)) ;
#74258=CARTESIAN_POINT('Ctrl Pts',(-1.7526,-0.0244726012247594,4.26807863693907)) ;
#74259=CARTESIAN_POINT('Ctrl Pts',(-1.7526,-1.39191904090825E-13,4.26640625000002)) ;
#74260=CARTESIAN_POINT('Ctrl Pts',(-1.7526,-2.88935542158687E-13,4.16718750000002)) ;
#74261=CARTESIAN_POINT('Ctrl Pts',(-1.75259999999999,-0.0778592500677814,
4.17250817644559)) ;
#74262=CARTESIAN_POINT('Ctrl Pts',(-1.74741231880974,-0.155785145504359,
4.17798025057415)) ;
#74263=CARTESIAN_POINT('Ctrl Pts',(-1.70616780214948,-0.462906643552702,
4.20013552125307)) ;
#74264=CARTESIAN_POINT('Ctrl Pts',(-1.63009713754219,-0.684150006894371,
4.21740792254869)) ;
#74265=CARTESIAN_POINT('Ctrl Pts',(-1.39975666801596,-1.07836487569639,
4.2508674830185)) ;
#74266=CARTESIAN_POINT('Ctrl Pts',(-1.24999034087451,-1.24888442921395,
4.26594601436367)) ;
#74267=CARTESIAN_POINT('Ctrl Pts',(-0.888665008594113,-1.52827751968141,
4.29854649013608)) ;
#74268=CARTESIAN_POINT('Ctrl Pts',(-0.678940366934257,-1.63229381110136,
4.31582276860299)) ;
#74269=CARTESIAN_POINT('Ctrl Pts',(-0.237928042188737,-1.75087446783154,
4.34931684107538)) ;
#74270=CARTESIAN_POINT('Ctrl Pts',(-0.0115868232081193,-1.76692803281445,
4.36442761836085)) ;
#74271=CARTESIAN_POINT('Ctrl Pts',(0.441913018063719,-1.7117638375004,4.3969799752066)) ;
#74272=CARTESIAN_POINT('Ctrl Pts',(0.664342551661163,-1.63830877582951,
4.41425939828048)) ;
#74273=CARTESIAN_POINT('Ctrl Pts',(1.06146566052312,-1.41260316424873,4.44778650445482)) ;
#74274=CARTESIAN_POINT('Ctrl Pts',(1.2337191956317,-1.26494693200175,4.46293215457177)) ;
#74275=CARTESIAN_POINT('Ctrl Pts',(1.51758671909389,-0.906871654067533,
4.49543718502358)) ;
#74276=CARTESIAN_POINT('Ctrl Pts',(1.62421107924902,-0.698145300472901,
4.51271906777459)) ;
#74277=CARTESIAN_POINT('Ctrl Pts',(1.74797322130534,-0.25833414777866,4.54627772356529)) ;
#74278=CARTESIAN_POINT('Ctrl Pts',(1.76666420047231,-0.0322502404855705,
4.56146050813967)) ;
#74279=CARTESIAN_POINT('Ctrl Pts',(1.71679968828143,0.422073094209958,4.593919126474)) ;
#74280=CARTESIAN_POINT('Ctrl Pts',(1.64582462485974,0.64559257787106,4.61120283436381)) ;
#74281=CARTESIAN_POINT('Ctrl Pts',(1.42450323936098,1.04543338478737,4.64479155957741)) ;
#74282=CARTESIAN_POINT('Ctrl Pts',(1.27882812276648,1.21931673326615,4.66001337566066)) ;
#74283=CARTESIAN_POINT('Ctrl Pts',(0.923827775295789,1.50736471058222,4.69242660683217)) ;
#74284=CARTESIAN_POINT('Ctrl Pts',(0.716066272743709,1.61642680955421,4.7097115574711)) ;
#74285=CARTESIAN_POINT('Ctrl Pts',(0.277408009498461,1.74504501462892,4.74332888461807)) ;
#74286=CARTESIAN_POINT('Ctrl Pts',(0.0515634108557028,1.76620249745117,
4.75859127085426)) ;
#74287=CARTESIAN_POINT('Ctrl Pts',(-0.403500598482737,1.72129330343181,
4.79096023872994)) ;
#74288=CARTESIAN_POINT('Ctrl Pts',(-0.628013288176575,1.65264694722788,
4.80824590269585)) ;
#74289=CARTESIAN_POINT('Ctrl Pts',(-1.03037182335714,1.4354341131867,4.84189038488026)) ;
#74290=CARTESIAN_POINT('Ctrl Pts',(-1.20577370834242,1.29160291027468,4.85719453252823)) ;
#74291=CARTESIAN_POINT('Ctrl Pts',(-1.49769414797966,0.939484314067199,
4.88952044767104)) ;
#74292=CARTESIAN_POINT('Ctrl Pts',(-1.60901484935553,0.732644451246718,
4.9068063484703)) ;
#74293=CARTESIAN_POINT('Ctrl Pts',(-1.72711252303101,0.344486838563733,
4.93667481106522)) ;
#74294=CARTESIAN_POINT('Ctrl Pts',(-1.75260000000006,0.172594590798071,
4.94914288377783)) ;
#74295=CARTESIAN_POINT('Ctrl Pts',(-1.7526,-5.58962598429247E-13,4.96093750000004)) ;
#74296=CARTESIAN_POINT('Origin',(0.,0.,0.)) ;
#74297=CARTESIAN_POINT('',(-1.7526,-5.41548163298149E-15,5.85390625)) ;
#74298=CARTESIAN_POINT('',(-1.7526,-1.50126202001478E-13,5.75468750000002)) ;
#74299=CARTESIAN_POINT('',(-1.7526,-2.14631598018565E-16,0.)) ;
#74300=CARTESIAN_POINT('Ctrl Pts',(-1.7526,-1.04083408558608E-14,5.85390625)) ;
#74301=CARTESIAN_POINT('Ctrl Pts',(-1.7526,0.215063581698836,5.83920942550641)) ;
#74302=CARTESIAN_POINT('Ctrl Pts',(-1.71301637555779,0.428433931657122,
5.82350785119934)) ;
#74303=CARTESIAN_POINT('Ctrl Pts',(-1.55154324405163,0.848059638465521,
5.79026115724544)) ;
#74304=CARTESIAN_POINT('Ctrl Pts',(-1.42440027697519,1.04767049607852,5.77302139822362)) ;
#74305=CARTESIAN_POINT('Ctrl Pts',(-1.10531671400859,1.37865171095447,5.7413710670186)) ;
#74306=CARTESIAN_POINT('Ctrl Pts',(-0.918996616265576,1.50927478176608,
5.72515792892315)) ;
#74307=CARTESIAN_POINT('Ctrl Pts',(-0.498990396180971,1.69631661152442,
5.69116148014123)) ;
#74308=CARTESIAN_POINT('Ctrl Pts',(-0.268009804098051,1.74776715638448,
5.67392056576987)) ;
#74309=CARTESIAN_POINT('Ctrl Pts',(0.191609637137813,1.75661159116519,5.64226114764989)) ;
#74310=CARTESIAN_POINT('Ctrl Pts',(0.415742569592707,1.71744437932947,5.62606298203586)) ;
#74311=CARTESIAN_POINT('Ctrl Pts',(0.845111418224298,1.55314432567097,5.59207045057964)) ;
#74312=CARTESIAN_POINT('Ctrl Pts',(1.0449254130281,1.4264077591063,5.57482831338614)) ;
#74313=CARTESIAN_POINT('Ctrl Pts',(1.37647173126268,1.10802376181094,5.54315916666592)) ;
#74314=CARTESIAN_POINT('Ctrl Pts',(1.50744177625706,0.921991233292156,5.52697695775436)) ;
#74315=CARTESIAN_POINT('Ctrl Pts',(1.69529178381865,0.502438791650662,5.49298864247188)) ;
#74316=CARTESIAN_POINT('Ctrl Pts',(1.74720429850968,0.271612750237907,5.4757452130556)) ;
#74317=CARTESIAN_POINT('Ctrl Pts',(1.75700745513532,-0.187904271158755,
5.44406565627846)) ;
#74318=CARTESIAN_POINT('Ctrl Pts',(1.71832120043968,-0.412082242742052,
5.42790043764716)) ;
#74319=CARTESIAN_POINT('Ctrl Pts',(1.55497759964053,-0.841719178154872,
5.39391665942113)) ;
#74320=CARTESIAN_POINT('Ctrl Pts',(1.42870848978082,-1.04176565822851,5.37667186675926)) ;
#74321=CARTESIAN_POINT('Ctrl Pts',(1.11112897410725,-1.37396044897767,5.34498117708394)) ;
#74322=CARTESIAN_POINT('Ctrl Pts',(0.925426697440239,-1.5053290123611,5.32883403169105)) ;
#74323=CARTESIAN_POINT('Ctrl Pts',(0.506396164499377,-1.69410628171457,
5.29485513492282)) ;
#74324=CARTESIAN_POINT('Ctrl Pts',(0.275748699203071,-1.7465487915919,5.27760890675472)) ;
#74325=CARTESIAN_POINT('Ctrl Pts',(-0.18364951780585,-1.75745242646143,
5.24590631841395)) ;
#74326=CARTESIAN_POINT('Ctrl Pts',(-0.407879202904414,-1.71931804669363,
5.22977837814854)) ;
#74327=CARTESIAN_POINT('Ctrl Pts',(-0.837822397688919,-1.55707177860285,
5.1958047323155)) ;
#74328=CARTESIAN_POINT('Ctrl Pts',(-1.03813430276736,-1.43133945442896,
5.17855699561603)) ;
#74329=CARTESIAN_POINT('Ctrl Pts',(-1.37107173384084,-1.11468349854734,
5.14684169847491)) ;
#74330=CARTESIAN_POINT('Ctrl Pts',(-1.50289716039955,-0.929359773570224,
5.1307341431521)) ;
#74331=CARTESIAN_POINT('Ctrl Pts',(-1.69273615719116,-0.510928497408213,
5.09676614443656)) ;
#74332=CARTESIAN_POINT('Ctrl Pts',(-1.74578545348992,-0.280487150192089,
5.07951682599002)) ;
#74333=CARTESIAN_POINT('Ctrl Pts',(-1.75239538719435,-0.0309314004765573,
5.06227580444235)) ;
#74334=CARTESIAN_POINT('Ctrl Pts',(-1.7526,-0.0154618997563056,5.06121287160586)) ;
#74335=CARTESIAN_POINT('Ctrl Pts',(-1.7526,-4.28122674557499E-14,5.06015625000001)) ;
#74336=CARTESIAN_POINT('Ctrl Pts',(-1.7526,-5.57887069874106E-13,4.96093750000004)) ;
#74337=CARTESIAN_POINT('Ctrl Pts',(-1.75259999999998,-0.0514754444292417,
4.96445518331268)) ;
#74338=CARTESIAN_POINT('Ctrl Pts',(-1.75033229848047,-0.103004617511181,
4.96804072820716)) ;
#74339=CARTESIAN_POINT('Ctrl Pts',(-1.72527339535509,-0.386268440786449,
4.988107481689)) ;
#74340=CARTESIAN_POINT('Ctrl Pts',(-1.65879384324703,-0.611679371540988,
5.00539319495447)) ;
#74341=CARTESIAN_POINT('Ctrl Pts',(-1.44539751850817,-1.01635167457427,
5.03908776263559)) ;
#74342=CARTESIAN_POINT('Ctrl Pts',(-1.30326860888275,-1.19315682040023,
5.05447769671142)) ;
#74343=CARTESIAN_POINT('Ctrl Pts',(-0.953826774202952,-1.4886359567931,
5.08672142273433)) ;
#74344=CARTESIAN_POINT('Ctrl Pts',(-0.747857632971182,-1.60203231349978,
5.10400657476385)) ;
#74345=CARTESIAN_POINT('Ctrl Pts',(-0.311322981091731,-1.73931875691161,
5.13772414497515)) ;
#74346=CARTESIAN_POINT('Ctrl Pts',(-0.0859013110107367,-1.76486779209003,
5.15315749824057)) ;
#74347=CARTESIAN_POINT('Ctrl Pts',(0.370411258410795,-1.7287761040988,5.18536219937763)) ;
#74348=CARTESIAN_POINT('Ctrl Pts',(0.596629075374267,-1.6642956856852,5.20264646512087)) ;
#74349=CARTESIAN_POINT('Ctrl Pts',(1.00341199399925,-1.45441565979707,5.23638573326439)) ;
#74350=CARTESIAN_POINT('Ctrl Pts',(1.18150397822415,-1.31384645521521,5.2518624900127)) ;
#74351=CARTESIAN_POINT('Ctrl Pts',(1.48022953107292,-0.966870472196266,
5.28402960043137)) ;
#74352=CARTESIAN_POINT('Ctrl Pts',(1.59551918713128,-0.761715580467981,
5.30131270103304)) ;
#74353=CARTESIAN_POINT('Ctrl Pts',(1.73660710597921,-0.326138942781364,
5.33507240848899)) ;
#74354=CARTESIAN_POINT('Ctrl Pts',(1.76407804995685,-0.100901126708342,
5.35059230869242)) ;
#74355=CARTESIAN_POINT('Ctrl Pts',(1.73184195511883,0.355929701719502,5.38272328911981)) ;
#74356=CARTESIAN_POINT('Ctrl Pts',(1.66919160755838,0.582868013518023,5.40000498912339)) ;
#74357=CARTESIAN_POINT('Ctrl Pts',(1.46252684911046,0.991563221616929,5.43378392573789)) ;
#74358=CARTESIAN_POINT('Ctrl Pts',(1.32337677146238,1.17082696103987,5.44934649035458)) ;
#74359=CARTESIAN_POINT('Ctrl Pts',(0.978655074350586,1.47249420866847,5.4814428174617)) ;
#74360=CARTESIAN_POINT('Ctrl Pts',(0.774254492279916,1.58949907634077,5.49872292177171)) ;
#74361=CARTESIAN_POINT('Ctrl Pts',(0.339562078660178,1.73403937841308,5.53251992761676)) ;
#74362=CARTESIAN_POINT('Ctrl Pts',(0.114490432682257,1.76325387278217,5.54812448403179)) ;
#74363=CARTESIAN_POINT('Ctrl Pts',(-0.342795796134348,1.73451329405964,
5.58018764057103)) ;
#74364=CARTESIAN_POINT('Ctrl Pts',(-0.570374083439141,1.67352630851254,
5.59746599126339)) ;
#74365=CARTESIAN_POINT('Ctrl Pts',(-0.98079126107425,1.46978121726822,5.63127995774103)) ;
#74366=CARTESIAN_POINT('Ctrl Pts',(-1.16111506906919,1.33191414004616,5.64692566486227)) ;
#74367=CARTESIAN_POINT('Ctrl Pts',(-1.46543165464954,0.98923897254071,5.67895713062485)) ;
#74368=CARTESIAN_POINT('Ctrl Pts',(-1.58398081695685,0.785531195556426,
5.69623360368484)) ;
#74369=CARTESIAN_POINT('Ctrl Pts',(-1.72110925026966,0.382583025914159,
5.72765149797256)) ;
#74370=CARTESIAN_POINT('Ctrl Pts',(-1.75260000000003,0.191839612966701,
5.74157773450451)) ;
#74371=CARTESIAN_POINT('Ctrl Pts',(-1.7526,-2.99725522179273E-13,5.75468750000002)) ;
#74372=CARTESIAN_POINT('Origin',(0.,0.,0.)) ;
#74373=CARTESIAN_POINT('',(1.24732203685813,1.23117606229494,6.24999999831013)) ;
#74374=CARTESIAN_POINT('Ctrl Pts',(-1.7526,-3.00037772404938E-13,5.75468750000002)) ;
#74375=CARTESIAN_POINT('Ctrl Pts',(-1.75259999999999,-0.032598322299679,
5.75691517526626)) ;
#74376=CARTESIAN_POINT('Ctrl Pts',(-1.75169052435328,-0.0652248173994592,
5.75917051954304)) ;
#74377=CARTESIAN_POINT('Ctrl Pts',(-1.73683227675797,-0.330958761491049,
5.77775059029158)) ;
#74378=CARTESIAN_POINT('Ctrl Pts',(-1.67734733744449,-0.559102898338026,
5.79502509234845)) ;
#74379=CARTESIAN_POINT('Ctrl Pts',(-1.47623678512082,-0.971062086850928,
5.8288698617205)) ;
#74380=CARTESIAN_POINT('Ctrl Pts',(-1.33952292301057,-1.15233928101824,
5.84459479373804)) ;
#74381=CARTESIAN_POINT('Ctrl Pts',(-0.998693925502225,-1.45902877365591,
5.87656726545657)) ;
#74382=CARTESIAN_POINT('Ctrl Pts',(-0.795617527723386,-1.57896062756801,
5.89383973057284)) ;
#74383=CARTESIAN_POINT('Ctrl Pts',(-0.362470600691468,-1.72941212332175,
5.9276984455155)) ;
#74384=CARTESIAN_POINT('Ctrl Pts',(-0.137681826299413,-1.76160826471163,
5.94346123196741)) ;
#74385=CARTESIAN_POINT('Ctrl Pts',(0.320350778809865,-1.73883941048927,
5.97540635712271)) ;
#74386=CARTESIAN_POINT('Ctrl Pts',(0.54899323602356,-1.68070291513661,5.99267674368556)) ;
#74387=CARTESIAN_POINT('Ctrl Pts',(0.962326432463704,-1.48195606680838,
6.02654850141181)) ;
#74388=CARTESIAN_POINT('Ctrl Pts',(1.14445650561047,-1.34627333654908,6.04234785886134)) ;
#74389=CARTESIAN_POINT('Ctrl Pts',(1.45326081358979,-1.00710025443336,6.07426703240116)) ;
#74390=CARTESIAN_POINT('Ctrl Pts',(1.57442451607132,-0.804595233816516,
6.09153532015318)) ;
#74391=CARTESIAN_POINT('Ctrl Pts',(1.72737162339113,-0.372112789748117,
6.12541926742668)) ;
#74392=CARTESIAN_POINT('Ctrl Pts',(1.76082533135169,-0.147442862085292,
6.14125385278895)) ;
#74393=CARTESIAN_POINT('Ctrl Pts',(1.74137248937904,0.292789957304284,6.17188872838747)) ;
#74394=CARTESIAN_POINT('Ctrl Pts',(1.69217994490562,0.504581831709392,6.18775442585301)) ;
#74395=CARTESIAN_POINT('Ctrl Pts',(1.51977635982089,0.898901097711236,6.21958114983884)) ;
#74396=CARTESIAN_POINT('Ctrl Pts',(1.3982679007908,1.07825065364772,6.23527681869574)) ;
#74397=CARTESIAN_POINT('Ctrl Pts',(1.24732203681668,1.23117606233693,6.24999999746791)) ;
#74398=CARTESIAN_POINT('',(1.57068438372304,-0.777603252442184,6.25000631418241)) ;
#74399=CARTESIAN_POINT('Origin',(0.,0.,6.25)) ;
#74400=CARTESIAN_POINT('',(1.35494872380545,-1.11162979288941,6.16356193246049)) ;
#74401=CARTESIAN_POINT('Ctrl Pts',(1.3549489689189,-1.11162945787956,6.16355972756376)) ;
#74402=CARTESIAN_POINT('Ctrl Pts',(1.44940645924245,-0.996496597542542,
6.17410130374198)) ;
#74403=CARTESIAN_POINT('Ctrl Pts',(1.50897892716071,-0.894016315078257,
6.19049173038489)) ;
#74404=CARTESIAN_POINT('Ctrl Pts',(1.54943011338412,-0.81923740960474,6.21567530064911)) ;
#74405=CARTESIAN_POINT('Ctrl Pts',(1.5604493439252,-0.797983948328948,6.22382703793116)) ;
#74406=CARTESIAN_POINT('Ctrl Pts',(1.5675598412834,-0.783817595875971,6.23657317890588)) ;
#74407=CARTESIAN_POINT('Ctrl Pts',(1.56873001705364,-0.781470558754527,
6.23913690798495)) ;
#74408=CARTESIAN_POINT('Ctrl Pts',(1.57003590014195,-0.77884225486478,6.24379691046241)) ;
#74409=CARTESIAN_POINT('Ctrl Pts',(1.57040611261523,-0.778094809706397,
6.24570740151285)) ;
#74410=CARTESIAN_POINT('Ctrl Pts',(1.57062599767995,-0.777650791220551,
6.24850359260972)) ;
#74411=CARTESIAN_POINT('Ctrl Pts',(1.57065531335762,-0.777591567997932,
6.24925253303392)) ;
#74412=CARTESIAN_POINT('Ctrl Pts',(1.57065531335762,-0.777591567997932,
6.25)) ;
#74413=CARTESIAN_POINT('Ctrl Pts',(1.354948802545,-1.11162966067026,6.16355970899623)) ;
#74414=CARTESIAN_POINT('Ctrl Pts',(1.2691105239076,-1.21625665738258,6.15398004999797)) ;
#74415=CARTESIAN_POINT('Ctrl Pts',(1.17146411011478,-1.31057075856948,6.1449103765824)) ;
#74416=CARTESIAN_POINT('Ctrl Pts',(0.953918635023722,-1.47675496499653,
6.12533991001694)) ;
#74417=CARTESIAN_POINT('Ctrl Pts',(0.834365619456194,-1.54744734708524,
6.1151689721293)) ;
#74418=CARTESIAN_POINT('Ctrl Pts',(0.493385532353786,-1.69796606169852,
6.0876067703235)) ;
#74419=CARTESIAN_POINT('Ctrl Pts',(0.2621558383588,-1.74866546389136,6.07037009501047)) ;
#74420=CARTESIAN_POINT('Ctrl Pts',(-0.197627883205035,-1.75595205213961,
6.03874354709929)) ;
#74421=CARTESIAN_POINT('Ctrl Pts',(-0.421687652843615,-1.716002974801,6.02249091157781)) ;
#74422=CARTESIAN_POINT('Ctrl Pts',(-0.850618335952917,-1.55014782434877,
5.98848430427106)) ;
#74423=CARTESIAN_POINT('Ctrl Pts',(-1.05005207636958,-1.42265205221592,
5.97124666237111)) ;
#74424=CARTESIAN_POINT('Ctrl Pts',(-1.38054170467941,-1.10296105685791,
5.93961273069518)) ;
#74425=CARTESIAN_POINT('Ctrl Pts',(-1.51086317209616,-0.916390969524942,
5.92337240531497)) ;
#74426=CARTESIAN_POINT('Ctrl Pts',(-1.69720186521872,-0.495990785382188,
5.88936893726401)) ;
#74427=CARTESIAN_POINT('Ctrl Pts',(-1.74825045640576,-0.264876556215191,
5.87213026828475)) ;
#74428=CARTESIAN_POINT('Ctrl Pts',(-1.75251138476543,-0.0203541928781188,
5.85529970515546)) ;
#74429=CARTESIAN_POINT('Ctrl Pts',(-1.7526,-0.0101753703444853,5.85460160544293)) ;
#74430=CARTESIAN_POINT('Ctrl Pts',(-1.7526,-1.06163316679444E-14,5.85390625)) ;
#74431=CARTESIAN_POINT('Origin',(3.10601593664312E-15,-2.12330153459561E-14,
-0.34726562499997)) ;
#74432=CARTESIAN_POINT('',(-0.194635088948059,-1.22163646928425,0.0797567518094987)) ;
#74433=CARTESIAN_POINT('Ctrl Pts',(-1.55774404735361E-13,-1.23704425180961,
0.0992187500000006)) ;
#74434=CARTESIAN_POINT('Ctrl Pts',(-0.0650557921671749,-1.2370442518096,
0.0929202058933744)) ;
#74435=CARTESIAN_POINT('Ctrl Pts',(-0.130120178037894,-1.23191519437095,
0.0864151383895563)) ;
#74436=CARTESIAN_POINT('Ctrl Pts',(-0.194635088950127,-1.22163646928396,
0.0797567518093028)) ;
#74437=CARTESIAN_POINT('Origin',(-2.4980018054066E-14,3.26683124995952E-13,
0.0797567518098535)) ;
#74438=CARTESIAN_POINT('Ctrl Pts',(-3.31205160669424,-0.887893661760288,
6.793484)) ;
#74439=CARTESIAN_POINT('Ctrl Pts',(-3.31287790153464,-0.884811388204761,
6.79777468341573)) ;
#74440=CARTESIAN_POINT('Ctrl Pts',(-3.31364139250918,-0.881705147287936,
6.80206837154771)) ;
#74441=CARTESIAN_POINT('Ctrl Pts',(-3.3271818086533,-0.821152481751811,
6.88564197720954)) ;
#74442=CARTESIAN_POINT('Ctrl Pts',(-3.31839899815499,-0.75612836629395,
6.96625435392858)) ;
#74443=CARTESIAN_POINT('Ctrl Pts',(-3.2794239181545,-0.707077062047013,
7.03908289042949)) ;
#74444=CARTESIAN_POINT('Ctrl Pts',(-3.31205160669424,-0.887893661760288,
6.793484)) ;
#74445=CARTESIAN_POINT('Ctrl Pts',(-3.31274522369532,-0.885306307663954,
6.79809343284722)) ;
#74446=CARTESIAN_POINT('Ctrl Pts',(-3.31334303732996,-0.882699040456771,
6.80271791145202)) ;
#74447=CARTESIAN_POINT('Ctrl Pts',(-3.32434030414173,-0.831838892965903,
6.89249111240127)) ;
#74448=CARTESIAN_POINT('Ctrl Pts',(-3.30868757227878,-0.775373519472582,
6.97904841531997)) ;
#74449=CARTESIAN_POINT('Ctrl Pts',(-3.26540522272929,-0.738492188311658,
7.04973176535319)) ;
#74450=CARTESIAN_POINT('Ctrl Pts',(-3.31205160669424,-0.887893661760288,
6.793484)) ;
#74451=CARTESIAN_POINT('Ctrl Pts',(-3.31261121114413,-0.885806205911472,
6.79841624482425)) ;
#74452=CARTESIAN_POINT('Ctrl Pts',(-3.31307594580977,-0.883698810455709,
6.8033633352161)) ;
#74453=CARTESIAN_POINT('Ctrl Pts',(-3.32193595542266,-0.842609793416927,
6.89941056353899)) ;
#74454=CARTESIAN_POINT('Ctrl Pts',(-3.30625449205529,-0.797119135192663,
6.99229450465509)) ;
#74455=CARTESIAN_POINT('Ctrl Pts',(-3.26888725785268,-0.772941191040195,
7.07185431702686)) ;
#74456=CARTESIAN_POINT('Ctrl Pts',(-3.31205160669424,-0.887893661760288,
6.793484)) ;
#74457=CARTESIAN_POINT('Ctrl Pts',(-3.31247680269833,-0.886307580938716,
6.79874217767331)) ;
#74458=CARTESIAN_POINT('Ctrl Pts',(-3.31286385709175,-0.884707693083396,
6.8040040381699)) ;
#74459=CARTESIAN_POINT('Ctrl Pts',(-3.31959859765461,-0.853484701399462,
6.90642242752541)) ;
#74460=CARTESIAN_POINT('Ctrl Pts',(-3.31286250738096,-0.819472008973412,
7.00521187075637)) ;
#74461=CARTESIAN_POINT('Ctrl Pts',(-3.2881405032392,-0.793313315480957,
7.09446231571417)) ;
#74462=CARTESIAN_POINT('',(-3.2881405032392,-0.793313315480957,7.09446231571417)) ;
#74463=CARTESIAN_POINT('',(-3.27942391815471,-0.707077062047147,7.03908289042914)) ;
#74464=CARTESIAN_POINT('Origin',(-3.36081883130047,-0.724626630961913,7.09446231571417)) ;
#74465=CARTESIAN_POINT('',(-3.31205160669424,-0.887893661760289,6.793484)) ;
#74466=CARTESIAN_POINT('Ctrl Pts',(-3.2794239181545,-0.707077062047013,
7.03908289042949)) ;
#74467=CARTESIAN_POINT('Ctrl Pts',(-3.31839899815499,-0.75612836629395,
6.96625435392858)) ;
#74468=CARTESIAN_POINT('Ctrl Pts',(-3.3271818086533,-0.821152481751811,
6.88564197720954)) ;
#74469=CARTESIAN_POINT('Ctrl Pts',(-3.31364139250918,-0.881705147287936,
6.80206837154771)) ;
#74470=CARTESIAN_POINT('Ctrl Pts',(-3.31287790153464,-0.884811388204761,
6.79777468341573)) ;
#74471=CARTESIAN_POINT('Ctrl Pts',(-3.31205160669424,-0.887893661760288,
6.793484)) ;
#74472=CARTESIAN_POINT('Ctrl Pts',(-3.31205160669424,-0.887893661760289,
6.793484)) ;
#74473=CARTESIAN_POINT('Ctrl Pts',(-3.31247680269833,-0.886307580938716,
6.79874217767331)) ;
#74474=CARTESIAN_POINT('Ctrl Pts',(-3.31286385709175,-0.884707693083396,
6.8040040381699)) ;
#74475=CARTESIAN_POINT('Ctrl Pts',(-3.31959859765461,-0.853484701399462,
6.90642242752541)) ;
#74476=CARTESIAN_POINT('Ctrl Pts',(-3.31286250738096,-0.819472008973412,
7.00521187075637)) ;
#74477=CARTESIAN_POINT('Ctrl Pts',(-3.2881405032392,-0.793313315480957,
7.09446231571417)) ;
#74478=CARTESIAN_POINT('Ctrl Pts',(-3.25930415002282,-0.772122965994088,
7.15495237069481)) ;
#74479=CARTESIAN_POINT('Ctrl Pts',(-3.27166340593034,-0.778151805203039,
7.1395492738358)) ;
#74480=CARTESIAN_POINT('Ctrl Pts',(-3.28134410254902,-0.786121950190065,
7.11899842460839)) ;
#74481=CARTESIAN_POINT('Ctrl Pts',(-3.28814050323922,-0.793313315480977,
7.0944623157141)) ;
#74482=CARTESIAN_POINT('Ctrl Pts',(-3.24720304082971,-0.766220050630805,
7.13091195407385)) ;
#74483=CARTESIAN_POINT('Ctrl Pts',(-3.25869714385255,-0.769669020390238,
7.11948103534319)) ;
#74484=CARTESIAN_POINT('Ctrl Pts',(-3.26931499881139,-0.775745323042673,
7.10257847346906)) ;
#74485=CARTESIAN_POINT('Ctrl Pts',(-3.27713864873267,-0.781672101514855,
7.0815434593213)) ;
#74486=CARTESIAN_POINT('Ctrl Pts',(-3.23542257587948,-0.737017859268681,
7.08914722322202)) ;
#74487=CARTESIAN_POINT('Ctrl Pts',(-3.24613293999889,-0.741135418665641,
7.08437187855016)) ;
#74488=CARTESIAN_POINT('Ctrl Pts',(-3.25765493730861,-0.747264169147483,
7.07395698641591)) ;
#74489=CARTESIAN_POINT('Ctrl Pts',(-3.26627246770002,-0.753460431697837,
7.05898639091382)) ;
#74490=CARTESIAN_POINT('Ctrl Pts',(-3.24626907090961,-0.691101901539863,
7.07061000050612)) ;
#74491=CARTESIAN_POINT('Ctrl Pts',(-3.25699307007247,-0.701213312565526,
7.06492336370951)) ;
#74492=CARTESIAN_POINT('Ctrl Pts',(-3.26646853336989,-0.711672429614719,
7.05583711304386)) ;
#74493=CARTESIAN_POINT('Ctrl Pts',(-3.27341590582957,-0.720540687589137,
7.04364669396793)) ;
#74494=CARTESIAN_POINT('Ctrl Pts',(-3.25413500684155,-0.672122965994088,
7.06837618534741)) ;
#74495=CARTESIAN_POINT('Ctrl Pts',(-3.2651569253511,-0.68462662701825,7.0606746369179)) ;
#74496=CARTESIAN_POINT('Ctrl Pts',(-3.27351027276397,-0.697039528212523,
7.05095544131491)) ;
#74497=CARTESIAN_POINT('Ctrl Pts',(-3.27942391815468,-0.707077062047158,
7.03908289042919)) ;
#74498=CARTESIAN_POINT('',(-3.25930415002282,-0.772122965994088,7.15495237069481)) ;
#74499=CARTESIAN_POINT('Ctrl Pts',(-3.28814050323922,-0.793313315480977,
7.0944623157141)) ;
#74500=CARTESIAN_POINT('Ctrl Pts',(-3.28134410254902,-0.786121950190065,
7.11899842460839)) ;
#74501=CARTESIAN_POINT('Ctrl Pts',(-3.27166340593034,-0.778151805203039,
7.1395492738358)) ;
#74502=CARTESIAN_POINT('Ctrl Pts',(-3.25930415002282,-0.772122965994088,
7.15495237069481)) ;
#74503=CARTESIAN_POINT('',(-3.25413500684155,-0.672122965994088,7.06837618534741)) ;
#74504=CARTESIAN_POINT('Origin',(-3.30314612486771,-0.682245931988176,7.15495237069481)) ;
#74505=CARTESIAN_POINT('Ctrl Pts',(-3.25413500684155,-0.672122965994088,
7.06837618534741)) ;
#74506=CARTESIAN_POINT('Ctrl Pts',(-3.25939413791001,-0.678089113548593,
7.06470137568647)) ;
#74507=CARTESIAN_POINT('Ctrl Pts',(-3.26403592778485,-0.684033341438776,
7.06055993267684)) ;
#74508=CARTESIAN_POINT('Ctrl Pts',(-3.27227350301816,-0.695529889843682,
7.05122867472026)) ;
#74509=CARTESIAN_POINT('Ctrl Pts',(-3.27584190801,-0.701066725671648,7.04601233351152)) ;
#74510=CARTESIAN_POINT('Ctrl Pts',(-3.27902209145488,-0.706397160161627,
7.03988142131546)) ;
#74511=CARTESIAN_POINT('Ctrl Pts',(-3.27922442992735,-0.706738460440355,
7.03948339366763)) ;
#74512=CARTESIAN_POINT('Ctrl Pts',(-3.27942391815467,-0.707077062047157,
7.03908289042919)) ;
#74513=CARTESIAN_POINT('Ctrl Pts',(-3.25413500684155,-0.672122965994087,
7.06837618534741)) ;
#74514=CARTESIAN_POINT('Ctrl Pts',(-3.24907828834912,-0.668116125762003,
7.07170731541641)) ;
#74515=CARTESIAN_POINT('Ctrl Pts',(-3.23589756364382,-0.660507101185359,
7.07825767676847)) ;
#74516=CARTESIAN_POINT('Ctrl Pts',(-3.21994984969872,-0.659191608936345,
7.08122103082289)) ;
#74517=CARTESIAN_POINT('Ctrl Pts',(-3.2105035504766,-0.660979117346627,
7.08167176697949)) ;
#74518=CARTESIAN_POINT('Ctrl Pts',(-3.24364709226562,-0.697428213388454,
7.07135460555903)) ;
#74519=CARTESIAN_POINT('Ctrl Pts',(-3.23904198217673,-0.694613604341688,
7.07381433044803)) ;
#74520=CARTESIAN_POINT('Ctrl Pts',(-3.22806793638566,-0.689730698218501,
7.07820430178644)) ;
#74521=CARTESIAN_POINT('Ctrl Pts',(-3.21711227111321,-0.689553339863551,
7.08049944622424)) ;
#74522=CARTESIAN_POINT('Ctrl Pts',(-3.21048830525436,-0.691091935293639,
7.08136471265295)) ;
#74523=CARTESIAN_POINT('Ctrl Pts',(-3.23575890408185,-0.743524350516924,
7.09478029250273)) ;
#74524=CARTESIAN_POINT('Ctrl Pts',(-3.23142097756856,-0.74257695355463,
7.09766695337376)) ;
#74525=CARTESIAN_POINT('Ctrl Pts',(-3.22221828421189,-0.741823967860394,
7.10251922930311)) ;
#74526=CARTESIAN_POINT('Ctrl Pts',(-3.21582930459776,-0.742834159269564,
7.10502824890571)) ;
#74527=CARTESIAN_POINT('Ctrl Pts',(-3.21172314782629,-0.743501302288172,
7.10623570350962)) ;
#74528=CARTESIAN_POINT('Ctrl Pts',(-3.25022831812798,-0.767695779471626,
7.13692205822909)) ;
#74529=CARTESIAN_POINT('Ctrl Pts',(-3.24530748822128,-0.765971442670609,
7.14245586827297)) ;
#74530=CARTESIAN_POINT('Ctrl Pts',(-3.23346592056584,-0.762891866825046,
7.15309078996572)) ;
#74531=CARTESIAN_POINT('Ctrl Pts',(-3.22141912805696,-0.761902076472111,
7.15799343781877)) ;
#74532=CARTESIAN_POINT('Ctrl Pts',(-3.21434217223136,-0.761999999999958,
7.15898553043246)) ;
#74533=CARTESIAN_POINT('Ctrl Pts',(-3.25930415002282,-0.772122965994088,
7.15495237069481)) ;
#74534=CARTESIAN_POINT('Ctrl Pts',(-3.253958434241,-0.769515328354208,7.16161463083283)) ;
#74535=CARTESIAN_POINT('Ctrl Pts',(-3.24030166703836,-0.764233790350221,
7.17471535353693)) ;
#74536=CARTESIAN_POINT('Ctrl Pts',(-3.22454046181232,-0.762000000000339,
7.18064206164579)) ;
#74537=CARTESIAN_POINT('Ctrl Pts',(-3.21546217518166,-0.762,7.18154353395898)) ;
#74538=CARTESIAN_POINT('',(-3.2154621751798,-0.762,7.18154353395898)) ;
#74539=CARTESIAN_POINT('',(-3.2105035504766,-0.660979117346627,7.08167176697949)) ;
#74540=CARTESIAN_POINT('Origin',(-3.2154621751854,-0.662,7.18154353395898)) ;
#74541=CARTESIAN_POINT('Ctrl Pts',(-3.2105035504766,-0.660979117346627,
7.08167176697949)) ;
#74542=CARTESIAN_POINT('Ctrl Pts',(-3.21994984969872,-0.659191608936345,
7.08122103082289)) ;
#74543=CARTESIAN_POINT('Ctrl Pts',(-3.23589756364382,-0.660507101185359,
7.07825767676847)) ;
#74544=CARTESIAN_POINT('Ctrl Pts',(-3.24907828834912,-0.668116125762003,
7.07170731541641)) ;
#74545=CARTESIAN_POINT('Ctrl Pts',(-3.25413500684155,-0.672122965994087,
7.06837618534741)) ;
#74546=CARTESIAN_POINT('Ctrl Pts',(-3.25930415002282,-0.772122965994088,
7.15495237069481)) ;
#74547=CARTESIAN_POINT('Ctrl Pts',(-3.253958434241,-0.769515328354208,7.16161463083283)) ;
#74548=CARTESIAN_POINT('Ctrl Pts',(-3.24030166703836,-0.764233790350221,
7.17471535353693)) ;
#74549=CARTESIAN_POINT('Ctrl Pts',(-3.22454046181232,-0.762000000000339,
7.18064206164579)) ;
#74550=CARTESIAN_POINT('Ctrl Pts',(-3.21546217518166,-0.762,7.18154353395898)) ;
#74551=CARTESIAN_POINT('Ctrl Pts',(-3.2105035504766,-0.660979117346627,
7.08167176697949)) ;
#74552=CARTESIAN_POINT('Ctrl Pts',(-3.20871214489261,-0.66131810222033,
7.08175724503273)) ;
#74553=CARTESIAN_POINT('Ctrl Pts',(-3.20691819492506,-0.661658530855223,
7.0818)) ;
#74554=CARTESIAN_POINT('Ctrl Pts',(-3.20512388881539,-0.662,7.0818)) ;
#74555=CARTESIAN_POINT('Ctrl Pts',(-3.21048830525548,-0.691091935293675,
7.08136471265289)) ;
#74556=CARTESIAN_POINT('Ctrl Pts',(-3.20871266627196,-0.691367100691539,
7.08155544690455)) ;
#74557=CARTESIAN_POINT('Ctrl Pts',(-3.20691291140055,-0.691643821063274,
7.08169470978418)) ;
#74558=CARTESIAN_POINT('Ctrl Pts',(-3.20512388881539,-0.691919930034189,
7.0818)) ;
#74559=CARTESIAN_POINT('Ctrl Pts',(-3.21172314486594,-0.743501373347166,
7.10623564382334)) ;
#74560=CARTESIAN_POINT('Ctrl Pts',(-3.2095315878856,-0.743584576017368,
7.1065058196023)) ;
#74561=CARTESIAN_POINT('Ctrl Pts',(-3.20733490885682,-0.743666470692696,
7.10672585564236)) ;
#74562=CARTESIAN_POINT('Ctrl Pts',(-3.20512388881539,-0.743749639050895,
7.1068882100183)) ;
#74563=CARTESIAN_POINT('Ctrl Pts',(-3.2143421722351,-0.762,7.15898553043244)) ;
#74564=CARTESIAN_POINT('Ctrl Pts',(-3.21127367849934,-0.761999102403065,
7.15918594173638)) ;
#74565=CARTESIAN_POINT('Ctrl Pts',(-3.20820121468723,-0.762000880498864,
7.15931169382832)) ;
#74566=CARTESIAN_POINT('Ctrl Pts',(-3.20512388881539,-0.762,7.15936005247436)) ;
#74567=CARTESIAN_POINT('Ctrl Pts',(-3.2154621751854,-0.762,7.18154353395898)) ;
#74568=CARTESIAN_POINT('Ctrl Pts',(-3.21201894456551,-0.762,7.18171449006546)) ;
#74569=CARTESIAN_POINT('Ctrl Pts',(-3.20857144403868,-0.762,7.1818)) ;
#74570=CARTESIAN_POINT('Ctrl Pts',(-3.20512388881539,-0.762,7.1818)) ;
#74571=CARTESIAN_POINT('',(-3.20512388881539,-0.762,7.1818)) ;
#74572=CARTESIAN_POINT('',(-3.2051238888154,-0.662,7.0818)) ;
#74573=CARTESIAN_POINT('Origin',(-3.20512388881539,-0.662,7.1818)) ;
#74574=CARTESIAN_POINT('Origin',(-3.2048792341882,-0.66383132792774,7.00284754580388)) ;
#74575=CARTESIAN_POINT('Origin',(-3.20581132767206,-0.762,7.0244442135551)) ;
#74576=CARTESIAN_POINT('Ctrl Pts',(-3.10768758242201,-0.761999999110866,
7.18178789612072)) ;
#74577=CARTESIAN_POINT('Ctrl Pts',(-3.10820350632125,-0.762,7.1818)) ;
#74578=CARTESIAN_POINT('Ctrl Pts',(-3.10871943022056,-0.762,7.1818)) ;
#74579=CARTESIAN_POINT('Ctrl Pts',(-3.11460888995322,-0.762,7.18179999999999)) ;
#74580=CARTESIAN_POINT('Ctrl Pts',(-3.12266919370325,-0.762,7.1818)) ;
#74581=CARTESIAN_POINT('Ctrl Pts',(-3.1374980096349,-0.762,7.1818)) ;
#74582=CARTESIAN_POINT('Ctrl Pts',(-3.1469532897332,-0.762,7.1818)) ;
#74583=CARTESIAN_POINT('Ctrl Pts',(-3.15372180191481,-0.762,7.1818)) ;
#74584=CARTESIAN_POINT('Ctrl Pts',(-3.10768758242201,-0.761999999110866,
7.18178789612072)) ;
#74585=CARTESIAN_POINT('Ctrl Pts',(-3.10820350632198,-0.761999971546708,
7.18162961113284)) ;
#74586=CARTESIAN_POINT('Ctrl Pts',(-3.10871943022056,-0.762,7.1814602658962)) ;
#74587=CARTESIAN_POINT('Ctrl Pts',(-3.11460888995322,-0.762,7.17949782470739)) ;
#74588=CARTESIAN_POINT('Ctrl Pts',(-3.12266919370325,-0.762,7.17631957154599)) ;
#74589=CARTESIAN_POINT('Ctrl Pts',(-3.1374980096349,-0.762,7.16854333762089)) ;
#74590=CARTESIAN_POINT('Ctrl Pts',(-3.1469532897332,-0.762,7.16306055736286)) ;
#74591=CARTESIAN_POINT('Ctrl Pts',(-3.15372180191481,-0.762,7.16076336222311)) ;
#74592=CARTESIAN_POINT('Ctrl Pts',(-3.10768758242201,-0.761999999110866,
7.18178789612072)) ;
#74593=CARTESIAN_POINT('Ctrl Pts',(-3.10820350632112,-0.761999937262456,
7.18142430431638)) ;
#74594=CARTESIAN_POINT('Ctrl Pts',(-3.10871943022057,-0.761997356649989,
7.18105351783653)) ;
#74595=CARTESIAN_POINT('Ctrl Pts',(-3.11460888995317,-0.761976495217826,
7.17672655551623)) ;
#74596=CARTESIAN_POINT('Ctrl Pts',(-3.12266919370324,-0.761694542972285,
7.16985111380514)) ;
#74597=CARTESIAN_POINT('Ctrl Pts',(-3.13749800963488,-0.759216921298734,
7.15262801012254)) ;
#74598=CARTESIAN_POINT('Ctrl Pts',(-3.14695328973321,-0.755825896474783,
7.14096328750365)) ;
#74599=CARTESIAN_POINT('Ctrl Pts',(-3.15372180191481,-0.753693441915688,
7.13527073955965)) ;
#74600=CARTESIAN_POINT('Ctrl Pts',(-3.10768758242201,-0.761999999110866,
7.18178789612072)) ;
#74601=CARTESIAN_POINT('Ctrl Pts',(-3.10820350632311,-0.761999900310011,
7.18120301937144)) ;
#74602=CARTESIAN_POINT('Ctrl Pts',(-3.10871943022057,-0.761994331607278,
7.18061138592162)) ;
#74603=CARTESIAN_POINT('Ctrl Pts',(-3.11460888995315,-0.761878231569385,
7.17374285180056)) ;
#74604=CARTESIAN_POINT('Ctrl Pts',(-3.12266919370323,-0.760928454763849,
7.16271105773673)) ;
#74605=CARTESIAN_POINT('Ctrl Pts',(-3.13749800963488,-0.752712459225539,
7.13650432564738)) ;
#74606=CARTESIAN_POINT('Ctrl Pts',(-3.14695328973321,-0.74201847270757,
7.1206541791479)) ;
#74607=CARTESIAN_POINT('Ctrl Pts',(-3.15372180191481,-0.735935879405177,
7.11434234885099)) ;
#74608=CARTESIAN_POINT('Ctrl Pts',(-3.10768758242201,-0.761999999110866,
7.18178789612072)) ;
#74609=CARTESIAN_POINT('Ctrl Pts',(-3.10820350632367,-0.761999890371836,
7.18114350589661)) ;
#74610=CARTESIAN_POINT('Ctrl Pts',(-3.10871943022057,-0.761993397983058,
7.18049224493129)) ;
#74611=CARTESIAN_POINT('Ctrl Pts',(-3.11460888995315,-0.761848304054905,
7.17294119572008)) ;
#74612=CARTESIAN_POINT('Ctrl Pts',(-3.12266919370323,-0.760692288773643,
7.1607896050519)) ;
#74613=CARTESIAN_POINT('Ctrl Pts',(-3.13749800963488,-0.750735669662562,
7.13225210589726)) ;
#74614=CARTESIAN_POINT('Ctrl Pts',(-3.14695328973321,-0.737874325756503,
7.11550492633058)) ;
#74615=CARTESIAN_POINT('Ctrl Pts',(-3.15372180191481,-0.730681059791499,
7.1091778777056)) ;
#74616=CARTESIAN_POINT('Ctrl Pts',(-3.10768758242201,-0.761999999110866,
7.18178789612072)) ;
#74617=CARTESIAN_POINT('Ctrl Pts',(-3.10820350632406,-0.761999885411581,
7.18111380205138)) ;
#74618=CARTESIAN_POINT('Ctrl Pts',(-3.10871943022057,-0.761992965550236,
7.18043260514312)) ;
#74619=CARTESIAN_POINT('Ctrl Pts',(-3.11460888995315,-0.761831627738708,
7.17254121063549)) ;
#74620=CARTESIAN_POINT('Ctrl Pts',(-3.12266919370323,-0.760566154944648,
7.1598249400892)) ;
#74621=CARTESIAN_POINT('Ctrl Pts',(-3.13749800963487,-0.749690046465535,
7.13015050138915)) ;
#74622=CARTESIAN_POINT('Ctrl Pts',(-3.14695328973321,-0.735691643270758,
7.11300325031031)) ;
#74623=CARTESIAN_POINT('Ctrl Pts',(-3.15372180191481,-0.727929085659609,
7.10673826884187)) ;
#74624=CARTESIAN_POINT('Ctrl Pts',(-3.10768758242201,-0.761999999110866,
7.18178789612072)) ;
#74625=CARTESIAN_POINT('Ctrl Pts',(-3.10820350632437,-0.761999882300983,
7.18109517463631)) ;
#74626=CARTESIAN_POINT('Ctrl Pts',(-3.10871943022057,-0.761992726760589,
7.18039509107439)) ;
#74627=CARTESIAN_POINT('Ctrl Pts',(-3.11460888995315,-0.761820320860478,
7.17229047989692)) ;
#74628=CARTESIAN_POINT('Ctrl Pts',(-3.12266919370323,-0.760484017917808,
7.15921737584589)) ;
#74629=CARTESIAN_POINT('Ctrl Pts',(-3.13749800963488,-0.749015451777574,
7.12883825022165)) ;
#74630=CARTESIAN_POINT('Ctrl Pts',(-3.14695328973321,-0.734287500072791,
7.11145355959439)) ;
#74631=CARTESIAN_POINT('Ctrl Pts',(-3.15372180191481,-0.726166969088686,
7.10525117650479)) ;
#74632=CARTESIAN_POINT('Ctrl Pts',(-3.10768758242201,-0.761999999110866,
7.18178789612072)) ;
#74633=CARTESIAN_POINT('Ctrl Pts',(-3.10820350632452,-0.761999880603801,
7.18108501128053)) ;
#74634=CARTESIAN_POINT('Ctrl Pts',(-3.10871943022057,-0.761992578089339,
7.18037464637613)) ;
#74635=CARTESIAN_POINT('Ctrl Pts',(-3.11460888995315,-0.761814227722725,
7.1721536831723)) ;
#74636=CARTESIAN_POINT('Ctrl Pts',(-3.12266919370323,-0.760438384835969,
7.15888643811152)) ;
#74637=CARTESIAN_POINT('Ctrl Pts',(-3.13749800963488,-0.748640047873434,
7.12812617670508)) ;
#74638=CARTESIAN_POINT('Ctrl Pts',(-3.14695328973321,-0.733507903613573,
7.11062229391851)) ;
#74639=CARTESIAN_POINT('Ctrl Pts',(-3.15372180191481,-0.725190242268012,
7.10445781568441)) ;
#74640=CARTESIAN_POINT('Ctrl Pts',(-3.10768758242201,-0.761999999110866,
7.18178789612072)) ;
#74641=CARTESIAN_POINT('Ctrl Pts',(-3.10820350632465,-0.761999879617918,
7.18107910744813)) ;
#74642=CARTESIAN_POINT('Ctrl Pts',(-3.10871943022057,-0.761992519832539,
7.18036270141455)) ;
#74643=CARTESIAN_POINT('Ctrl Pts',(-3.11460888995315,-0.761810241967301,
7.17207425568446)) ;
#74644=CARTESIAN_POINT('Ctrl Pts',(-3.12266919370323,-0.76041106646782,
7.15869248076817)) ;
#74645=CARTESIAN_POINT('Ctrl Pts',(-3.13749800963488,-0.74841848455698,
7.12771246966564)) ;
#74646=CARTESIAN_POINT('Ctrl Pts',(-3.14695328973321,-0.733048178705464,
7.11013808561189)) ;
#74647=CARTESIAN_POINT('Ctrl Pts',(-3.15372180191481,-0.724616601445939,
7.10400482490522)) ;
#74648=CARTESIAN_POINT('',(-3.14953687287002,-0.730523456132445,7.10896775467099)) ;
#74649=CARTESIAN_POINT('',(-3.14953687287001,-0.762,7.1818)) ;
#74650=CARTESIAN_POINT('Origin',(-3.14953687287001,-0.662,7.1818)) ;
#74651=CARTESIAN_POINT('',(-3.10768474164716,-0.761999999558836,7.18179289868234)) ;
#74652=CARTESIAN_POINT('',(-3.14953687287001,-0.762,7.1818)) ;
#74653=CARTESIAN_POINT('Ctrl Pts',(-3.10768189955247,-0.761999999565641,
7.18179079992629)) ;
#74654=CARTESIAN_POINT('Ctrl Pts',(-3.11550396931728,-0.7619989990746,7.17119510360894)) ;
#74655=CARTESIAN_POINT('Ctrl Pts',(-3.12158404061982,-0.760269612060714,
7.1602507583022)) ;
#74656=CARTESIAN_POINT('Ctrl Pts',(-3.13169750131939,-0.753543279843757,
7.14032498264226)) ;
#74657=CARTESIAN_POINT('Ctrl Pts',(-3.13586387425679,-0.748880446529675,
7.13126215380791)) ;
#74658=CARTESIAN_POINT('Ctrl Pts',(-3.14321743559729,-0.739229351300546,
7.11795970925599)) ;
#74659=CARTESIAN_POINT('Ctrl Pts',(-3.1461798989977,-0.735037333748867,
7.11321458920752)) ;
#74660=CARTESIAN_POINT('Ctrl Pts',(-3.14953687287001,-0.730523456132447,
7.10896775467099)) ;
#74661=CARTESIAN_POINT('Ctrl Pts',(-3.14953687287001,-0.762,7.1818)) ;
#74662=CARTESIAN_POINT('Ctrl Pts',(-3.15676355558523,-0.762,7.1818)) ;
#74663=CARTESIAN_POINT('Ctrl Pts',(-3.16399023830045,-0.762,7.1818)) ;
#74664=CARTESIAN_POINT('Ctrl Pts',(-3.17121692101567,-0.762,7.1818)) ;
#74665=CARTESIAN_POINT('Ctrl Pts',(-3.14953687287001,-0.762,7.16625960724294)) ;
#74666=CARTESIAN_POINT('Ctrl Pts',(-3.15676355558523,-0.762015837610647,
7.16371429760845)) ;
#74667=CARTESIAN_POINT('Ctrl Pts',(-3.16399023830045,-0.761980537877959,
7.16173716654572)) ;
#74668=CARTESIAN_POINT('Ctrl Pts',(-3.17121692101567,-0.762,7.16049051462243)) ;
#74669=CARTESIAN_POINT('Ctrl Pts',(-3.14953687287001,-0.755540893518778,
7.1390837819811)) ;
#74670=CARTESIAN_POINT('Ctrl Pts',(-3.15676355558523,-0.75338304373689,
7.13211431434399)) ;
#74671=CARTESIAN_POINT('Ctrl Pts',(-3.16399023830045,-0.751152261593369,
7.1266719591844)) ;
#74672=CARTESIAN_POINT('Ctrl Pts',(-3.17121692101567,-0.749661462765229,
7.12329552595192)) ;
#74673=CARTESIAN_POINT('Ctrl Pts',(-3.14953687287002,-0.739012268865877,
7.11695436533126)) ;
#74674=CARTESIAN_POINT('Ctrl Pts',(-3.15676355558523,-0.73174878770295,
7.10798226702609)) ;
#74675=CARTESIAN_POINT('Ctrl Pts',(-3.16399023830045,-0.724623549182784,
7.10220324165009)) ;
#74676=CARTESIAN_POINT('Ctrl Pts',(-3.17121692101567,-0.720057683295034,
7.09882570651471)) ;
#74677=CARTESIAN_POINT('Ctrl Pts',(-3.14953687287002,-0.730523456132442,
7.10896775467099)) ;
#74678=CARTESIAN_POINT('Ctrl Pts',(-3.15676355558523,-0.720806263628133,
7.09982543575316)) ;
#74679=CARTESIAN_POINT('Ctrl Pts',(-3.16399023830045,-0.711535796534348,
7.09468761566807)) ;
#74680=CARTESIAN_POINT('Ctrl Pts',(-3.17121692101567,-0.705680904617081,
7.09184457452808)) ;
#74681=CARTESIAN_POINT('',(-3.17121692101567,-0.705680904617081,7.09184457452808)) ;
#74682=CARTESIAN_POINT('',(-3.17121692101567,-0.762,7.1818)) ;
#74683=CARTESIAN_POINT('Origin',(-3.17121692101567,-0.662,7.1818)) ;
#74684=CARTESIAN_POINT('',(-3.17121692101567,-0.762,7.1818)) ;
#74685=CARTESIAN_POINT('Ctrl Pts',(-3.14953687287002,-0.730523456132445,
7.10896775467099)) ;
#74686=CARTESIAN_POINT('Ctrl Pts',(-3.15676355558523,-0.720806263628138,
7.09982543575316)) ;
#74687=CARTESIAN_POINT('Ctrl Pts',(-3.16399023830045,-0.711535796534354,
7.09468761566807)) ;
#74688=CARTESIAN_POINT('Ctrl Pts',(-3.17121692101566,-0.705680904617088,
7.09184457452809)) ;
#74689=CARTESIAN_POINT('Ctrl Pts',(-3.20512388881539,-0.661999999999999,
7.0818)) ;
#74690=CARTESIAN_POINT('Ctrl Pts',(-3.20472023443683,-0.662977161851642,
7.0818)) ;
#74691=CARTESIAN_POINT('Ctrl Pts',(-3.20391292567969,-0.664831438935813,
7.0818281326209)) ;
#74692=CARTESIAN_POINT('Ctrl Pts',(-3.20270196254399,-0.667381960953699,
7.08193509059619)) ;
#74693=CARTESIAN_POINT('Ctrl Pts',(-3.20149099940828,-0.669755131272187,
7.08209149598161)) ;
#74694=CARTESIAN_POINT('Ctrl Pts',(-3.1974544556226,-0.67713609635116,7.08275930201881)) ;
#74695=CARTESIAN_POINT('Ctrl Pts',(-3.18736309615839,-0.691331994006399,
7.08558723772616)) ;
#74696=CARTESIAN_POINT('Ctrl Pts',(-3.17767539107276,-0.700448400904756,
7.08930375506814)) ;
#74697=CARTESIAN_POINT('Ctrl Pts',(-3.17121692101566,-0.705680904617081,
7.09184457452809)) ;
#74698=CARTESIAN_POINT('Ctrl Pts',(-3.20512388881539,-0.691919930034188,
7.0818)) ;
#74699=CARTESIAN_POINT('Ctrl Pts',(-3.20472023443683,-0.692710054581018,
7.08210130272039)) ;
#74700=CARTESIAN_POINT('Ctrl Pts',(-3.20391292567969,-0.694201326478369,
7.08268816612552)) ;
#74701=CARTESIAN_POINT('Ctrl Pts',(-3.20270196254399,-0.696232474572727,
7.08353635047393)) ;
#74702=CARTESIAN_POINT('Ctrl Pts',(-3.20149099940828,-0.698105863873827,
7.08436153702967)) ;
#74703=CARTESIAN_POINT('Ctrl Pts',(-3.1974544556226,-0.703886507865681,
7.0870216034983)) ;
#74704=CARTESIAN_POINT('Ctrl Pts',(-3.18736309615839,-0.714604348638996,
7.09308139393355)) ;
#74705=CARTESIAN_POINT('Ctrl Pts',(-3.17767539107276,-0.721164846104133,
7.09796452550531)) ;
#74706=CARTESIAN_POINT('Ctrl Pts',(-3.17121692101566,-0.724849942854352,
7.10115275051025)) ;
#74707=CARTESIAN_POINT('Ctrl Pts',(-3.20512388881539,-0.743749664724923,
7.10688818862076)) ;
#74708=CARTESIAN_POINT('Ctrl Pts',(-3.20472023443683,-0.743987662646956,
7.10735278843905)) ;
#74709=CARTESIAN_POINT('Ctrl Pts',(-3.20391292567969,-0.744433776876774,
7.10823521710843)) ;
#74710=CARTESIAN_POINT('Ctrl Pts',(-3.20270196254399,-0.745035453736892,
7.10945017013558)) ;
#74711=CARTESIAN_POINT('Ctrl Pts',(-3.20149099940828,-0.745586219467376,
7.11058176595391)) ;
#74712=CARTESIAN_POINT('Ctrl Pts',(-3.1974544556226,-0.747266305413514,
7.11411357106582)) ;
#74713=CARTESIAN_POINT('Ctrl Pts',(-3.18736309615839,-0.750270097373977,
7.12099360901837)) ;
#74714=CARTESIAN_POINT('Ctrl Pts',(-3.17767539107276,-0.751952696995019,
7.1257288226096)) ;
#74715=CARTESIAN_POINT('Ctrl Pts',(-3.17121692101566,-0.75291924171095,
7.12849905621401)) ;
#74716=CARTESIAN_POINT('Ctrl Pts',(-3.20512388881539,-0.762,7.15936005247436)) ;
#74717=CARTESIAN_POINT('Ctrl Pts',(-3.20472023443683,-0.761997480329003,
7.1594984375227)) ;
#74718=CARTESIAN_POINT('Ctrl Pts',(-3.20391292567969,-0.761993348192325,
7.1597613592822)) ;
#74719=CARTESIAN_POINT('Ctrl Pts',(-3.20270196254399,-0.76198811015298,
7.16012343058549)) ;
#74720=CARTESIAN_POINT('Ctrl Pts',(-3.20149099940828,-0.761983122426318,
7.16046067089829)) ;
#74721=CARTESIAN_POINT('Ctrl Pts',(-3.1974544556226,-0.761972743237157,
7.16151393713481)) ;
#74722=CARTESIAN_POINT('Ctrl Pts',(-3.18736309615839,-0.761958192393428,
7.16356744125941)) ;
#74723=CARTESIAN_POINT('Ctrl Pts',(-3.17767539107276,-0.762003840410888,
7.16498934960751)) ;
#74724=CARTESIAN_POINT('Ctrl Pts',(-3.17121692101567,-0.762,7.16581788596682)) ;
#74725=CARTESIAN_POINT('Ctrl Pts',(-3.20512388881539,-0.762,7.1818)) ;
#74726=CARTESIAN_POINT('Ctrl Pts',(-3.20472023443683,-0.762,7.1818)) ;
#74727=CARTESIAN_POINT('Ctrl Pts',(-3.20391292567969,-0.762,7.1818)) ;
#74728=CARTESIAN_POINT('Ctrl Pts',(-3.20270196254399,-0.762,7.1818)) ;
#74729=CARTESIAN_POINT('Ctrl Pts',(-3.20149099940828,-0.762,7.1818)) ;
#74730=CARTESIAN_POINT('Ctrl Pts',(-3.1974544556226,-0.762,7.1818)) ;
#74731=CARTESIAN_POINT('Ctrl Pts',(-3.18736309615839,-0.762,7.1818)) ;
#74732=CARTESIAN_POINT('Ctrl Pts',(-3.17767539107276,-0.762,7.1818)) ;
#74733=CARTESIAN_POINT('Ctrl Pts',(-3.17121692101567,-0.762,7.1818)) ;
#74734=CARTESIAN_POINT('Ctrl Pts',(-3.17121692101567,-0.705680904617077,
7.09184457452808)) ;
#74735=CARTESIAN_POINT('Ctrl Pts',(-3.17444615604422,-0.703064652760914,
7.09057416479811)) ;
#74736=CARTESIAN_POINT('Ctrl Pts',(-3.17767539107276,-0.700235809090658,
7.0893360813593)) ;
#74737=CARTESIAN_POINT('Ctrl Pts',(-3.18371137404519,-0.694285563440634,
7.08710907960385)) ;
#74738=CARTESIAN_POINT('Ctrl Pts',(-3.18651812198907,-0.691250186366111,
7.08610870787848)) ;
#74739=CARTESIAN_POINT('Ctrl Pts',(-3.18974735701762,-0.687336965752854,
7.08506159474165)) ;
#74740=CARTESIAN_POINT('Ctrl Pts',(-3.19016984410228,-0.686816704289863,
7.08492674037565)) ;
#74741=CARTESIAN_POINT('Ctrl Pts',(-3.19239331865279,-0.684033333884775,
7.08422985303717)) ;
#74742=CARTESIAN_POINT('Ctrl Pts',(-3.19419430611863,-0.68162375111484,
7.08370642162001)) ;
#74743=CARTESIAN_POINT('Ctrl Pts',(-3.19742354114718,-0.676803085814083,
7.082878067165)) ;
#74744=CARTESIAN_POINT('Ctrl Pts',(-3.19885178870988,-0.674495257467968,
7.0825507746911)) ;
#74745=CARTESIAN_POINT('Ctrl Pts',(-3.20068369065114,-0.67123138690268,
7.08222438102226)) ;
#74746=CARTESIAN_POINT('Ctrl Pts',(-3.20108734502971,-0.670493217907312,
7.08215837537037)) ;
#74747=CARTESIAN_POINT('Ctrl Pts',(-3.20189465378685,-0.66896403985744,
7.08203983631671)) ;
#74748=CARTESIAN_POINT('Ctrl Pts',(-3.20229830816542,-0.668173012083411,
7.08198732917139)) ;
#74749=CARTESIAN_POINT('Ctrl Pts',(-3.20310561692256,-0.666531791312407,
7.08189935834229)) ;
#74750=CARTESIAN_POINT('Ctrl Pts',(-3.20350927130112,-0.665681610657713,
7.08186384002979)) ;
#74751=CARTESIAN_POINT('Ctrl Pts',(-3.20431658005826,-0.663904297940051,
7.08181418112562)) ;
#74752=CARTESIAN_POINT('Ctrl Pts',(-3.20472023443683,-0.662977161851642,
7.0818)) ;
#74753=CARTESIAN_POINT('Ctrl Pts',(-3.20512388881539,-0.661999999999999,
7.0818)) ;
#74754=CARTESIAN_POINT('',(-3.20512388881539,-0.762,7.1818)) ;
#74755=CARTESIAN_POINT('Ctrl Pts',(-3.28702640935013,-0.678916496982596,
7.03662526114754)) ;
#74756=CARTESIAN_POINT('Ctrl Pts',(-3.28505420805782,-0.68846506114502,
7.03662526114754)) ;
#74757=CARTESIAN_POINT('Ctrl Pts',(-3.28250316889159,-0.697892264769899,
7.03746773980168)) ;
#74758=CARTESIAN_POINT('Ctrl Pts',(-3.27942391815487,-0.707077062047443,
7.03908289042881)) ;
#74759=CARTESIAN_POINT('Ctrl Pts',(-3.27867914825951,-0.677192417966096,
7.04962706151189)) ;
#74760=CARTESIAN_POINT('Ctrl Pts',(-3.27680440972048,-0.685870309279993,
7.04975105769206)) ;
#74761=CARTESIAN_POINT('Ctrl Pts',(-3.2743643275819,-0.694431071838909,
7.05063960533657)) ;
#74762=CARTESIAN_POINT('Ctrl Pts',(-3.27140856314625,-0.702764080010726,
7.05223037429132)) ;
#74763=CARTESIAN_POINT('Ctrl Pts',(-3.26731641278835,-0.674845509970385,
7.06059580486523)) ;
#74764=CARTESIAN_POINT('Ctrl Pts',(-3.26548227953707,-0.682632591536585,
7.06080383849016)) ;
#74765=CARTESIAN_POINT('Ctrl Pts',(-3.26310082825167,-0.69030704612225,
7.06169180427166)) ;
#74766=CARTESIAN_POINT('Ctrl Pts',(-3.26021975085612,-0.697769125082816,
7.06320246322368)) ;
#74767=CARTESIAN_POINT('Ctrl Pts',(-3.25413500684155,-0.672122965994088,
7.06837618534741)) ;
#74768=CARTESIAN_POINT('Ctrl Pts',(-3.2523024532275,-0.679097662424487,
7.06859808108705)) ;
#74769=CARTESIAN_POINT('Ctrl Pts',(-3.24994321022021,-0.685968760565752,
7.0694168668701)) ;
#74770=CARTESIAN_POINT('Ctrl Pts',(-3.24710198979478,-0.692647775796551,
7.07077875440761)) ;
#74771=CARTESIAN_POINT('',(-3.28702640935013,-0.678916496982596,7.03662526114754)) ;
#74772=CARTESIAN_POINT('Origin',(-3.2051238888154,-0.662,6.9818)) ;
#74773=CARTESIAN_POINT('Origin',(-3.18317729866126,-0.677221167011857,7.17900526082346)) ;
#74774=CARTESIAN_POINT('Origin',(0.,-8.67361737988404E-16,6.793484)) ;
#74775=CARTESIAN_POINT('',(3.31205160669424,0.887893661760288,6.793484)) ;
#74776=CARTESIAN_POINT('',(-4.19931387427627E-16,3.429,6.793484)) ;
#74777=CARTESIAN_POINT('Origin',(0.,-1.01919954906029E-15,6.793484)) ;
#74778=CARTESIAN_POINT('',(3.27942391815471,0.707077062047146,7.03908289042914)) ;
#74779=CARTESIAN_POINT('Ctrl Pts',(3.2794239181545,0.707077062047012,7.03908289042949)) ;
#74780=CARTESIAN_POINT('Ctrl Pts',(3.31839899815499,0.756128366293949,6.96625435392858)) ;
#74781=CARTESIAN_POINT('Ctrl Pts',(3.32718180865331,0.82115248175181,6.88564197720954)) ;
#74782=CARTESIAN_POINT('Ctrl Pts',(3.31364139250919,0.881705147287931,6.80206837154771)) ;
#74783=CARTESIAN_POINT('Ctrl Pts',(3.31287790153465,0.884811388204746,6.79777468341573)) ;
#74784=CARTESIAN_POINT('Ctrl Pts',(3.31205160669424,0.887893661760288,6.793484)) ;
#74785=CARTESIAN_POINT('',(3.28702640935013,0.678916496982597,7.03662526114754)) ;
#74786=CARTESIAN_POINT('Origin',(3.18317729880794,0.677221167035773,7.17900526061628)) ;
#74787=CARTESIAN_POINT('',(3.2870264093502,-0.678916496982227,7.03662526114754)) ;
#74788=CARTESIAN_POINT('Origin',(0.,-7.50806669192421E-16,7.03662526114754)) ;
#74789=CARTESIAN_POINT('',(3.27942391815471,-0.707077062047155,7.03908289042913)) ;
#74790=CARTESIAN_POINT('Origin',(3.18706485416322,-0.677836112548214,7.17352010134439)) ;
#74791=CARTESIAN_POINT('',(3.31205160669424,-0.887893661760288,6.793484)) ;
#74792=CARTESIAN_POINT('Ctrl Pts',(3.31205160669424,-0.887893661760288,
6.793484)) ;
#74793=CARTESIAN_POINT('Ctrl Pts',(3.31287790157776,-0.884811388043908,
6.79777468368237)) ;
#74794=CARTESIAN_POINT('Ctrl Pts',(3.31364139250205,-0.881705147317766,
6.80206837149932)) ;
#74795=CARTESIAN_POINT('Ctrl Pts',(3.32718180880554,-0.821152481073567,
6.88564197832078)) ;
#74796=CARTESIAN_POINT('Ctrl Pts',(3.31839899815499,-0.756128366293962,
6.96625435392856)) ;
#74797=CARTESIAN_POINT('Ctrl Pts',(3.27942391815451,-0.707077062047025,
7.03908289042947)) ;
#74798=CARTESIAN_POINT('Origin',(0.,-1.01919954906029E-15,6.793484)) ;
#74799=CARTESIAN_POINT('',(-3.2870264093502,0.678916496982226,7.03662526114754)) ;
#74800=CARTESIAN_POINT('Origin',(0.,-7.50806669192421E-16,7.03662526114754)) ;
#74801=CARTESIAN_POINT('',(-3.27942391815471,0.707077062047156,7.03908289042913)) ;
#74802=CARTESIAN_POINT('Origin',(-3.18706485424506,0.677836112556869,7.17352010123012)) ;
#74803=CARTESIAN_POINT('',(-3.31205160669424,0.887893661760289,6.793484)) ;
#74804=CARTESIAN_POINT('Ctrl Pts',(-3.31205160669424,0.887893661760288,
6.793484)) ;
#74805=CARTESIAN_POINT('Ctrl Pts',(-3.31287790157776,0.884811388043911,
6.79777468368234)) ;
#74806=CARTESIAN_POINT('Ctrl Pts',(-3.31364139250206,0.881705147317757,
6.80206837149931)) ;
#74807=CARTESIAN_POINT('Ctrl Pts',(-3.32718180880552,0.821152481073622,
6.88564197832082)) ;
#74808=CARTESIAN_POINT('Ctrl Pts',(-3.31839899815499,0.756128366293961,
6.96625435392856)) ;
#74809=CARTESIAN_POINT('Ctrl Pts',(-3.27942391815451,0.707077062047025,
7.03908289042948)) ;
#74810=CARTESIAN_POINT('Origin',(0.,-1.01919954906029E-15,6.793484)) ;
#74811=CARTESIAN_POINT('',(-3.65620261320321E-16,2.985516,6.35)) ;
#74812=CARTESIAN_POINT('Origin',(-3.65620261320321E-16,2.985516,6.793484)) ;
#74813=CARTESIAN_POINT('Origin',(0.,-1.23179328113998E-15,6.35)) ;
#74814=CARTESIAN_POINT('Origin',(0.,-8.2222504619082E-16,6.9818)) ;
#74815=CARTESIAN_POINT('',(-3.20512388881552,0.661999999999843,7.0818)) ;
#74816=CARTESIAN_POINT('Origin',(0.,-8.2222504619082E-16,7.0818)) ;
#74817=CARTESIAN_POINT('',(-3.2105035504766,0.660979117346627,7.08167176697949)) ;
#74818=CARTESIAN_POINT('Origin',(-3.2048792375206,0.663831325381439,7.00284763048191)) ;
#74819=CARTESIAN_POINT('',(-3.25413500684125,0.672122965993743,7.06837618534762)) ;
#74820=CARTESIAN_POINT('Ctrl Pts',(-3.25413500684122,0.672122965993824,
7.06837618534763)) ;
#74821=CARTESIAN_POINT('Ctrl Pts',(-3.24739271551801,0.666780512351139,
7.07281769210623)) ;
#74822=CARTESIAN_POINT('Ctrl Pts',(-3.23371088749541,0.659801218122162,
7.07893541781973)) ;
#74823=CARTESIAN_POINT('Ctrl Pts',(-3.21758827489312,0.659638486038928,
7.08133371486205)) ;
#74824=CARTESIAN_POINT('Ctrl Pts',(-3.2105035504766,0.660979117346627,7.08167176697949)) ;
#74825=CARTESIAN_POINT('Origin',(-3.20512388881547,0.661999999999639,6.9818)) ;
#74826=CARTESIAN_POINT('Ctrl Pts',(-3.31205160669424,0.887893661760288,
6.793484)) ;
#74827=CARTESIAN_POINT('Ctrl Pts',(-3.31247680274145,0.886307580777865,
6.79874217793992)) ;
#74828=CARTESIAN_POINT('Ctrl Pts',(-3.31286385708463,0.884707693113234,
6.80400403812142)) ;
#74829=CARTESIAN_POINT('Ctrl Pts',(-3.31959859780671,0.853484700721687,
6.90642242863739)) ;
#74830=CARTESIAN_POINT('Ctrl Pts',(-3.31286250738096,0.819472008973418,
7.00521187075636)) ;
#74831=CARTESIAN_POINT('Ctrl Pts',(-3.2881405032392,0.793313315480963,7.09446231571415)) ;
#74832=CARTESIAN_POINT('Ctrl Pts',(-3.31205160669424,0.887893661760288,
6.793484)) ;
#74833=CARTESIAN_POINT('Ctrl Pts',(-3.31261121118724,0.885806205750657,
6.79841624509089)) ;
#74834=CARTESIAN_POINT('Ctrl Pts',(-3.31307594580264,0.883698810485547,
6.80336333516763)) ;
#74835=CARTESIAN_POINT('Ctrl Pts',(-3.32193595557476,0.842609792739153,
6.89941056465096)) ;
#74836=CARTESIAN_POINT('Ctrl Pts',(-3.30625449205529,0.797119135192672,
6.99229450465508)) ;
#74837=CARTESIAN_POINT('Ctrl Pts',(-3.26888725785269,0.7729411910402,7.07185431702684)) ;
#74838=CARTESIAN_POINT('Ctrl Pts',(-3.31205160669424,0.887893661760288,
6.793484)) ;
#74839=CARTESIAN_POINT('Ctrl Pts',(-3.31274522373845,0.885306307503067,
6.79809343311381)) ;
#74840=CARTESIAN_POINT('Ctrl Pts',(-3.31334303732283,0.8826990404866,6.8027179114036)) ;
#74841=CARTESIAN_POINT('Ctrl Pts',(-3.32434030429394,0.831838892287706,
6.89249111351257)) ;
#74842=CARTESIAN_POINT('Ctrl Pts',(-3.30868757227878,0.775373519472595,
6.97904841531995)) ;
#74843=CARTESIAN_POINT('Ctrl Pts',(-3.2654052227293,0.738492188311667,7.04973176535317)) ;
#74844=CARTESIAN_POINT('Ctrl Pts',(-3.31205160669424,0.887893661760288,
6.793484)) ;
#74845=CARTESIAN_POINT('Ctrl Pts',(-3.31287790157776,0.884811388043911,
6.79777468368234)) ;
#74846=CARTESIAN_POINT('Ctrl Pts',(-3.31364139250206,0.881705147317757,
6.80206837149931)) ;
#74847=CARTESIAN_POINT('Ctrl Pts',(-3.32718180880552,0.821152481073622,
6.88564197832082)) ;
#74848=CARTESIAN_POINT('Ctrl Pts',(-3.31839899815499,0.756128366293961,
6.96625435392856)) ;
#74849=CARTESIAN_POINT('Ctrl Pts',(-3.27942391815451,0.707077062047025,
7.03908289042948)) ;
#74850=CARTESIAN_POINT('',(-3.2881405032392,0.793313315480963,7.09446231571415)) ;
#74851=CARTESIAN_POINT('Origin',(-3.36081883130048,0.724626630961926,7.09446231571415)) ;
#74852=CARTESIAN_POINT('Ctrl Pts',(-3.2881405032392,0.793313315480963,7.09446231571415)) ;
#74853=CARTESIAN_POINT('Ctrl Pts',(-3.31286250738096,0.819472008973418,
7.00521187075636)) ;
#74854=CARTESIAN_POINT('Ctrl Pts',(-3.31959859780671,0.853484700721687,
6.90642242863739)) ;
#74855=CARTESIAN_POINT('Ctrl Pts',(-3.31286385708463,0.884707693113234,
6.80400403812142)) ;
#74856=CARTESIAN_POINT('Ctrl Pts',(-3.31247680274145,0.886307580777865,
6.79874217793992)) ;
#74857=CARTESIAN_POINT('Ctrl Pts',(-3.31205160669424,0.887893661760288,
6.793484)) ;
#74858=CARTESIAN_POINT('Ctrl Pts',(-3.28814050323922,0.793313315480982,
7.09446231571408)) ;
#74859=CARTESIAN_POINT('Ctrl Pts',(-3.28134410252723,0.786121950167006,
7.11899842468707)) ;
#74860=CARTESIAN_POINT('Ctrl Pts',(-3.27166340596969,0.778151805222174,
7.13954927378692)) ;
#74861=CARTESIAN_POINT('Ctrl Pts',(-3.25930415002248,0.77212296599392,7.15495237069524)) ;
#74862=CARTESIAN_POINT('Ctrl Pts',(-3.27713864873268,0.781672101514859,
7.08154345932128)) ;
#74863=CARTESIAN_POINT('Ctrl Pts',(-3.2693149987863,0.775745323023668,7.10257847353651)) ;
#74864=CARTESIAN_POINT('Ctrl Pts',(-3.2586971438891,0.76966902040116,7.11948103530695)) ;
#74865=CARTESIAN_POINT('Ctrl Pts',(-3.24720304082939,0.766220050630706,
7.13091195407417)) ;
#74866=CARTESIAN_POINT('Ctrl Pts',(-3.26627246770002,0.753460431697841,
7.05898639091381)) ;
#74867=CARTESIAN_POINT('Ctrl Pts',(-3.25765493728098,0.747264169127614,
7.07395698646391)) ;
#74868=CARTESIAN_POINT('Ctrl Pts',(-3.24613294003293,0.741135418678703,
7.08437187853508)) ;
#74869=CARTESIAN_POINT('Ctrl Pts',(-3.23542257587918,0.737017859268566,
7.08914722322215)) ;
#74870=CARTESIAN_POINT('Ctrl Pts',(-3.27341590582958,0.720540687589143,
7.04364669396792)) ;
#74871=CARTESIAN_POINT('Ctrl Pts',(-3.26646853334762,0.711672429586283,
7.05583711308295)) ;
#74872=CARTESIAN_POINT('Ctrl Pts',(-3.25699307010659,0.701213312597674,
7.06492336369149)) ;
#74873=CARTESIAN_POINT('Ctrl Pts',(-3.24626907090931,0.691101901539582,
7.07061000050628)) ;
#74874=CARTESIAN_POINT('Ctrl Pts',(-3.27942391815468,0.707077062047165,
7.03908289042918)) ;
#74875=CARTESIAN_POINT('Ctrl Pts',(-3.27351027274501,0.697039528180337,
7.05095544135298)) ;
#74876=CARTESIAN_POINT('Ctrl Pts',(-3.26515692538619,0.684626627058011,
7.06067463689345)) ;
#74877=CARTESIAN_POINT('Ctrl Pts',(-3.25413500684125,0.67212296599374,7.06837618534762)) ;
#74878=CARTESIAN_POINT('',(-3.25930415002248,0.77212296599392,7.15495237069524)) ;
#74879=CARTESIAN_POINT('Origin',(-3.30314612486703,0.68224593198784,7.15495237069524)) ;
#74880=CARTESIAN_POINT('Ctrl Pts',(-3.25930415002248,0.77212296599392,7.15495237069524)) ;
#74881=CARTESIAN_POINT('Ctrl Pts',(-3.27166340596969,0.778151805222174,
7.13954927378692)) ;
#74882=CARTESIAN_POINT('Ctrl Pts',(-3.28134410252723,0.786121950167006,
7.11899842468707)) ;
#74883=CARTESIAN_POINT('Ctrl Pts',(-3.28814050323922,0.793313315480982,
7.09446231571408)) ;
#74884=CARTESIAN_POINT('Ctrl Pts',(-3.27942391815468,0.707077062047165,
7.03908289042918)) ;
#74885=CARTESIAN_POINT('Ctrl Pts',(-3.2764538639168,0.702035836553619,7.04504573022475)) ;
#74886=CARTESIAN_POINT('Ctrl Pts',(-3.27285683396428,0.696395529148052,
7.05045952339999)) ;
#74887=CARTESIAN_POINT('Ctrl Pts',(-3.26443586616697,0.684547202106127,
7.0602016814902)) ;
#74888=CARTESIAN_POINT('Ctrl Pts',(-3.25962130503425,0.678346820109796,
7.06454264301149)) ;
#74889=CARTESIAN_POINT('Ctrl Pts',(-3.25413500684125,0.672122965993741,
7.06837618534762)) ;
#74890=CARTESIAN_POINT('Ctrl Pts',(-3.25930415002247,0.772122965993916,
7.15495237069525)) ;
#74891=CARTESIAN_POINT('Ctrl Pts',(-3.25217652898008,0.768646115807462,
7.16383538421246)) ;
#74892=CARTESIAN_POINT('Ctrl Pts',(-3.23808903446775,0.763655482586567,
7.17607083563947)) ;
#74893=CARTESIAN_POINT('Ctrl Pts',(-3.22227089015459,0.762000000000254,
7.18086742972409)) ;
#74894=CARTESIAN_POINT('Ctrl Pts',(-3.21546217518166,0.762,7.18154353395898)) ;
#74895=CARTESIAN_POINT('Ctrl Pts',(-3.24720304082939,0.766220050630709,
7.13091195407419)) ;
#74896=CARTESIAN_POINT('Ctrl Pts',(-3.24082772074753,0.764341685381236,
7.13776252021244)) ;
#74897=CARTESIAN_POINT('Ctrl Pts',(-3.22957572127668,0.76230454784959,7.14681577983074)) ;
#74898=CARTESIAN_POINT('Ctrl Pts',(-3.21874824269101,0.761905886466605,
7.15069418882242)) ;
#74899=CARTESIAN_POINT('Ctrl Pts',(-3.2139688379146,0.761999999999944,7.15146619592362)) ;
#74900=CARTESIAN_POINT('Ctrl Pts',(-3.23542257429462,0.737017860463239,
7.08914722161447)) ;
#74901=CARTESIAN_POINT('Ctrl Pts',(-3.22965611967589,0.735483547844239,
7.09257680559161)) ;
#74902=CARTESIAN_POINT('Ctrl Pts',(-3.22096836281863,0.734845466512303,
7.09620345120675)) ;
#74903=CARTESIAN_POINT('Ctrl Pts',(-3.21447987532315,0.735942196903049,
7.09846645621959)) ;
#74904=CARTESIAN_POINT('Ctrl Pts',(-3.21138266038764,0.736564632620709,
7.0993779386748)) ;
#74905=CARTESIAN_POINT('Ctrl Pts',(-3.2462690709093,0.691101901539657,7.0706100005063)) ;
#74906=CARTESIAN_POINT('Ctrl Pts',(-3.23998072705782,0.686932534379085,
7.07420186243876)) ;
#74907=CARTESIAN_POINT('Ctrl Pts',(-3.22834802048836,0.681963529037854,
7.07871480715488)) ;
#74908=CARTESIAN_POINT('Ctrl Pts',(-3.2160102402617,0.68236088570503,7.08087457454952)) ;
#74909=CARTESIAN_POINT('Ctrl Pts',(-3.21049211655992,0.683563730806886,
7.08144147623458)) ;
#74910=CARTESIAN_POINT('Ctrl Pts',(-3.25413500684122,0.672122965993824,
7.06837618534763)) ;
#74911=CARTESIAN_POINT('Ctrl Pts',(-3.24739271551801,0.666780512351139,
7.07281769210623)) ;
#74912=CARTESIAN_POINT('Ctrl Pts',(-3.23371088749541,0.659801218122162,
7.07893541781973)) ;
#74913=CARTESIAN_POINT('Ctrl Pts',(-3.21758827489312,0.659638486038928,
7.08133371486205)) ;
#74914=CARTESIAN_POINT('Ctrl Pts',(-3.2105035504766,0.660979117346627,7.08167176697949)) ;
#74915=CARTESIAN_POINT('',(-3.2154621751798,0.762,7.18154353395898)) ;
#74916=CARTESIAN_POINT('Origin',(-3.2154621751854,0.662,7.18154353395898)) ;
#74917=CARTESIAN_POINT('Ctrl Pts',(-3.21546217518166,0.762,7.18154353395898)) ;
#74918=CARTESIAN_POINT('Ctrl Pts',(-3.22227089015459,0.762000000000254,
7.18086742972409)) ;
#74919=CARTESIAN_POINT('Ctrl Pts',(-3.23808903446775,0.763655482586567,
7.17607083563947)) ;
#74920=CARTESIAN_POINT('Ctrl Pts',(-3.25217652898008,0.768646115807462,
7.16383538421246)) ;
#74921=CARTESIAN_POINT('Ctrl Pts',(-3.25930415002247,0.772122965993916,
7.15495237069525)) ;
#74922=CARTESIAN_POINT('Ctrl Pts',(-3.2154621751854,0.762,7.18154353395898)) ;
#74923=CARTESIAN_POINT('Ctrl Pts',(-3.21201894456566,0.762,7.18171449006545)) ;
#74924=CARTESIAN_POINT('Ctrl Pts',(-3.20857144403885,0.762,7.1818)) ;
#74925=CARTESIAN_POINT('Ctrl Pts',(-3.20512388881564,0.762,7.1818)) ;
#74926=CARTESIAN_POINT('Ctrl Pts',(-3.21396883791834,0.762,7.15146619592359)) ;
#74927=CARTESIAN_POINT('Ctrl Pts',(-3.21102860740559,0.761997290973651,
7.15167826758758)) ;
#74928=CARTESIAN_POINT('Ctrl Pts',(-3.20807464984533,0.762002680217736,
7.15181361851019)) ;
#74929=CARTESIAN_POINT('Ctrl Pts',(-3.20512388881561,0.762,7.15188006996581)) ;
#74930=CARTESIAN_POINT('Ctrl Pts',(-3.21138265683666,0.736564691651965,
7.0993778670976)) ;
#74931=CARTESIAN_POINT('Ctrl Pts',(-3.20930558735074,0.736681278140644,
7.09965201966661)) ;
#74932=CARTESIAN_POINT('Ctrl Pts',(-3.20722130366678,0.7367952805891,7.09987813004075)) ;
#74933=CARTESIAN_POINT('Ctrl Pts',(-3.20512388881555,0.736911789981695,
7.10005036094909)) ;
#74934=CARTESIAN_POINT('Ctrl Pts',(-3.21049211656076,0.683563730806912,
7.08144147623454)) ;
#74935=CARTESIAN_POINT('Ctrl Pts',(-3.20870975639603,0.683855790193559,
7.08160438817637)) ;
#74936=CARTESIAN_POINT('Ctrl Pts',(-3.20691685125597,0.684146559499709,
7.08172265074698)) ;
#74937=CARTESIAN_POINT('Ctrl Pts',(-3.20512388881552,0.68443994752562,7.08179999999999)) ;
#74938=CARTESIAN_POINT('Ctrl Pts',(-3.2105035504766,0.660979117346626,7.08167176697949)) ;
#74939=CARTESIAN_POINT('Ctrl Pts',(-3.20871214489269,0.661318102220315,
7.08175724503272)) ;
#74940=CARTESIAN_POINT('Ctrl Pts',(-3.20691819492514,0.661658530855206,
7.0818)) ;
#74941=CARTESIAN_POINT('Ctrl Pts',(-3.20512388881552,0.661999999999975,
7.0818)) ;
#74942=CARTESIAN_POINT('',(-3.20512388881569,0.762,7.1818)) ;
#74943=CARTESIAN_POINT('Origin',(-3.20512388881569,0.662,7.1818)) ;
#74944=CARTESIAN_POINT('Origin',(-3.20581132625523,0.762,7.02444416805792)) ;
#74945=CARTESIAN_POINT('Ctrl Pts',(-3.14953687287001,0.762,7.1818)) ;
#74946=CARTESIAN_POINT('Ctrl Pts',(-3.14687049250718,0.762,7.1818)) ;
#74947=CARTESIAN_POINT('Ctrl Pts',(-3.14153773178152,0.762,7.1818)) ;
#74948=CARTESIAN_POINT('Ctrl Pts',(-3.13353859069304,0.762,7.1818)) ;
#74949=CARTESIAN_POINT('Ctrl Pts',(-3.12287306924172,0.762,7.1818)) ;
#74950=CARTESIAN_POINT('Ctrl Pts',(-3.11487392815324,0.762,7.18180000000001)) ;
#74951=CARTESIAN_POINT('Ctrl Pts',(-3.10892316710968,0.762,7.18179999999999)) ;
#74952=CARTESIAN_POINT('Ctrl Pts',(-3.10830516679178,0.762,7.18179999999999)) ;
#74953=CARTESIAN_POINT('Ctrl Pts',(-3.10768716647391,0.761999999491749,
7.18179159914902)) ;
#74954=CARTESIAN_POINT('Ctrl Pts',(-3.14953687287001,0.762,7.16625960724294)) ;
#74955=CARTESIAN_POINT('Ctrl Pts',(-3.14687049250718,0.762,7.16719533415406)) ;
#74956=CARTESIAN_POINT('Ctrl Pts',(-3.14153773178152,0.762,7.16928720207077)) ;
#74957=CARTESIAN_POINT('Ctrl Pts',(-3.13353859069304,0.762,7.17285503844875)) ;
#74958=CARTESIAN_POINT('Ctrl Pts',(-3.12287306924172,0.762,7.17733421919101)) ;
#74959=CARTESIAN_POINT('Ctrl Pts',(-3.11487392815324,0.762,7.17988076927801)) ;
#74960=CARTESIAN_POINT('Ctrl Pts',(-3.10892316710968,0.762,7.18147435116188)) ;
#74961=CARTESIAN_POINT('Ctrl Pts',(-3.10830516679238,0.76199997373953,7.18163768471162)) ;
#74962=CARTESIAN_POINT('Ctrl Pts',(-3.10768716647391,0.761999999491749,
7.18179159914902)) ;
#74963=CARTESIAN_POINT('Ctrl Pts',(-3.14953687287001,0.755540898601867,
7.13908377950685)) ;
#74964=CARTESIAN_POINT('Ctrl Pts',(-3.14687049250718,0.756336720061584,
7.1416558838152)) ;
#74965=CARTESIAN_POINT('Ctrl Pts',(-3.14153773178152,0.757950944898512,
7.14739328800637)) ;
#74966=CARTESIAN_POINT('Ctrl Pts',(-3.13353859069303,0.760010135132571,
7.157199311821)) ;
#74967=CARTESIAN_POINT('Ctrl Pts',(-3.12287306924172,0.761680931524669,
7.16950958658713)) ;
#74968=CARTESIAN_POINT('Ctrl Pts',(-3.11487392815321,0.761961216462268,
7.17650146046705)) ;
#74969=CARTESIAN_POINT('Ctrl Pts',(-3.10892316710969,0.761997489103582,
7.18090629058231)) ;
#74970=CARTESIAN_POINT('Ctrl Pts',(-3.10830516679297,0.761999927581,7.18135238002238)) ;
#74971=CARTESIAN_POINT('Ctrl Pts',(-3.10768716647391,0.761999999491749,
7.18179159914902)) ;
#74972=CARTESIAN_POINT('Ctrl Pts',(-3.14953687287001,0.739012268865883,
7.11695436533127)) ;
#74973=CARTESIAN_POINT('Ctrl Pts',(-3.14687049250718,0.74169687311928,7.12026196117322)) ;
#74974=CARTESIAN_POINT('Ctrl Pts',(-3.14153773178152,0.747258461785075,
7.12796089840982)) ;
#74975=CARTESIAN_POINT('Ctrl Pts',(-3.13353859069302,0.754625778458326,
7.1423590326318)) ;
#74976=CARTESIAN_POINT('Ctrl Pts',(-3.12287306924171,0.760786688710496,
7.16164067071631)) ;
#74977=CARTESIAN_POINT('Ctrl Pts',(-3.11487392815318,0.761845223762039,
7.17312655610409)) ;
#74978=CARTESIAN_POINT('Ctrl Pts',(-3.10892316710969,0.761991474599831,
7.18033804412795)) ;
#74979=CARTESIAN_POINT('Ctrl Pts',(-3.10830516679363,0.761999881429747,
7.18106712031758)) ;
#74980=CARTESIAN_POINT('Ctrl Pts',(-3.10768716647391,0.761999999491749,
7.18179159914902)) ;
#74981=CARTESIAN_POINT('Ctrl Pts',(-3.14953687287001,0.73052345613245,7.10896775467099)) ;
#74982=CARTESIAN_POINT('Ctrl Pts',(-3.14687049250718,0.734108743088629,
7.11234093439866)) ;
#74983=CARTESIAN_POINT('Ctrl Pts',(-3.14153773178152,0.741620611344294,
7.12039126654701)) ;
#74984=CARTESIAN_POINT('Ctrl Pts',(-3.13353859069302,0.751722671586531,
7.13626512385343)) ;
#74985=CARTESIAN_POINT('Ctrl Pts',(-3.12287306924171,0.760294668457555,
7.15825743742988)) ;
#74986=CARTESIAN_POINT('Ctrl Pts',(-3.11487392815318,0.761768784399304,
7.17170556226768)) ;
#74987=CARTESIAN_POINT('Ctrl Pts',(-3.10892316710969,0.761989461278184,
7.18009224570766)) ;
#74988=CARTESIAN_POINT('Ctrl Pts',(-3.10830516679515,0.761999861904407,
7.18094643469176)) ;
#74989=CARTESIAN_POINT('Ctrl Pts',(-3.10768716647391,0.761999999491749,
7.18179159914902)) ;
#74990=CARTESIAN_POINT('',(-3.14953687287002,0.730523456132444,7.10896775467099)) ;
#74991=CARTESIAN_POINT('',(-3.10768716647391,0.761999999491749,7.18179159914902)) ;
#74992=CARTESIAN_POINT('Ctrl Pts',(-3.14953687287001,0.73052345613245,7.10896775467099)) ;
#74993=CARTESIAN_POINT('Ctrl Pts',(-3.14797942941845,0.732617636606373,
7.11093804246303)) ;
#74994=CARTESIAN_POINT('Ctrl Pts',(-3.14650618411119,0.734653311026188,
7.11301988346854)) ;
#74995=CARTESIAN_POINT('Ctrl Pts',(-3.14387449159256,0.738267786921109,
7.11706119147952)) ;
#74996=CARTESIAN_POINT('Ctrl Pts',(-3.14270349733143,0.739869138198676,
7.11898770799634)) ;
#74997=CARTESIAN_POINT('Ctrl Pts',(-3.14003428427703,0.743434565765228,
7.12365088269313)) ;
#74998=CARTESIAN_POINT('Ctrl Pts',(-3.13853953335781,0.745372225194674,
7.12646045464107)) ;
#74999=CARTESIAN_POINT('Ctrl Pts',(-3.13653045010517,0.747788501075358,
7.13038308945641)) ;
#75000=CARTESIAN_POINT('Ctrl Pts',(-3.13605623456106,0.748345478006875,
7.13131931951466)) ;
#75001=CARTESIAN_POINT('Ctrl Pts',(-3.13490030581321,0.749663361810016,
7.13362028111691)) ;
#75002=CARTESIAN_POINT('Ctrl Pts',(-3.13422095933187,0.750405401569636,
7.1349879362403)) ;
#75003=CARTESIAN_POINT('Ctrl Pts',(-3.13116301782668,0.753565178819733,
7.14117483383158)) ;
#75004=CARTESIAN_POINT('Ctrl Pts',(-3.12875081675081,0.755569874503869,
7.14614156555835)) ;
#75005=CARTESIAN_POINT('Ctrl Pts',(-3.12605506967943,0.757288027552031,
7.15141997627083)) ;
#75006=CARTESIAN_POINT('Ctrl Pts',(-3.12579739926236,0.75744707015426,7.15192175274669)) ;
#75007=CARTESIAN_POINT('Ctrl Pts',(-3.12252089822597,0.759403912638519,
7.15826199813988)) ;
#75008=CARTESIAN_POINT('Ctrl Pts',(-3.1194641078908,0.760518751613542,7.16374160917873)) ;
#75009=CARTESIAN_POINT('Ctrl Pts',(-3.11411372865795,0.761651857385016,
7.17250963958096)) ;
#75010=CARTESIAN_POINT('Ctrl Pts',(-3.11182852612461,0.761881719502846,
7.17599758854373)) ;
#75011=CARTESIAN_POINT('Ctrl Pts',(-3.10892327200399,0.761989457388304,
7.18009209787526)) ;
#75012=CARTESIAN_POINT('Ctrl Pts',(-3.1083052192423,0.761999861892731,7.18094636296612)) ;
#75013=CARTESIAN_POINT('Ctrl Pts',(-3.10768716647391,0.761999999491749,
7.18179159914902)) ;
#75014=CARTESIAN_POINT('',(-3.14953687287001,0.762,7.1818)) ;
#75015=CARTESIAN_POINT('',(-3.10768716647391,0.761999999491749,7.18179159914902)) ;
#75016=CARTESIAN_POINT('Origin',(-3.14953687287001,0.661999999999999,7.1818)) ;
#75017=CARTESIAN_POINT('Ctrl Pts',(-3.17121692101567,0.762,7.1818)) ;
#75018=CARTESIAN_POINT('Ctrl Pts',(-3.16399023830045,0.762,7.1818)) ;
#75019=CARTESIAN_POINT('Ctrl Pts',(-3.15676355558523,0.762,7.1818)) ;
#75020=CARTESIAN_POINT('Ctrl Pts',(-3.14953687287001,0.762,7.1818)) ;
#75021=CARTESIAN_POINT('Ctrl Pts',(-3.17121692101567,0.762,7.16049051462243)) ;
#75022=CARTESIAN_POINT('Ctrl Pts',(-3.16399023830045,0.761980537877959,
7.16173716654572)) ;
#75023=CARTESIAN_POINT('Ctrl Pts',(-3.15676355558523,0.762015837610647,
7.16371429760845)) ;
#75024=CARTESIAN_POINT('Ctrl Pts',(-3.14953687287001,0.762,7.16625960724294)) ;
#75025=CARTESIAN_POINT('Ctrl Pts',(-3.17121692101567,0.749661462765229,
7.12329552595192)) ;
#75026=CARTESIAN_POINT('Ctrl Pts',(-3.16399023830045,0.751152261593369,
7.1266719591844)) ;
#75027=CARTESIAN_POINT('Ctrl Pts',(-3.15676355558523,0.75338304373689,7.13211431434399)) ;
#75028=CARTESIAN_POINT('Ctrl Pts',(-3.14953687287001,0.755540893518778,
7.1390837819811)) ;
#75029=CARTESIAN_POINT('Ctrl Pts',(-3.17121692101567,0.720057683295033,
7.09882570651471)) ;
#75030=CARTESIAN_POINT('Ctrl Pts',(-3.16399023830045,0.724623549182785,
7.10220324165009)) ;
#75031=CARTESIAN_POINT('Ctrl Pts',(-3.15676355558523,0.731748787702952,
7.10798226702609)) ;
#75032=CARTESIAN_POINT('Ctrl Pts',(-3.14953687287002,0.739012268865877,
7.11695436533126)) ;
#75033=CARTESIAN_POINT('Ctrl Pts',(-3.17121692101567,0.70568090461708,7.09184457452808)) ;
#75034=CARTESIAN_POINT('Ctrl Pts',(-3.16399023830045,0.711535796534348,
7.09468761566807)) ;
#75035=CARTESIAN_POINT('Ctrl Pts',(-3.15676355558523,0.720806263628136,
7.09982543575316)) ;
#75036=CARTESIAN_POINT('Ctrl Pts',(-3.14953687287002,0.730523456132442,
7.10896775467099)) ;
#75037=CARTESIAN_POINT('',(-3.17121692101567,0.762,7.1818)) ;
#75038=CARTESIAN_POINT('',(-3.14953687287001,0.762,7.1818)) ;
#75039=CARTESIAN_POINT('',(-3.17121692101567,0.70568090461708,7.09184457452808)) ;
#75040=CARTESIAN_POINT('Origin',(-3.17121692101567,0.662,7.1818)) ;
#75041=CARTESIAN_POINT('Ctrl Pts',(-3.17121692101567,0.70568090461708,7.09184457452808)) ;
#75042=CARTESIAN_POINT('Ctrl Pts',(-3.16399023830045,0.711535796534348,
7.09468761566807)) ;
#75043=CARTESIAN_POINT('Ctrl Pts',(-3.15676355558523,0.720806263628136,
7.09982543575316)) ;
#75044=CARTESIAN_POINT('Ctrl Pts',(-3.14953687287002,0.730523456132442,
7.10896775467099)) ;
#75045=CARTESIAN_POINT('Ctrl Pts',(-3.20512388881547,0.762,7.1818)) ;
#75046=CARTESIAN_POINT('Ctrl Pts',(-3.2047202344369,0.762,7.1818)) ;
#75047=CARTESIAN_POINT('Ctrl Pts',(-3.20391292567976,0.762,7.1818)) ;
#75048=CARTESIAN_POINT('Ctrl Pts',(-3.20270196254405,0.762,7.1818)) ;
#75049=CARTESIAN_POINT('Ctrl Pts',(-3.20149099940835,0.762,7.1818)) ;
#75050=CARTESIAN_POINT('Ctrl Pts',(-3.19745445562265,0.762,7.1818)) ;
#75051=CARTESIAN_POINT('Ctrl Pts',(-3.18736309615843,0.762,7.1818)) ;
#75052=CARTESIAN_POINT('Ctrl Pts',(-3.17767539107277,0.762,7.1818)) ;
#75053=CARTESIAN_POINT('Ctrl Pts',(-3.17121692101567,0.762,7.1818)) ;
#75054=CARTESIAN_POINT('Ctrl Pts',(-3.20512388881547,0.762,7.15188006996578)) ;
#75055=CARTESIAN_POINT('Ctrl Pts',(-3.2047202344369,0.761992330181026,7.1520702301264)) ;
#75056=CARTESIAN_POINT('Ctrl Pts',(-3.20391292567976,0.76197980992607,7.15243005278884)) ;
#75057=CARTESIAN_POINT('Ctrl Pts',(-3.20270196254405,0.761963555547577,
7.15292464422255)) ;
#75058=CARTESIAN_POINT('Ctrl Pts',(-3.20149099940835,0.761947562028465,
7.15338566691011)) ;
#75059=CARTESIAN_POINT('Ctrl Pts',(-3.19745445562265,0.76191470846392,7.15481366906456)) ;
#75060=CARTESIAN_POINT('Ctrl Pts',(-3.18736309615843,0.761861071074269,
7.15758629528363)) ;
#75061=CARTESIAN_POINT('Ctrl Pts',(-3.17767539107277,0.76201739325461,7.15937638460794)) ;
#75062=CARTESIAN_POINT('Ctrl Pts',(-3.17121692101567,0.762,7.16049051462243)) ;
#75063=CARTESIAN_POINT('Ctrl Pts',(-3.20512388881547,0.736911811379183,
7.10005033527499)) ;
#75064=CARTESIAN_POINT('Ctrl Pts',(-3.2047202344369,0.737245219347505,7.10054319817603)) ;
#75065=CARTESIAN_POINT('Ctrl Pts',(-3.20391292567976,0.737869883520249,
7.10148033026224)) ;
#75066=CARTESIAN_POINT('Ctrl Pts',(-3.20270196254405,0.738711770607014,
7.10277348618571)) ;
#75067=CARTESIAN_POINT('Ctrl Pts',(-3.20149099940835,0.73948195346955,7.1039804248426)) ;
#75068=CARTESIAN_POINT('Ctrl Pts',(-3.19745445562265,0.741829197217652,
7.10775251408813)) ;
#75069=CARTESIAN_POINT('Ctrl Pts',(-3.18736309615843,0.746011102788114,
7.11515718689346)) ;
#75070=CARTESIAN_POINT('Ctrl Pts',(-3.17767539107277,0.748329114460406,
7.12027803292724)) ;
#75071=CARTESIAN_POINT('Ctrl Pts',(-3.17121692101567,0.749661438013567,
7.12329554369824)) ;
#75072=CARTESIAN_POINT('Ctrl Pts',(-3.20512388881547,0.684439947525491,
7.08179999999996)) ;
#75073=CARTESIAN_POINT('Ctrl Pts',(-3.2047202344369,0.685279518511752,7.08202134573632)) ;
#75074=CARTESIAN_POINT('Ctrl Pts',(-3.20391292567976,0.686865903002586,
7.08246093200816)) ;
#75075=CARTESIAN_POINT('Ctrl Pts',(-3.20270196254405,0.689032722166199,
7.08311409360665)) ;
#75076=CARTESIAN_POINT('Ctrl Pts',(-3.20149099940835,0.691037008739264,
7.08376272980254)) ;
#75077=CARTESIAN_POINT('Ctrl Pts',(-3.19745445562265,0.697229783074605,
7.08590527875505)) ;
#75078=CARTESIAN_POINT('Ctrl Pts',(-3.18736309615843,0.708839952636613,
7.09112838260725)) ;
#75079=CARTESIAN_POINT('Ctrl Pts',(-3.17767539107277,0.715977179240427,
7.09580721097557)) ;
#75080=CARTESIAN_POINT('Ctrl Pts',(-3.17121692101567,0.720057683295033,
7.09882570651471)) ;
#75081=CARTESIAN_POINT('Ctrl Pts',(-3.20512388881547,0.661999999999825,
7.0818)) ;
#75082=CARTESIAN_POINT('Ctrl Pts',(-3.2047202344369,0.662977161851475,7.0818)) ;
#75083=CARTESIAN_POINT('Ctrl Pts',(-3.20391292567976,0.664831438935661,
7.08182813262089)) ;
#75084=CARTESIAN_POINT('Ctrl Pts',(-3.20270196254405,0.667381960953565,
7.08193509059619)) ;
#75085=CARTESIAN_POINT('Ctrl Pts',(-3.20149099940835,0.669755131272068,
7.08209149598161)) ;
#75086=CARTESIAN_POINT('Ctrl Pts',(-3.19745445562265,0.677136096351085,
7.08275930201879)) ;
#75087=CARTESIAN_POINT('Ctrl Pts',(-3.18736309615843,0.691331994006365,
7.08558723772615)) ;
#75088=CARTESIAN_POINT('Ctrl Pts',(-3.17767539107277,0.700448400904743,
7.08930375506813)) ;
#75089=CARTESIAN_POINT('Ctrl Pts',(-3.17121692101567,0.705680904617079,
7.09184457452808)) ;
#75090=CARTESIAN_POINT('',(-3.17121692101567,0.762,7.1818)) ;
#75091=CARTESIAN_POINT('Ctrl Pts',(-3.20512388881547,0.661999999999825,
7.0818)) ;
#75092=CARTESIAN_POINT('Ctrl Pts',(-3.2047202344369,0.662977161851475,7.0818)) ;
#75093=CARTESIAN_POINT('Ctrl Pts',(-3.20431658005833,0.663904297939892,
7.08181418112561)) ;
#75094=CARTESIAN_POINT('Ctrl Pts',(-3.20350927130119,0.665681610657567,
7.08186384002979)) ;
#75095=CARTESIAN_POINT('Ctrl Pts',(-3.20310561692262,0.666531791312267,
7.08189935834228)) ;
#75096=CARTESIAN_POINT('Ctrl Pts',(-3.20229830816548,0.668173012083282,
7.08198732917139)) ;
#75097=CARTESIAN_POINT('Ctrl Pts',(-3.20189465378691,0.668964039857316,
7.0820398363167)) ;
#75098=CARTESIAN_POINT('Ctrl Pts',(-3.20108734502978,0.670493217907198,
7.08215837537036)) ;
#75099=CARTESIAN_POINT('Ctrl Pts',(-3.20068369065121,0.67123138690257,7.08222438102225)) ;
#75100=CARTESIAN_POINT('Ctrl Pts',(-3.19847904880683,0.675159362227489,
7.08261718651246)) ;
#75101=CARTESIAN_POINT('Ctrl Pts',(-3.19667806134099,0.677991390732854,
7.08305203429455)) ;
#75102=CARTESIAN_POINT('Ctrl Pts',(-3.19344882631242,0.682614461197415,
7.08392572248012)) ;
#75103=CARTESIAN_POINT('Ctrl Pts',(-3.19202057874969,0.684499933880174,
7.08434667817418)) ;
#75104=CARTESIAN_POINT('Ctrl Pts',(-3.18778558324305,0.689801348801302,
7.08567402178888)) ;
#75105=CARTESIAN_POINT('Ctrl Pts',(-3.18497883529916,0.692934482334903,
7.08665681146921)) ;
#75106=CARTESIAN_POINT('Ctrl Pts',(-3.17911128623287,0.698892281462533,
7.0887953603999)) ;
#75107=CARTESIAN_POINT('Ctrl Pts',(-3.17605048511049,0.70166412270943,7.08995925874849)) ;
#75108=CARTESIAN_POINT('Ctrl Pts',(-3.17239876299729,0.704716249384997,
7.09138087098938)) ;
#75109=CARTESIAN_POINT('Ctrl Pts',(-3.17180784200648,0.705202154038262,
7.09161210096399)) ;
#75110=CARTESIAN_POINT('Ctrl Pts',(-3.17121692101567,0.705680904617079,
7.09184457452808)) ;
#75111=CARTESIAN_POINT('Origin',(-3.21546217517793,0.862,0.)) ;
#75112=CARTESIAN_POINT('',(-3.21546217517793,0.762,7.36730649953872)) ;
#75113=CARTESIAN_POINT('',(-3.21546217517793,0.762,0.)) ;
#75114=CARTESIAN_POINT('',(-3.31205160669424,0.887893661760289,7.36730649953872)) ;
#75115=CARTESIAN_POINT('Origin',(-3.21546217517793,0.862,7.36730649953872)) ;
#75116=CARTESIAN_POINT('',(-3.31205160669424,0.887893661760288,0.)) ;
#75117=CARTESIAN_POINT('Origin',(-9.525,0.762,8.72161438184689)) ;
#75118=CARTESIAN_POINT('',(-0.598228027472806,0.762,7.1818)) ;
#75119=CARTESIAN_POINT('',(0.,0.762,7.1818)) ;
#75120=CARTESIAN_POINT('',(-0.731723284002018,0.762,8.59150875795967)) ;
#75121=CARTESIAN_POINT('',(-0.787882878836553,0.762,9.1845535952074)) ;
#75122=CARTESIAN_POINT('',(-3.07434158440252,0.762,7.64111756647598)) ;
#75123=CARTESIAN_POINT('Origin',(0.,0.762,3.42553041237115)) ;
#75124=CARTESIAN_POINT('Ctrl Pts',(-3.21546217517793,0.762,7.36730649953872)) ;
#75125=CARTESIAN_POINT('Ctrl Pts',(-3.21546217517793,0.762,7.41298218019493)) ;
#75126=CARTESIAN_POINT('Ctrl Pts',(-3.19308177554602,0.762,7.51957930543031)) ;
#75127=CARTESIAN_POINT('Ctrl Pts',(-3.12354733145101,0.762,7.60523282045775)) ;
#75128=CARTESIAN_POINT('Ctrl Pts',(-3.07434158440252,0.762,7.64111756647598)) ;
#75129=CARTESIAN_POINT('Ctrl Pts',(3.31205160669424,0.887893661760288,6.793484)) ;
#75130=CARTESIAN_POINT('Ctrl Pts',(3.31287790153465,0.884811388204746,6.79777468341573)) ;
#75131=CARTESIAN_POINT('Ctrl Pts',(3.31364139250919,0.881705147287931,6.80206837154771)) ;
#75132=CARTESIAN_POINT('Ctrl Pts',(3.32718180865331,0.82115248175181,6.88564197720954)) ;
#75133=CARTESIAN_POINT('Ctrl Pts',(3.31839899815499,0.756128366293949,6.96625435392858)) ;
#75134=CARTESIAN_POINT('Ctrl Pts',(3.2794239181545,0.707077062047012,7.03908289042949)) ;
#75135=CARTESIAN_POINT('Ctrl Pts',(3.31205160669424,0.887893661760288,6.793484)) ;
#75136=CARTESIAN_POINT('Ctrl Pts',(3.31274522369532,0.885306307663944,6.79809343284722)) ;
#75137=CARTESIAN_POINT('Ctrl Pts',(3.31334303732996,0.882699040456766,6.80271791145202)) ;
#75138=CARTESIAN_POINT('Ctrl Pts',(3.32434030414173,0.831838892965902,6.89249111240128)) ;
#75139=CARTESIAN_POINT('Ctrl Pts',(3.30868757227878,0.775373519472581,6.97904841531997)) ;
#75140=CARTESIAN_POINT('Ctrl Pts',(3.26540522272929,0.738492188311657,7.04973176535319)) ;
#75141=CARTESIAN_POINT('Ctrl Pts',(3.31205160669424,0.887893661760288,6.793484)) ;
#75142=CARTESIAN_POINT('Ctrl Pts',(3.31261121114413,0.88580620591146,6.79841624482426)) ;
#75143=CARTESIAN_POINT('Ctrl Pts',(3.31307594580977,0.883698810455707,6.8033633352161)) ;
#75144=CARTESIAN_POINT('Ctrl Pts',(3.32193595542266,0.842609793416925,6.899410563539)) ;
#75145=CARTESIAN_POINT('Ctrl Pts',(3.30625449205529,0.797119135192663,6.99229450465509)) ;
#75146=CARTESIAN_POINT('Ctrl Pts',(3.26888725785268,0.772941191040193,7.07185431702686)) ;
#75147=CARTESIAN_POINT('Ctrl Pts',(3.31205160669424,0.887893661760288,6.793484)) ;
#75148=CARTESIAN_POINT('Ctrl Pts',(3.31247680269833,0.886307580938705,6.79874217767332)) ;
#75149=CARTESIAN_POINT('Ctrl Pts',(3.31286385709175,0.884707693083394,6.8040040381699)) ;
#75150=CARTESIAN_POINT('Ctrl Pts',(3.31959859765461,0.85348470139946,6.90642242752542)) ;
#75151=CARTESIAN_POINT('Ctrl Pts',(3.31286250738096,0.819472008973411,7.00521187075637)) ;
#75152=CARTESIAN_POINT('Ctrl Pts',(3.2881405032392,0.793313315480956,7.09446231571417)) ;
#75153=CARTESIAN_POINT('',(3.2881405032392,0.793313315480956,7.09446231571417)) ;
#75154=CARTESIAN_POINT('Origin',(3.36081883130047,0.724626630961912,7.09446231571417)) ;
#75155=CARTESIAN_POINT('Ctrl Pts',(3.31205160669424,0.887893661760288,6.793484)) ;
#75156=CARTESIAN_POINT('Ctrl Pts',(3.31247680269833,0.886307580938705,6.79874217767332)) ;
#75157=CARTESIAN_POINT('Ctrl Pts',(3.31286385709175,0.884707693083394,6.8040040381699)) ;
#75158=CARTESIAN_POINT('Ctrl Pts',(3.31959859765461,0.85348470139946,6.90642242752542)) ;
#75159=CARTESIAN_POINT('Ctrl Pts',(3.31286250738096,0.819472008973411,7.00521187075637)) ;
#75160=CARTESIAN_POINT('Ctrl Pts',(3.2881405032392,0.793313315480956,7.09446231571417)) ;
#75161=CARTESIAN_POINT('Ctrl Pts',(3.25930415002282,0.772122965994088,7.15495237069481)) ;
#75162=CARTESIAN_POINT('Ctrl Pts',(3.27166340593034,0.77815180520304,7.13954927383579)) ;
#75163=CARTESIAN_POINT('Ctrl Pts',(3.28134410254902,0.786121950190065,7.11899842460839)) ;
#75164=CARTESIAN_POINT('Ctrl Pts',(3.28814050323922,0.793313315480976,7.0944623157141)) ;
#75165=CARTESIAN_POINT('Ctrl Pts',(3.24720304082971,0.766220050630804,7.13091195407385)) ;
#75166=CARTESIAN_POINT('Ctrl Pts',(3.25869714385255,0.769669020390238,7.11948103534318)) ;
#75167=CARTESIAN_POINT('Ctrl Pts',(3.26931499881139,0.775745323042673,7.10257847346906)) ;
#75168=CARTESIAN_POINT('Ctrl Pts',(3.27713864873267,0.781672101514854,7.0815434593213)) ;
#75169=CARTESIAN_POINT('Ctrl Pts',(3.23542257587948,0.73701785926868,7.08914722322202)) ;
#75170=CARTESIAN_POINT('Ctrl Pts',(3.24613293999889,0.741135418665641,7.08437187855016)) ;
#75171=CARTESIAN_POINT('Ctrl Pts',(3.25765493730861,0.747264169147483,7.07395698641591)) ;
#75172=CARTESIAN_POINT('Ctrl Pts',(3.26627246770002,0.753460431697836,7.05898639091382)) ;
#75173=CARTESIAN_POINT('Ctrl Pts',(3.24626907090961,0.691101901539863,7.07061000050612)) ;
#75174=CARTESIAN_POINT('Ctrl Pts',(3.25699307007247,0.701213312565527,7.06492336370951)) ;
#75175=CARTESIAN_POINT('Ctrl Pts',(3.26646853336989,0.711672429614719,7.05583711304386)) ;
#75176=CARTESIAN_POINT('Ctrl Pts',(3.27341590582957,0.720540687589136,7.04364669396793)) ;
#75177=CARTESIAN_POINT('Ctrl Pts',(3.25413500684156,0.672122965994088,7.0683761853474)) ;
#75178=CARTESIAN_POINT('Ctrl Pts',(3.2651569253511,0.684626627018251,7.0606746369179)) ;
#75179=CARTESIAN_POINT('Ctrl Pts',(3.27351027276397,0.697039528212523,7.05095544131491)) ;
#75180=CARTESIAN_POINT('Ctrl Pts',(3.27942391815468,0.707077062047157,7.03908289042919)) ;
#75181=CARTESIAN_POINT('',(3.25930415002282,0.772122965994088,7.15495237069481)) ;
#75182=CARTESIAN_POINT('Ctrl Pts',(3.28814050323922,0.793313315480976,7.0944623157141)) ;
#75183=CARTESIAN_POINT('Ctrl Pts',(3.28134410254902,0.786121950190065,7.11899842460839)) ;
#75184=CARTESIAN_POINT('Ctrl Pts',(3.27166340593034,0.77815180520304,7.13954927383579)) ;
#75185=CARTESIAN_POINT('Ctrl Pts',(3.25930415002282,0.772122965994088,7.15495237069481)) ;
#75186=CARTESIAN_POINT('',(3.25413500684156,0.672122965994089,7.0683761853474)) ;
#75187=CARTESIAN_POINT('Origin',(3.30314612486772,0.682245931988177,7.15495237069481)) ;
#75188=CARTESIAN_POINT('Ctrl Pts',(3.25413500684156,0.672122965994088,7.0683761853474)) ;
#75189=CARTESIAN_POINT('Ctrl Pts',(3.25939413790927,0.678089113547748,7.06470137568699)) ;
#75190=CARTESIAN_POINT('Ctrl Pts',(3.26403592778354,0.684033341437091,7.06055993267801)) ;
#75191=CARTESIAN_POINT('Ctrl Pts',(3.27227350301661,0.69552988984136,7.05122867472234)) ;
#75192=CARTESIAN_POINT('Ctrl Pts',(3.27584190800862,0.701066725669454,7.04601233351373)) ;
#75193=CARTESIAN_POINT('Ctrl Pts',(3.27902209145408,0.706397160160282,7.03988142131703)) ;
#75194=CARTESIAN_POINT('Ctrl Pts',(3.27922442992696,0.706738460439687,7.03948339366842)) ;
#75195=CARTESIAN_POINT('Ctrl Pts',(3.27942391815467,0.707077062047156,7.03908289042919)) ;
#75196=CARTESIAN_POINT('Ctrl Pts',(3.25413500684156,0.672122965994089,7.0683761853474)) ;
#75197=CARTESIAN_POINT('Ctrl Pts',(3.24907828834913,0.668116125762004,7.07170731541641)) ;
#75198=CARTESIAN_POINT('Ctrl Pts',(3.23589756364382,0.660507101185358,7.07825767676846)) ;
#75199=CARTESIAN_POINT('Ctrl Pts',(3.21994984969872,0.659191608936344,7.08122103082289)) ;
#75200=CARTESIAN_POINT('Ctrl Pts',(3.2105035504766,0.660979117346626,7.08167176697949)) ;
#75201=CARTESIAN_POINT('Ctrl Pts',(3.24364709226563,0.697428213388455,7.07135460555903)) ;
#75202=CARTESIAN_POINT('Ctrl Pts',(3.23904198217673,0.694613604341688,7.07381433044803)) ;
#75203=CARTESIAN_POINT('Ctrl Pts',(3.22806793638566,0.6897306982185,7.07820430178644)) ;
#75204=CARTESIAN_POINT('Ctrl Pts',(3.21711227111321,0.689553339863549,7.08049944622424)) ;
#75205=CARTESIAN_POINT('Ctrl Pts',(3.21048830525436,0.691091935293638,7.08136471265295)) ;
#75206=CARTESIAN_POINT('Ctrl Pts',(3.23575890408185,0.743524350516923,7.09478029250273)) ;
#75207=CARTESIAN_POINT('Ctrl Pts',(3.23142097756856,0.742576953554628,7.09766695337376)) ;
#75208=CARTESIAN_POINT('Ctrl Pts',(3.2222182842119,0.741823967860392,7.10251922930311)) ;
#75209=CARTESIAN_POINT('Ctrl Pts',(3.21582930459776,0.742834159269563,7.10502824890571)) ;
#75210=CARTESIAN_POINT('Ctrl Pts',(3.21172314782629,0.74350130228817,7.10623570350962)) ;
#75211=CARTESIAN_POINT('Ctrl Pts',(3.25022831812799,0.767695779471625,7.13692205822909)) ;
#75212=CARTESIAN_POINT('Ctrl Pts',(3.24530748822129,0.765971442670608,7.14245586827297)) ;
#75213=CARTESIAN_POINT('Ctrl Pts',(3.23346592056584,0.762891866825044,7.15309078996572)) ;
#75214=CARTESIAN_POINT('Ctrl Pts',(3.22141912805696,0.76190207647211,7.15799343781877)) ;
#75215=CARTESIAN_POINT('Ctrl Pts',(3.21434217223136,0.761999999999958,7.15898553043246)) ;
#75216=CARTESIAN_POINT('Ctrl Pts',(3.25930415002282,0.772122965994088,7.15495237069481)) ;
#75217=CARTESIAN_POINT('Ctrl Pts',(3.253958434241,0.769515328354208,7.16161463083282)) ;
#75218=CARTESIAN_POINT('Ctrl Pts',(3.24030166703836,0.76423379035022,7.17471535353693)) ;
#75219=CARTESIAN_POINT('Ctrl Pts',(3.22454046181232,0.762000000000338,7.18064206164579)) ;
#75220=CARTESIAN_POINT('Ctrl Pts',(3.21546217518166,0.761999999999999,7.18154353395898)) ;
#75221=CARTESIAN_POINT('',(3.2154621751798,0.761999999999999,7.18154353395898)) ;
#75222=CARTESIAN_POINT('',(3.2105035504766,0.660979117346626,7.08167176697949)) ;
#75223=CARTESIAN_POINT('Origin',(3.2154621751854,0.661999999999999,7.18154353395898)) ;
#75224=CARTESIAN_POINT('Ctrl Pts',(3.2105035504766,0.660979117346626,7.08167176697949)) ;
#75225=CARTESIAN_POINT('Ctrl Pts',(3.21994984969872,0.659191608936344,7.08122103082289)) ;
#75226=CARTESIAN_POINT('Ctrl Pts',(3.23589756364382,0.660507101185358,7.07825767676846)) ;
#75227=CARTESIAN_POINT('Ctrl Pts',(3.24907828834913,0.668116125762004,7.07170731541641)) ;
#75228=CARTESIAN_POINT('Ctrl Pts',(3.25413500684156,0.672122965994089,7.0683761853474)) ;
#75229=CARTESIAN_POINT('Ctrl Pts',(3.25930415002282,0.772122965994088,7.15495237069481)) ;
#75230=CARTESIAN_POINT('Ctrl Pts',(3.253958434241,0.769515328354208,7.16161463083282)) ;
#75231=CARTESIAN_POINT('Ctrl Pts',(3.24030166703836,0.76423379035022,7.17471535353693)) ;
#75232=CARTESIAN_POINT('Ctrl Pts',(3.22454046181232,0.762000000000338,7.18064206164579)) ;
#75233=CARTESIAN_POINT('Ctrl Pts',(3.21546217518166,0.761999999999999,7.18154353395898)) ;
#75234=CARTESIAN_POINT('Ctrl Pts',(3.2105035504766,0.660979117346627,7.08167176697949)) ;
#75235=CARTESIAN_POINT('Ctrl Pts',(3.20871214489261,0.66131810222033,7.08175724503273)) ;
#75236=CARTESIAN_POINT('Ctrl Pts',(3.20691819492506,0.661658530855223,7.0818)) ;
#75237=CARTESIAN_POINT('Ctrl Pts',(3.20512388881539,0.662,7.0818)) ;
#75238=CARTESIAN_POINT('Ctrl Pts',(3.21048830525548,0.691091935293674,7.08136471265289)) ;
#75239=CARTESIAN_POINT('Ctrl Pts',(3.20871266627196,0.691367100691539,7.08155544690455)) ;
#75240=CARTESIAN_POINT('Ctrl Pts',(3.20691291140055,0.691643821063274,7.08169470978418)) ;
#75241=CARTESIAN_POINT('Ctrl Pts',(3.20512388881539,0.691919930034189,7.0818)) ;
#75242=CARTESIAN_POINT('Ctrl Pts',(3.21172314486594,0.743501373347166,7.10623564382333)) ;
#75243=CARTESIAN_POINT('Ctrl Pts',(3.2095315878856,0.743584576017367,7.1065058196023)) ;
#75244=CARTESIAN_POINT('Ctrl Pts',(3.20733490885682,0.743666470692696,7.10672585564236)) ;
#75245=CARTESIAN_POINT('Ctrl Pts',(3.20512388881539,0.743749639050895,7.1068882100183)) ;
#75246=CARTESIAN_POINT('Ctrl Pts',(3.21434217223511,0.762,7.15898553043244)) ;
#75247=CARTESIAN_POINT('Ctrl Pts',(3.21127367849935,0.761999102403065,7.15918594173638)) ;
#75248=CARTESIAN_POINT('Ctrl Pts',(3.20820121468723,0.762000880498864,7.15931169382832)) ;
#75249=CARTESIAN_POINT('Ctrl Pts',(3.20512388881539,0.762,7.15936005247436)) ;
#75250=CARTESIAN_POINT('Ctrl Pts',(3.2154621751854,0.762,7.18154353395898)) ;
#75251=CARTESIAN_POINT('Ctrl Pts',(3.21201894456551,0.762,7.18171449006546)) ;
#75252=CARTESIAN_POINT('Ctrl Pts',(3.20857144403868,0.762,7.1818)) ;
#75253=CARTESIAN_POINT('Ctrl Pts',(3.20512388881539,0.762,7.1818)) ;
#75254=CARTESIAN_POINT('',(3.2051238888154,0.762,7.1818)) ;
#75255=CARTESIAN_POINT('',(3.20512388881539,0.662,7.0818)) ;
#75256=CARTESIAN_POINT('Origin',(3.20512388881539,0.662,7.1818)) ;
#75257=CARTESIAN_POINT('Origin',(3.20487923750922,0.663831325042322,7.00284764547056)) ;
#75258=CARTESIAN_POINT('Origin',(3.20581132727714,0.76199999999966,7.02444419421177)) ;
#75259=CARTESIAN_POINT('Ctrl Pts',(3.10768744607367,0.761999999467905,7.18179140434587)) ;
#75260=CARTESIAN_POINT('Ctrl Pts',(3.10820341545623,0.762,7.18179999999999)) ;
#75261=CARTESIAN_POINT('Ctrl Pts',(3.10871938483883,0.762,7.18179999999999)) ;
#75262=CARTESIAN_POINT('Ctrl Pts',(3.11460889004124,0.762,7.18180000000001)) ;
#75263=CARTESIAN_POINT('Ctrl Pts',(3.12266919377095,0.762,7.1818)) ;
#75264=CARTESIAN_POINT('Ctrl Pts',(3.13341626541058,0.762,7.1818)) ;
#75265=CARTESIAN_POINT('Ctrl Pts',(3.14287155003351,0.762,7.1818)) ;
#75266=CARTESIAN_POINT('Ctrl Pts',(3.14964006674653,0.762,7.1818)) ;
#75267=CARTESIAN_POINT('Ctrl Pts',(3.15372181554966,0.761999999999999,7.1818)) ;
#75268=CARTESIAN_POINT('Ctrl Pts',(3.10768744607367,0.761999999467905,7.18179140434587)) ;
#75269=CARTESIAN_POINT('Ctrl Pts',(3.10820341545672,0.76199997751292,7.18166386825364)) ;
#75270=CARTESIAN_POINT('Ctrl Pts',(3.10871938483883,0.762,7.1815280060974)) ;
#75271=CARTESIAN_POINT('Ctrl Pts',(3.11460889004124,0.762,7.1799608805651)) ;
#75272=CARTESIAN_POINT('Ctrl Pts',(3.12266919377095,0.762,7.17741226428925)) ;
#75273=CARTESIAN_POINT('Ctrl Pts',(3.13341626541058,0.762,7.17291023642561)) ;
#75274=CARTESIAN_POINT('Ctrl Pts',(3.14287155003351,0.762,7.16868971481193)) ;
#75275=CARTESIAN_POINT('Ctrl Pts',(3.14964006674653,0.762,7.1661262931308)) ;
#75276=CARTESIAN_POINT('Ctrl Pts',(3.15372181554966,0.761999999999999,7.16488752501317)) ;
#75277=CARTESIAN_POINT('Ctrl Pts',(3.10768744607367,0.761999999467905,7.18179140434587)) ;
#75278=CARTESIAN_POINT('Ctrl Pts',(3.10820341545704,0.761999937929388,7.18142423841737)) ;
#75279=CARTESIAN_POINT('Ctrl Pts',(3.10871938483883,0.761998151108146,7.18105256832397)) ;
#75280=CARTESIAN_POINT('Ctrl Pts',(3.1146088900412,0.761969548435925,7.17671715413705)) ;
#75281=CARTESIAN_POINT('Ctrl Pts',(3.12266919377094,0.761700099488059,7.16971001224105)) ;
#75282=CARTESIAN_POINT('Ctrl Pts',(3.13341626541057,0.760034666415805,7.15732329778495)) ;
#75283=CARTESIAN_POINT('Ctrl Pts',(3.1428715500335,0.75760394642085,7.14570932205733)) ;
#75284=CARTESIAN_POINT('Ctrl Pts',(3.14964006674653,0.755469629013722,7.13867554654612)) ;
#75285=CARTESIAN_POINT('Ctrl Pts',(3.15372181554965,0.754297293609929,7.13525111814463)) ;
#75286=CARTESIAN_POINT('Ctrl Pts',(3.10768744607367,0.761999999467905,7.18179140434587)) ;
#75287=CARTESIAN_POINT('Ctrl Pts',(3.10820341545741,0.761999898346827,7.18118461445737)) ;
#75288=CARTESIAN_POINT('Ctrl Pts',(3.10871938483883,0.761993843816192,7.18057701642878)) ;
#75289=CARTESIAN_POINT('Ctrl Pts',(3.11460889004116,0.761875850635945,7.17347680246517)) ;
#75290=CARTESIAN_POINT('Ctrl Pts',(3.12266919377094,0.760857575245186,7.16195813475203)) ;
#75291=CARTESIAN_POINT('Ctrl Pts',(3.13341626541056,0.75470827730496,7.14253521372758)) ;
#75292=CARTESIAN_POINT('Ctrl Pts',(3.1428715500335,0.746000976828155,7.12546626554375)) ;
#75293=CARTESIAN_POINT('Ctrl Pts',(3.14964006674653,0.738700687509333,7.11630258534313)) ;
#75294=CARTESIAN_POINT('Ctrl Pts',(3.15372181554965,0.734844333349612,7.11213480673515)) ;
#75295=CARTESIAN_POINT('Ctrl Pts',(3.10768744607367,0.761999999467905,7.18179140434587)) ;
#75296=CARTESIAN_POINT('Ctrl Pts',(3.10820341545899,0.761999881560119,7.18108299149052)) ;
#75297=CARTESIAN_POINT('Ctrl Pts',(3.10871938483884,0.76199264020277,7.18037081204062)) ;
#75298=CARTESIAN_POINT('Ctrl Pts',(3.11460889004116,0.761810225860248,7.17211020648586)) ;
#75299=CARTESIAN_POINT('Ctrl Pts',(3.12266919377094,0.760392329518759,7.15861536359771)) ;
#75300=CARTESIAN_POINT('Ctrl Pts',(3.13341626541056,0.751826307912168,7.13644513645035)) ;
#75301=CARTESIAN_POINT('Ctrl Pts',(3.1428715500335,0.739875257225671,7.11761639275596)) ;
#75302=CARTESIAN_POINT('Ctrl Pts',(3.14964006674653,0.730040128626012,7.10821938255966)) ;
#75303=CARTESIAN_POINT('Ctrl Pts',(3.15372181554966,0.724964736792743,7.10411096076474)) ;
#75304=CARTESIAN_POINT('',(3.14953687287002,0.730523456132444,7.10896775467099)) ;
#75305=CARTESIAN_POINT('',(3.14953687287002,0.762,7.1818)) ;
#75306=CARTESIAN_POINT('Origin',(3.14953687287002,0.662,7.1818)) ;
#75307=CARTESIAN_POINT('',(3.10768744685834,0.761999999467905,7.18179140434604)) ;
#75308=CARTESIAN_POINT('',(3.14953687287002,0.762,7.1818)) ;
#75309=CARTESIAN_POINT('Ctrl Pts',(3.10768744607367,0.761999999467905,7.18179140434587)) ;
#75310=CARTESIAN_POINT('Ctrl Pts',(3.10814686764283,0.761999895879657,7.181169089747)) ;
#75311=CARTESIAN_POINT('Ctrl Pts',(3.108595512336,0.761994276012473,7.18054760409202)) ;
#75312=CARTESIAN_POINT('Ctrl Pts',(3.10904173751006,0.761982320202708,7.179922051077)) ;
#75313=CARTESIAN_POINT('Ctrl Pts',(3.10910631864829,0.76198058986599,7.17983151623477)) ;
#75314=CARTESIAN_POINT('Ctrl Pts',(3.10917084910702,0.761978727878474,7.17974098537151)) ;
#75315=CARTESIAN_POINT('Ctrl Pts',(3.10923535422143,0.761976735136791,7.17965053196769)) ;
#75316=CARTESIAN_POINT('Ctrl Pts',(3.10924577422062,0.761976413234149,7.17963592034497)) ;
#75317=CARTESIAN_POINT('Ctrl Pts',(3.10925619355847,0.761976088548957,7.17962131002028)) ;
#75318=CARTESIAN_POINT('Ctrl Pts',(3.10926661234177,0.761975761093632,7.17960670141875)) ;
#75319=CARTESIAN_POINT('Ctrl Pts',(3.10934097866288,0.761973423810371,7.17950242936298)) ;
#75320=CARTESIAN_POINT('Ctrl Pts',(3.10941518403546,0.761970942676249,7.17939812937458)) ;
#75321=CARTESIAN_POINT('Ctrl Pts',(3.10948922921177,0.761968316107535,7.17929380201451)) ;
#75322=CARTESIAN_POINT('Ctrl Pts',(3.10968668301525,0.761961311924298,7.179015595721)) ;
#75323=CARTESIAN_POINT('Ctrl Pts',(3.10988299752596,0.761953273432761,7.17873719465478)) ;
#75324=CARTESIAN_POINT('Ctrl Pts',(3.11007818909737,0.761944170760676,7.17845861140893)) ;
#75325=CARTESIAN_POINT('Ctrl Pts',(3.11085895538299,0.761907760072338,7.17734427842554)) ;
#75326=CARTESIAN_POINT('Ctrl Pts',(3.1116217541577,0.761854272437308,7.17622702027995)) ;
#75327=CARTESIAN_POINT('Ctrl Pts',(3.11236770729956,0.761782159002747,7.17510778320945)) ;
#75328=CARTESIAN_POINT('Ctrl Pts',(3.11385961358327,0.761637932133624,7.17286930906843)) ;
#75329=CARTESIAN_POINT('Ctrl Pts',(3.11528416322639,0.761418774233399,7.17062291210547)) ;
#75330=CARTESIAN_POINT('Ctrl Pts',(3.11665012530342,0.761118711339838,7.16837696163586)) ;
#75331=CARTESIAN_POINT('Ctrl Pts',(3.11756076668811,0.760918669410798,7.16687966132279)) ;
#75332=CARTESIAN_POINT('Ctrl Pts',(3.11844535991553,0.760682843534042,7.16538258060634)) ;
#75333=CARTESIAN_POINT('Ctrl Pts',(3.11930647503948,0.76041094654234,7.16388813921314)) ;
#75334=CARTESIAN_POINT('Ctrl Pts',(3.12067324691137,0.759979388496298,7.16151614457083)) ;
#75335=CARTESIAN_POINT('Ctrl Pts',(3.12198086249394,0.759456809631881,7.15915107368702)) ;
#75336=CARTESIAN_POINT('Ctrl Pts',(3.12323968895681,0.75884638944459,7.15680228300592)) ;
#75337=CARTESIAN_POINT('Ctrl Pts',(3.12396045061273,0.758496883394329,7.15545744453084)) ;
#75338=CARTESIAN_POINT('Ctrl Pts',(3.12466522294237,0.758118966837494,7.15411895662314)) ;
#75339=CARTESIAN_POINT('Ctrl Pts',(3.12535596168084,0.757713132778189,7.15278604121403)) ;
#75340=CARTESIAN_POINT('Ctrl Pts',(3.12587161370382,0.757410168513958,7.15179098984526)) ;
#75341=CARTESIAN_POINT('Ctrl Pts',(3.12637944486437,0.757091653201126,7.1507990565287)) ;
#75342=CARTESIAN_POINT('Ctrl Pts',(3.12688026881464,0.756758303828418,7.14981225466973)) ;
#75343=CARTESIAN_POINT('Ctrl Pts',(3.12777798358105,0.756160783174511,7.14804343630581)) ;
#75344=CARTESIAN_POINT('Ctrl Pts',(3.12865309125015,0.755514942557349,7.14628870169546)) ;
#75345=CARTESIAN_POINT('Ctrl Pts',(3.12951212930122,0.754820486702849,7.14455120781842)) ;
#75346=CARTESIAN_POINT('Ctrl Pts',(3.13037116735229,0.754126030848349,7.14281371394138)) ;
#75347=CARTESIAN_POINT('Ctrl Pts',(3.13121414087768,0.753382918701887,7.14109344755347)) ;
#75348=CARTESIAN_POINT('Ctrl Pts',(3.13204762512955,0.752589632180928,7.13939455997675)) ;
#75349=CARTESIAN_POINT('Ctrl Pts',(3.13250636720713,0.752153014565273,7.13845950785698)) ;
#75350=CARTESIAN_POINT('Ctrl Pts',(3.13296221766801,0.75170146888399,7.13753154269046)) ;
#75351=CARTESIAN_POINT('Ctrl Pts',(3.13341626541056,0.751234198256885,7.1366105887522)) ;
#75352=CARTESIAN_POINT('Ctrl Pts',(3.13461212798369,0.750003509494208,7.13418499724911)) ;
#75353=CARTESIAN_POINT('Ctrl Pts',(3.13579548545068,0.748664969355334,7.13180786305741)) ;
#75354=CARTESIAN_POINT('Ctrl Pts',(3.13698623201723,0.74723540828036,7.12948562600539)) ;
#75355=CARTESIAN_POINT('Ctrl Pts',(3.13810837514584,0.745888209655321,7.12729718186106)) ;
#75356=CARTESIAN_POINT('Ctrl Pts',(3.13923713344721,0.744459227164416,7.12515591598396)) ;
#75357=CARTESIAN_POINT('Ctrl Pts',(3.1403891636022,0.742949052380492,7.1230703090154)) ;
#75358=CARTESIAN_POINT('Ctrl Pts',(3.1407492773333,0.74247698602555,7.1224183680017)) ;
#75359=CARTESIAN_POINT('Ctrl Pts',(3.14111156676817,0.741997237039512,7.12177239451161)) ;
#75360=CARTESIAN_POINT('Ctrl Pts',(3.14147656914029,0.741510000116974,7.12113329701046)) ;
#75361=CARTESIAN_POINT('Ctrl Pts',(3.14287298364461,0.739645944544631,7.11868825805063)) ;
#75362=CARTESIAN_POINT('Ctrl Pts',(3.14430910606337,0.737670456610344,7.11634112949919)) ;
#75363=CARTESIAN_POINT('Ctrl Pts',(3.14581501925236,0.735599221670195,7.11409458620081)) ;
#75364=CARTESIAN_POINT('Ctrl Pts',(3.14662638563887,0.734483267296939,7.11288417797046)) ;
#75365=CARTESIAN_POINT('Ctrl Pts',(3.14745801168483,0.73333986361788,7.11170358448786)) ;
#75366=CARTESIAN_POINT('Ctrl Pts',(3.1483146025057,0.732175957104253,7.11055799739402)) ;
#75367=CARTESIAN_POINT('Ctrl Pts',(3.14871637138839,0.73163004719238,7.11002067988431)) ;
#75368=CARTESIAN_POINT('Ctrl Pts',(3.14912363306523,0.731079109520277,7.10949053534834)) ;
#75369=CARTESIAN_POINT('Ctrl Pts',(3.14953687287001,0.730523456132444,7.10896775467099)) ;
#75370=CARTESIAN_POINT('Ctrl Pts',(3.14953687287002,0.762,7.1818)) ;
#75371=CARTESIAN_POINT('Ctrl Pts',(3.15676355558524,0.762,7.1818)) ;
#75372=CARTESIAN_POINT('Ctrl Pts',(3.16399023830045,0.762,7.1818)) ;
#75373=CARTESIAN_POINT('Ctrl Pts',(3.17121692101567,0.762,7.1818)) ;
#75374=CARTESIAN_POINT('Ctrl Pts',(3.14953687287002,0.762,7.16625960724294)) ;
#75375=CARTESIAN_POINT('Ctrl Pts',(3.15676355558524,0.762015837610647,7.16371429760845)) ;
#75376=CARTESIAN_POINT('Ctrl Pts',(3.16399023830045,0.761980537877959,7.16173716654572)) ;
#75377=CARTESIAN_POINT('Ctrl Pts',(3.17121692101567,0.762,7.16049051462243)) ;
#75378=CARTESIAN_POINT('Ctrl Pts',(3.14953687287002,0.75554089351878,7.1390837819811)) ;
#75379=CARTESIAN_POINT('Ctrl Pts',(3.15676355558524,0.75338304373689,7.13211431434399)) ;
#75380=CARTESIAN_POINT('Ctrl Pts',(3.16399023830045,0.751152261593367,7.12667195918439)) ;
#75381=CARTESIAN_POINT('Ctrl Pts',(3.17121692101567,0.749661462765228,7.12329552595192)) ;
#75382=CARTESIAN_POINT('Ctrl Pts',(3.14953687287002,0.739012268865881,7.11695436533126)) ;
#75383=CARTESIAN_POINT('Ctrl Pts',(3.15676355558524,0.731748787702952,7.10798226702609)) ;
#75384=CARTESIAN_POINT('Ctrl Pts',(3.16399023830045,0.724623549182781,7.10220324165008)) ;
#75385=CARTESIAN_POINT('Ctrl Pts',(3.17121692101567,0.720057683295031,7.09882570651471)) ;
#75386=CARTESIAN_POINT('Ctrl Pts',(3.14953687287002,0.730523456132446,7.10896775467099)) ;
#75387=CARTESIAN_POINT('Ctrl Pts',(3.15676355558524,0.720806263628135,7.09982543575316)) ;
#75388=CARTESIAN_POINT('Ctrl Pts',(3.16399023830045,0.711535796534343,7.09468761566807)) ;
#75389=CARTESIAN_POINT('Ctrl Pts',(3.17121692101567,0.705680904617078,7.09184457452808)) ;
#75390=CARTESIAN_POINT('',(3.17121692101567,0.70568090461708,7.09184457452808)) ;
#75391=CARTESIAN_POINT('',(3.17121692101567,0.762,7.1818)) ;
#75392=CARTESIAN_POINT('Origin',(3.17121692101567,0.662,7.1818)) ;
#75393=CARTESIAN_POINT('',(3.17121692101567,0.762,7.1818)) ;
#75394=CARTESIAN_POINT('Ctrl Pts',(3.14953687287002,0.730523456132446,7.10896775467099)) ;
#75395=CARTESIAN_POINT('Ctrl Pts',(3.15676355558524,0.720806263628135,7.09982543575316)) ;
#75396=CARTESIAN_POINT('Ctrl Pts',(3.16399023830045,0.711535796534345,7.09468761566807)) ;
#75397=CARTESIAN_POINT('Ctrl Pts',(3.17121692101567,0.705680904617079,7.09184457452808)) ;
#75398=CARTESIAN_POINT('Ctrl Pts',(3.20512388881539,0.662000000000007,7.0818)) ;
#75399=CARTESIAN_POINT('Ctrl Pts',(3.20472023443682,0.662977161851648,7.0818)) ;
#75400=CARTESIAN_POINT('Ctrl Pts',(3.20391292567969,0.664831055223105,7.08182824388547)) ;
#75401=CARTESIAN_POINT('Ctrl Pts',(3.20229830816541,0.668233044916084,7.08197050745125)) ;
#75402=CARTESIAN_POINT('Ctrl Pts',(3.19947272751544,0.673555722181198,7.0823952931706)) ;
#75403=CARTESIAN_POINT('Ctrl Pts',(3.19382156621548,0.682473494394306,7.08371679048587)) ;
#75404=CARTESIAN_POINT('Ctrl Pts',(3.18413386112985,0.694361345054536,7.08684227892487)) ;
#75405=CARTESIAN_POINT('Ctrl Pts',(3.17606077355848,0.701756526832837,7.08993895993313)) ;
#75406=CARTESIAN_POINT('Ctrl Pts',(3.17121692101566,0.705680904617081,7.09184457452808)) ;
#75407=CARTESIAN_POINT('Ctrl Pts',(3.20512388881539,0.691919930034194,7.0818)) ;
#75408=CARTESIAN_POINT('Ctrl Pts',(3.20472023443682,0.692710054581024,7.08210130272039)) ;
#75409=CARTESIAN_POINT('Ctrl Pts',(3.20391292567969,0.694201036499879,7.08268790815876)) ;
#75410=CARTESIAN_POINT('Ctrl Pts',(3.20229830816541,0.696910532566344,7.08381855754183)) ;
#75411=CARTESIAN_POINT('Ctrl Pts',(3.19947272751544,0.70109258926873,7.0857091269066)) ;
#75412=CARTESIAN_POINT('Ctrl Pts',(3.19382156621548,0.707949082694699,7.08920850079664)) ;
#75413=CARTESIAN_POINT('Ctrl Pts',(3.18413386112985,0.716769011824387,7.09473686068323)) ;
#75414=CARTESIAN_POINT('Ctrl Pts',(3.17606077355848,0.722086120291688,7.09876158175655)) ;
#75415=CARTESIAN_POINT('Ctrl Pts',(3.17121692101566,0.724849942854352,7.10115275051025)) ;
#75416=CARTESIAN_POINT('Ctrl Pts',(3.20512388881539,0.743749664724925,7.10688818862076)) ;
#75417=CARTESIAN_POINT('Ctrl Pts',(3.20472023443682,0.743987662646958,7.10735278843905)) ;
#75418=CARTESIAN_POINT('Ctrl Pts',(3.20391292567969,0.744433617144009,7.10823510700091)) ;
#75419=CARTESIAN_POINT('Ctrl Pts',(3.20229830816541,0.745236150925325,7.10985584551939)) ;
#75420=CARTESIAN_POINT('Ctrl Pts',(3.19947272751544,0.746458040208068,7.11239771899758)) ;
#75421=CARTESIAN_POINT('Ctrl Pts',(3.19382156621548,0.748404219152807,7.11670187166256)) ;
#75422=CARTESIAN_POINT('Ctrl Pts',(3.18413386112984,0.75082846283691,7.12255514112684)) ;
#75423=CARTESIAN_POINT('Ctrl Pts',(3.17606077355848,0.752194333174002,7.1264213810107)) ;
#75424=CARTESIAN_POINT('Ctrl Pts',(3.17121692101566,0.75291924171095,7.12849905621401)) ;
#75425=CARTESIAN_POINT('Ctrl Pts',(3.20512388881539,0.762000000000001,7.15936005247436)) ;
#75426=CARTESIAN_POINT('Ctrl Pts',(3.20472023443682,0.761997480329004,7.1594984375227)) ;
#75427=CARTESIAN_POINT('Ctrl Pts',(3.20391292567969,0.761993403439479,7.15976133310581)) ;
#75428=CARTESIAN_POINT('Ctrl Pts',(3.20229830816542,0.76198653040893,7.16024434777636)) ;
#75429=CARTESIAN_POINT('Ctrl Pts',(3.19947272751544,0.761977017261511,7.16100211541313)) ;
#75430=CARTESIAN_POINT('Ctrl Pts',(3.19382156621548,0.761973864307133,7.16228718255731)) ;
#75431=CARTESIAN_POINT('Ctrl Pts',(3.18413386112985,0.761967804257152,7.16403570034217)) ;
#75432=CARTESIAN_POINT('Ctrl Pts',(3.17606077355848,0.762002880308166,7.16519648369734)) ;
#75433=CARTESIAN_POINT('Ctrl Pts',(3.17121692101567,0.762,7.16581788596682)) ;
#75434=CARTESIAN_POINT('Ctrl Pts',(3.20512388881539,0.762000000000001,7.1818)) ;
#75435=CARTESIAN_POINT('Ctrl Pts',(3.20472023443682,0.762000000000001,7.1818)) ;
#75436=CARTESIAN_POINT('Ctrl Pts',(3.20391292567969,0.762,7.1818)) ;
#75437=CARTESIAN_POINT('Ctrl Pts',(3.20229830816542,0.762000000000001,7.1818)) ;
#75438=CARTESIAN_POINT('Ctrl Pts',(3.19947272751544,0.762,7.1818)) ;
#75439=CARTESIAN_POINT('Ctrl Pts',(3.19382156621548,0.762,7.1818)) ;
#75440=CARTESIAN_POINT('Ctrl Pts',(3.18413386112985,0.762,7.1818)) ;
#75441=CARTESIAN_POINT('Ctrl Pts',(3.17606077355848,0.762,7.1818)) ;
#75442=CARTESIAN_POINT('Ctrl Pts',(3.17121692101567,0.762,7.1818)) ;
#75443=CARTESIAN_POINT('Ctrl Pts',(3.17121692101566,0.70568090461708,7.09184457452808)) ;
#75444=CARTESIAN_POINT('Ctrl Pts',(3.17436786852518,0.703128079505998,7.09060496380315)) ;
#75445=CARTESIAN_POINT('Ctrl Pts',(3.17751881603471,0.700358139827596,7.0893901166366)) ;
#75446=CARTESIAN_POINT('Ctrl Pts',(3.18236266857753,0.695601589255923,7.08759761564935)) ;
#75447=CARTESIAN_POINT('Ctrl Pts',(3.18405557361082,0.693845452611266,7.08698598747326)) ;
#75448=CARTESIAN_POINT('Ctrl Pts',(3.18797743406931,0.689520310025353,7.08562686578412)) ;
#75449=CARTESIAN_POINT('Ctrl Pts',(3.19020638949449,0.68687117977675,7.08489484854452)) ;
#75450=CARTESIAN_POINT('Ctrl Pts',(3.19343562452304,0.682587407723472,7.08393270101539)) ;
#75451=CARTESIAN_POINT('Ctrl Pts',(3.1944359041264,0.681198456542271,7.08364897009716)) ;
#75452=CARTESIAN_POINT('Ctrl Pts',(3.19705080124403,0.677377816432161,7.08296038741939)) ;
#75453=CARTESIAN_POINT('Ctrl Pts',(3.1986654187583,0.674829666389823,7.08258427785979)) ;
#75454=CARTESIAN_POINT('Ctrl Pts',(3.20108734502971,0.670514186935405,7.08215262880689)) ;
#75455=CARTESIAN_POINT('Ctrl Pts',(3.20189465378685,0.668993420670207,7.08203130550947)) ;
#75456=CARTESIAN_POINT('Ctrl Pts',(3.20310561692255,0.666532050590563,7.08189937136985)) ;
#75457=CARTESIAN_POINT('Ctrl Pts',(3.20350927130112,0.665681551511474,7.08186383726635)) ;
#75458=CARTESIAN_POINT('Ctrl Pts',(3.20431658005825,0.663904107368423,7.08181417691199)) ;
#75459=CARTESIAN_POINT('Ctrl Pts',(3.20472023443682,0.662977161851648,7.0818)) ;
#75460=CARTESIAN_POINT('Ctrl Pts',(3.20512388881539,0.662000000000007,7.0818)) ;
#75461=CARTESIAN_POINT('',(3.20512388881539,0.762000000000001,7.1818)) ;
#75462=CARTESIAN_POINT('Ctrl Pts',(3.28702640935013,0.678916496982596,7.03662526114754)) ;
#75463=CARTESIAN_POINT('Ctrl Pts',(3.28505420805782,0.68846506114502,7.03662526114754)) ;
#75464=CARTESIAN_POINT('Ctrl Pts',(3.28250316889159,0.697892264769897,7.03746773980168)) ;
#75465=CARTESIAN_POINT('Ctrl Pts',(3.27942391815487,0.70707706204744,7.03908289042881)) ;
#75466=CARTESIAN_POINT('Ctrl Pts',(3.27867914825951,0.677192417966096,7.04962706151189)) ;
#75467=CARTESIAN_POINT('Ctrl Pts',(3.27680440972048,0.685870309279993,7.04975105769206)) ;
#75468=CARTESIAN_POINT('Ctrl Pts',(3.2743643275819,0.694431071838907,7.05063960533657)) ;
#75469=CARTESIAN_POINT('Ctrl Pts',(3.27140856314625,0.702764080010723,7.05223037429132)) ;
#75470=CARTESIAN_POINT('Ctrl Pts',(3.26731641278835,0.674845509970385,7.06059580486522)) ;
#75471=CARTESIAN_POINT('Ctrl Pts',(3.26548227953707,0.682632591536585,7.06080383849015)) ;
#75472=CARTESIAN_POINT('Ctrl Pts',(3.26310082825167,0.690307046122249,7.06169180427166)) ;
#75473=CARTESIAN_POINT('Ctrl Pts',(3.26021975085612,0.697769125082814,7.06320246322368)) ;
#75474=CARTESIAN_POINT('Ctrl Pts',(3.25413500684156,0.672122965994088,7.0683761853474)) ;
#75475=CARTESIAN_POINT('Ctrl Pts',(3.2523024532275,0.679097662424488,7.06859808108705)) ;
#75476=CARTESIAN_POINT('Ctrl Pts',(3.24994321022021,0.685968760565752,7.0694168668701)) ;
#75477=CARTESIAN_POINT('Ctrl Pts',(3.24710198979478,0.69264777579655,7.07077875440761)) ;
#75478=CARTESIAN_POINT('Origin',(3.20512388881539,0.662,6.9818)) ;
#75479=CARTESIAN_POINT('Origin',(0.,-8.2222504619082E-16,6.9818)) ;
#75480=CARTESIAN_POINT('',(3.20512388881552,-0.661999999999843,7.0818)) ;
#75481=CARTESIAN_POINT('Origin',(0.,-8.2222504619082E-16,7.0818)) ;
#75482=CARTESIAN_POINT('',(3.2105035504766,-0.660979117346626,7.08167176697949)) ;
#75483=CARTESIAN_POINT('Origin',(3.20487923730672,-0.663831325588436,7.00284762309432)) ;
#75484=CARTESIAN_POINT('',(3.25413500684125,-0.672122965993743,7.06837618534762)) ;
#75485=CARTESIAN_POINT('Ctrl Pts',(3.25413500684122,-0.672122965993823,
7.06837618534763)) ;
#75486=CARTESIAN_POINT('Ctrl Pts',(3.24907828834881,-0.66811612576181,7.07170731541658)) ;
#75487=CARTESIAN_POINT('Ctrl Pts',(3.23589756364359,-0.660507101185318,
7.07825767676852)) ;
#75488=CARTESIAN_POINT('Ctrl Pts',(3.21994984969863,-0.659191608936361,
7.0812210308229)) ;
#75489=CARTESIAN_POINT('Ctrl Pts',(3.2105035504766,-0.660979117346626,7.08167176697949)) ;
#75490=CARTESIAN_POINT('Origin',(3.20512388881547,-0.66199999999964,6.9818)) ;
#75491=CARTESIAN_POINT('Ctrl Pts',(3.31205160669424,-0.887893661760288,
6.793484)) ;
#75492=CARTESIAN_POINT('Ctrl Pts',(3.31247680274145,-0.886307580777865,
6.79874217793995)) ;
#75493=CARTESIAN_POINT('Ctrl Pts',(3.31286385708463,-0.884707693113238,
6.80400403812143)) ;
#75494=CARTESIAN_POINT('Ctrl Pts',(3.31959859780673,-0.853484700721658,
6.90642242863736)) ;
#75495=CARTESIAN_POINT('Ctrl Pts',(3.31286250738096,-0.819472008973418,
7.00521187075635)) ;
#75496=CARTESIAN_POINT('Ctrl Pts',(3.28814050323921,-0.793313315480963,
7.09446231571415)) ;
#75497=CARTESIAN_POINT('Ctrl Pts',(3.31205160669424,-0.887893661760288,
6.793484)) ;
#75498=CARTESIAN_POINT('Ctrl Pts',(3.31261121118724,-0.885806205750656,
6.79841624509091)) ;
#75499=CARTESIAN_POINT('Ctrl Pts',(3.31307594580264,-0.883698810485554,
6.80336333516764)) ;
#75500=CARTESIAN_POINT('Ctrl Pts',(3.32193595557477,-0.842609792739121,
6.89941056465093)) ;
#75501=CARTESIAN_POINT('Ctrl Pts',(3.30625449205529,-0.797119135192673,
6.99229450465508)) ;
#75502=CARTESIAN_POINT('Ctrl Pts',(3.26888725785269,-0.7729411910402,7.07185431702684)) ;
#75503=CARTESIAN_POINT('Ctrl Pts',(3.31205160669424,-0.887893661760288,
6.793484)) ;
#75504=CARTESIAN_POINT('Ctrl Pts',(3.31274522373845,-0.885306307503065,
6.79809343311384)) ;
#75505=CARTESIAN_POINT('Ctrl Pts',(3.31334303732283,-0.882699040486607,
6.80271791140361)) ;
#75506=CARTESIAN_POINT('Ctrl Pts',(3.32434030429396,-0.831838892287652,
6.89249111351254)) ;
#75507=CARTESIAN_POINT('Ctrl Pts',(3.30868757227878,-0.775373519472595,
6.97904841531995)) ;
#75508=CARTESIAN_POINT('Ctrl Pts',(3.26540522272931,-0.738492188311667,
7.04973176535317)) ;
#75509=CARTESIAN_POINT('Ctrl Pts',(3.31205160669424,-0.887893661760288,
6.793484)) ;
#75510=CARTESIAN_POINT('Ctrl Pts',(3.31287790157776,-0.884811388043908,
6.79777468368237)) ;
#75511=CARTESIAN_POINT('Ctrl Pts',(3.31364139250205,-0.881705147317766,
6.80206837149932)) ;
#75512=CARTESIAN_POINT('Ctrl Pts',(3.32718180880554,-0.821152481073567,
6.88564197832078)) ;
#75513=CARTESIAN_POINT('Ctrl Pts',(3.31839899815499,-0.756128366293962,
6.96625435392856)) ;
#75514=CARTESIAN_POINT('Ctrl Pts',(3.27942391815451,-0.707077062047025,
7.03908289042947)) ;
#75515=CARTESIAN_POINT('',(3.28814050323921,-0.793313315480963,7.09446231571415)) ;
#75516=CARTESIAN_POINT('Origin',(3.36081883130048,-0.724626630961926,7.09446231571415)) ;
#75517=CARTESIAN_POINT('Ctrl Pts',(3.28814050323921,-0.793313315480963,
7.09446231571415)) ;
#75518=CARTESIAN_POINT('Ctrl Pts',(3.31286250738096,-0.819472008973418,
7.00521187075635)) ;
#75519=CARTESIAN_POINT('Ctrl Pts',(3.31959859780673,-0.853484700721658,
6.90642242863736)) ;
#75520=CARTESIAN_POINT('Ctrl Pts',(3.31286385708463,-0.884707693113238,
6.80400403812143)) ;
#75521=CARTESIAN_POINT('Ctrl Pts',(3.31247680274145,-0.886307580777865,
6.79874217793995)) ;
#75522=CARTESIAN_POINT('Ctrl Pts',(3.31205160669424,-0.887893661760288,
6.793484)) ;
#75523=CARTESIAN_POINT('Ctrl Pts',(3.28814050323922,-0.793313315480982,
7.09446231571408)) ;
#75524=CARTESIAN_POINT('Ctrl Pts',(3.28134410252723,-0.786121950167006,
7.11899842468707)) ;
#75525=CARTESIAN_POINT('Ctrl Pts',(3.27166340596969,-0.778151805222174,
7.13954927378692)) ;
#75526=CARTESIAN_POINT('Ctrl Pts',(3.25930415002248,-0.77212296599392,7.15495237069524)) ;
#75527=CARTESIAN_POINT('Ctrl Pts',(3.27713864873268,-0.781672101514859,
7.08154345932128)) ;
#75528=CARTESIAN_POINT('Ctrl Pts',(3.2693149987863,-0.775745323023668,7.10257847353651)) ;
#75529=CARTESIAN_POINT('Ctrl Pts',(3.25869714388911,-0.76966902040116,7.11948103530695)) ;
#75530=CARTESIAN_POINT('Ctrl Pts',(3.24720304082939,-0.766220050630705,
7.13091195407417)) ;
#75531=CARTESIAN_POINT('Ctrl Pts',(3.26627246770002,-0.753460431697841,
7.05898639091381)) ;
#75532=CARTESIAN_POINT('Ctrl Pts',(3.25765493728098,-0.747264169127614,
7.07395698646391)) ;
#75533=CARTESIAN_POINT('Ctrl Pts',(3.24613294003293,-0.741135418678703,
7.08437187853508)) ;
#75534=CARTESIAN_POINT('Ctrl Pts',(3.23542257587918,-0.737017859268566,
7.08914722322215)) ;
#75535=CARTESIAN_POINT('Ctrl Pts',(3.27341590582958,-0.720540687589143,
7.04364669396792)) ;
#75536=CARTESIAN_POINT('Ctrl Pts',(3.26646853334762,-0.711672429586283,
7.05583711308295)) ;
#75537=CARTESIAN_POINT('Ctrl Pts',(3.25699307010659,-0.701213312597675,
7.06492336369149)) ;
#75538=CARTESIAN_POINT('Ctrl Pts',(3.24626907090931,-0.691101901539582,
7.07061000050628)) ;
#75539=CARTESIAN_POINT('Ctrl Pts',(3.27942391815468,-0.707077062047165,
7.03908289042918)) ;
#75540=CARTESIAN_POINT('Ctrl Pts',(3.27351027274501,-0.697039528180338,
7.05095544135298)) ;
#75541=CARTESIAN_POINT('Ctrl Pts',(3.26515692538619,-0.684626627058012,
7.06067463689345)) ;
#75542=CARTESIAN_POINT('Ctrl Pts',(3.25413500684125,-0.67212296599374,7.06837618534762)) ;
#75543=CARTESIAN_POINT('',(3.25930415002248,-0.77212296599392,7.15495237069524)) ;
#75544=CARTESIAN_POINT('Origin',(3.30314612486703,-0.682245931987841,7.15495237069524)) ;
#75545=CARTESIAN_POINT('Ctrl Pts',(3.25930415002248,-0.77212296599392,7.15495237069524)) ;
#75546=CARTESIAN_POINT('Ctrl Pts',(3.27166340596969,-0.778151805222174,
7.13954927378692)) ;
#75547=CARTESIAN_POINT('Ctrl Pts',(3.28134410252723,-0.786121950167006,
7.11899842468707)) ;
#75548=CARTESIAN_POINT('Ctrl Pts',(3.28814050323922,-0.793313315480982,
7.09446231571408)) ;
#75549=CARTESIAN_POINT('Ctrl Pts',(3.27942391815468,-0.707077062047165,
7.03908289042918)) ;
#75550=CARTESIAN_POINT('Ctrl Pts',(3.27645386391631,-0.702035836552783,
7.04504573022574)) ;
#75551=CARTESIAN_POINT('Ctrl Pts',(3.27285683396309,-0.696395529146179,
7.05045952340178)) ;
#75552=CARTESIAN_POINT('Ctrl Pts',(3.26443586616536,-0.684547202104048,
7.06020168149165)) ;
#75553=CARTESIAN_POINT('Ctrl Pts',(3.25962130503333,-0.678346820108753,
7.06454264301213)) ;
#75554=CARTESIAN_POINT('Ctrl Pts',(3.25413500684125,-0.67212296599374,7.06837618534762)) ;
#75555=CARTESIAN_POINT('Ctrl Pts',(3.25930415002247,-0.772122965993915,
7.15495237069525)) ;
#75556=CARTESIAN_POINT('Ctrl Pts',(3.25395843424068,-0.769515328354075,
7.16161463083315)) ;
#75557=CARTESIAN_POINT('Ctrl Pts',(3.24030166703813,-0.764233790350177,
7.17471535353703)) ;
#75558=CARTESIAN_POINT('Ctrl Pts',(3.22454046181224,-0.762000000000338,
7.1806420616458)) ;
#75559=CARTESIAN_POINT('Ctrl Pts',(3.21546217518166,-0.761999999999999,
7.18154353395898)) ;
#75560=CARTESIAN_POINT('Ctrl Pts',(3.24720304082939,-0.766220050630709,
7.13091195407419)) ;
#75561=CARTESIAN_POINT('Ctrl Pts',(3.242421550768,-0.764811276693603,7.13604987867788)) ;
#75562=CARTESIAN_POINT('Ctrl Pts',(3.2311564898124,-0.762486695804742,7.14584148266612)) ;
#75563=CARTESIAN_POINT('Ctrl Pts',(3.22034137761648,-0.761874515288824,
7.15043685312202)) ;
#75564=CARTESIAN_POINT('Ctrl Pts',(3.2139688379146,-0.761999999999944,7.15146619592362)) ;
#75565=CARTESIAN_POINT('Ctrl Pts',(3.23542257429462,-0.737017860463238,
7.08914722161447)) ;
#75566=CARTESIAN_POINT('Ctrl Pts',(3.23109773333057,-0.735867125998988,
7.09171940959733)) ;
#75567=CARTESIAN_POINT('Ctrl Pts',(3.22191662758841,-0.734718108963128,
7.09591659196459)) ;
#75568=CARTESIAN_POINT('Ctrl Pts',(3.21551228030165,-0.735734718330495,
7.09816262873452)) ;
#75569=CARTESIAN_POINT('Ctrl Pts',(3.21138266038765,-0.736564632620707,
7.0993779386748)) ;
#75570=CARTESIAN_POINT('Ctrl Pts',(3.2462690709093,-0.691101901539656,7.0706100005063)) ;
#75571=CARTESIAN_POINT('Ctrl Pts',(3.24155281302069,-0.687974876169227,
7.07330389695565)) ;
#75572=CARTESIAN_POINT('Ctrl Pts',(3.23004851902068,-0.682396466707053,
7.07825157589535)) ;
#75573=CARTESIAN_POINT('Ctrl Pts',(3.21784961482896,-0.681959937337743,
7.08068560732117)) ;
#75574=CARTESIAN_POINT('Ctrl Pts',(3.21049211655992,-0.683563730806885,
7.08144147623458)) ;
#75575=CARTESIAN_POINT('Ctrl Pts',(3.25413500684122,-0.672122965993823,
7.06837618534763)) ;
#75576=CARTESIAN_POINT('Ctrl Pts',(3.24907828834881,-0.66811612576181,7.07170731541658)) ;
#75577=CARTESIAN_POINT('Ctrl Pts',(3.23589756364359,-0.660507101185318,
7.07825767676852)) ;
#75578=CARTESIAN_POINT('Ctrl Pts',(3.21994984969863,-0.659191608936361,
7.0812210308229)) ;
#75579=CARTESIAN_POINT('Ctrl Pts',(3.2105035504766,-0.660979117346626,7.08167176697949)) ;
#75580=CARTESIAN_POINT('',(3.2154621751798,-0.761999999999999,7.18154353395898)) ;
#75581=CARTESIAN_POINT('Origin',(3.2154621751854,-0.661999999999999,7.18154353395898)) ;
#75582=CARTESIAN_POINT('Ctrl Pts',(3.21546217518166,-0.761999999999999,
7.18154353395898)) ;
#75583=CARTESIAN_POINT('Ctrl Pts',(3.22454046181224,-0.762000000000338,
7.1806420616458)) ;
#75584=CARTESIAN_POINT('Ctrl Pts',(3.24030166703813,-0.764233790350177,
7.17471535353703)) ;
#75585=CARTESIAN_POINT('Ctrl Pts',(3.25395843424068,-0.769515328354075,
7.16161463083315)) ;
#75586=CARTESIAN_POINT('Ctrl Pts',(3.25930415002247,-0.772122965993915,
7.15495237069525)) ;
#75587=CARTESIAN_POINT('Ctrl Pts',(3.2154621751854,-0.762,7.18154353395898)) ;
#75588=CARTESIAN_POINT('Ctrl Pts',(3.21201894456566,-0.762,7.18171449006545)) ;
#75589=CARTESIAN_POINT('Ctrl Pts',(3.20857144403885,-0.762,7.1818)) ;
#75590=CARTESIAN_POINT('Ctrl Pts',(3.20512388881564,-0.762,7.1818)) ;
#75591=CARTESIAN_POINT('Ctrl Pts',(3.21396883791835,-0.762,7.15146619592359)) ;
#75592=CARTESIAN_POINT('Ctrl Pts',(3.21102860740559,-0.761997290973651,
7.15167826758758)) ;
#75593=CARTESIAN_POINT('Ctrl Pts',(3.20807464984533,-0.762002680217736,
7.15181361851019)) ;
#75594=CARTESIAN_POINT('Ctrl Pts',(3.20512388881561,-0.762,7.15188006996581)) ;
#75595=CARTESIAN_POINT('Ctrl Pts',(3.21138265683666,-0.736564691651965,
7.0993778670976)) ;
#75596=CARTESIAN_POINT('Ctrl Pts',(3.20930558735075,-0.736681278140644,
7.09965201966661)) ;
#75597=CARTESIAN_POINT('Ctrl Pts',(3.20722130366678,-0.7367952805891,7.09987813004075)) ;
#75598=CARTESIAN_POINT('Ctrl Pts',(3.20512388881554,-0.736911789981695,
7.1000503609491)) ;
#75599=CARTESIAN_POINT('Ctrl Pts',(3.21049211656076,-0.683563730806912,
7.08144147623454)) ;
#75600=CARTESIAN_POINT('Ctrl Pts',(3.20870975639604,-0.683855790193559,
7.08160438817637)) ;
#75601=CARTESIAN_POINT('Ctrl Pts',(3.20691685125597,-0.684146559499709,
7.08172265074698)) ;
#75602=CARTESIAN_POINT('Ctrl Pts',(3.20512388881552,-0.68443994752562,7.08179999999999)) ;
#75603=CARTESIAN_POINT('Ctrl Pts',(3.2105035504766,-0.660979117346626,7.08167176697949)) ;
#75604=CARTESIAN_POINT('Ctrl Pts',(3.20871214489269,-0.661318102220315,
7.08175724503272)) ;
#75605=CARTESIAN_POINT('Ctrl Pts',(3.20691819492514,-0.661658530855206,
7.0818)) ;
#75606=CARTESIAN_POINT('Ctrl Pts',(3.20512388881552,-0.661999999999975,
7.0818)) ;
#75607=CARTESIAN_POINT('',(3.20512388881569,-0.762,7.1818)) ;
#75608=CARTESIAN_POINT('Origin',(3.20512388881569,-0.662,7.1818)) ;
#75609=CARTESIAN_POINT('Origin',(3.20581132625523,-0.762,7.02444416805792)) ;
#75610=CARTESIAN_POINT('Ctrl Pts',(3.14953687287001,-0.762,7.1818)) ;
#75611=CARTESIAN_POINT('Ctrl Pts',(3.14687049251069,-0.762,7.1818)) ;
#75612=CARTESIAN_POINT('Ctrl Pts',(3.14153773179204,-0.762,7.1818)) ;
#75613=CARTESIAN_POINT('Ctrl Pts',(3.13353859071408,-0.762,7.1818)) ;
#75614=CARTESIAN_POINT('Ctrl Pts',(3.12287306927679,-0.762,7.1818)) ;
#75615=CARTESIAN_POINT('Ctrl Pts',(3.11487392819883,-0.762,7.18180000000002)) ;
#75616=CARTESIAN_POINT('Ctrl Pts',(3.10892329344282,-0.762,7.18179999999999)) ;
#75617=CARTESIAN_POINT('Ctrl Pts',(3.10830541940544,-0.762,7.18179999999999)) ;
#75618=CARTESIAN_POINT('Ctrl Pts',(3.1076875453681,-0.761999999459305,7.181791335163)) ;
#75619=CARTESIAN_POINT('Ctrl Pts',(3.14953687287001,-0.762,7.16625960724294)) ;
#75620=CARTESIAN_POINT('Ctrl Pts',(3.14687049251069,-0.762,7.16719533415535)) ;
#75621=CARTESIAN_POINT('Ctrl Pts',(3.14153773179204,-0.762,7.16928720206195)) ;
#75622=CARTESIAN_POINT('Ctrl Pts',(3.13353859071408,-0.762,7.17285503844539)) ;
#75623=CARTESIAN_POINT('Ctrl Pts',(3.12287306927679,-0.762,7.1773342191656)) ;
#75624=CARTESIAN_POINT('Ctrl Pts',(3.11487392819883,-0.762,7.17988076928538)) ;
#75625=CARTESIAN_POINT('Ctrl Pts',(3.10892329344282,-0.762,7.18147431730214)) ;
#75626=CARTESIAN_POINT('Ctrl Pts',(3.10830541940608,-0.761999972911341,
7.18163761817159)) ;
#75627=CARTESIAN_POINT('Ctrl Pts',(3.1076875453681,-0.761999999459305,7.181791335163)) ;
#75628=CARTESIAN_POINT('Ctrl Pts',(3.14953687287001,-0.755540898601866,
7.13908377950685)) ;
#75629=CARTESIAN_POINT('Ctrl Pts',(3.14687049251069,-0.756336720063884,
7.14165588380709)) ;
#75630=CARTESIAN_POINT('Ctrl Pts',(3.14153773179204,-0.757950944893126,
7.1473932880007)) ;
#75631=CARTESIAN_POINT('Ctrl Pts',(3.13353859071408,-0.760010135143031,
7.15719931177908)) ;
#75632=CARTESIAN_POINT('Ctrl Pts',(3.12287306927679,-0.761680931514211,
7.16950958656739)) ;
#75633=CARTESIAN_POINT('Ctrl Pts',(3.11487392819882,-0.761961216508624,
7.17650146037765)) ;
#75634=CARTESIAN_POINT('Ctrl Pts',(3.10892329344283,-0.761997488316066,
7.1809061971102)) ;
#75635=CARTESIAN_POINT('Ctrl Pts',(3.10830541940668,-0.761999925297214,
7.18135219728602)) ;
#75636=CARTESIAN_POINT('Ctrl Pts',(3.1076875453681,-0.761999999459305,7.181791335163)) ;
#75637=CARTESIAN_POINT('Ctrl Pts',(3.14953687287001,-0.739012268865882,
7.11695436533127)) ;
#75638=CARTESIAN_POINT('Ctrl Pts',(3.14687049251069,-0.741696873122348,
7.12026196115736)) ;
#75639=CARTESIAN_POINT('Ctrl Pts',(3.14153773179204,-0.747258461773346,
7.12796089840492)) ;
#75640=CARTESIAN_POINT('Ctrl Pts',(3.13353859071408,-0.754625778477829,
7.14235903254706)) ;
#75641=CARTESIAN_POINT('Ctrl Pts',(3.12287306927679,-0.760786688692489,
7.16164067068996)) ;
#75642=CARTESIAN_POINT('Ctrl Pts',(3.11487392819881,-0.761845223870069,
7.17312655589753)) ;
#75643=CARTESIAN_POINT('Ctrl Pts',(3.10892329344283,-0.761991471478693,
7.18033789111251)) ;
#75644=CARTESIAN_POINT('Ctrl Pts',(3.10830541940737,-0.761999877690589,
7.18106682137182)) ;
#75645=CARTESIAN_POINT('Ctrl Pts',(3.1076875453681,-0.761999999459305,7.181791335163)) ;
#75646=CARTESIAN_POINT('Ctrl Pts',(3.14953687287001,-0.730523456132448,
7.10896775467099)) ;
#75647=CARTESIAN_POINT('Ctrl Pts',(3.14687049251069,-0.73410874308391,7.11234093439422)) ;
#75648=CARTESIAN_POINT('Ctrl Pts',(3.14153773179204,-0.741620611340461,
7.12039126652058)) ;
#75649=CARTESIAN_POINT('Ctrl Pts',(3.13353859071408,-0.751722671583157,
7.13626512379224)) ;
#75650=CARTESIAN_POINT('Ctrl Pts',(3.12287306927679,-0.760294668466002,
7.15825743733922)) ;
#75651=CARTESIAN_POINT('Ctrl Pts',(3.11487392819881,-0.761768784449911,
7.17170556214749)) ;
#75652=CARTESIAN_POINT('Ctrl Pts',(3.10892329344284,-0.761989456647343,
7.18009206761753)) ;
#75653=CARTESIAN_POINT('Ctrl Pts',(3.10830541940898,-0.761999857549363,
7.18094608564176)) ;
#75654=CARTESIAN_POINT('Ctrl Pts',(3.1076875453681,-0.761999999459305,7.181791335163)) ;
#75655=CARTESIAN_POINT('',(3.14953687287002,-0.730523456132445,7.10896775467099)) ;
#75656=CARTESIAN_POINT('',(3.1076875453681,-0.761999999459305,7.181791335163)) ;
#75657=CARTESIAN_POINT('Ctrl Pts',(3.14953687287001,-0.730523456132448,
7.10896775467099)) ;
#75658=CARTESIAN_POINT('Ctrl Pts',(3.14797942264904,-0.732617645708692,
7.11093805102685)) ;
#75659=CARTESIAN_POINT('Ctrl Pts',(3.1465061713264,-0.734653328663648,7.11301990160851)) ;
#75660=CARTESIAN_POINT('Ctrl Pts',(3.14387447911892,-0.738267803994675,
7.117061211881)) ;
#75661=CARTESIAN_POINT('Ctrl Pts',(3.1427034903174,-0.739869147575639,7.11898772024392)) ;
#75662=CARTESIAN_POINT('Ctrl Pts',(3.14003426783858,-0.743434587735941,
7.12365091140022)) ;
#75663=CARTESIAN_POINT('Ctrl Pts',(3.13853950336846,-0.745372263846278,
7.12646051120024)) ;
#75664=CARTESIAN_POINT('Ctrl Pts',(3.13653043645198,-0.74778851672796,7.13038311670479)) ;
#75665=CARTESIAN_POINT('Ctrl Pts',(3.13605624929057,-0.748345460226584,
7.13131929065347)) ;
#75666=CARTESIAN_POINT('Ctrl Pts',(3.13490033520594,-0.749663329733279,
7.13362022192598)) ;
#75667=CARTESIAN_POINT('Ctrl Pts',(3.13422097401358,-0.750405386417455,
7.13498790652006)) ;
#75668=CARTESIAN_POINT('Ctrl Pts',(3.13116298082121,-0.753565217081952,
7.14117490868328)) ;
#75669=CARTESIAN_POINT('Ctrl Pts',(3.12875074376133,-0.755569934781551,
7.14614171575595)) ;
#75670=CARTESIAN_POINT('Ctrl Pts',(3.1260549976317,-0.757288072049574,7.15142011655119)) ;
#75671=CARTESIAN_POINT('Ctrl Pts',(3.12579736320653,-0.757447091715282,
7.15192182249422)) ;
#75672=CARTESIAN_POINT('Ctrl Pts',(3.12252085545441,-0.759403938221167,
7.15826208088107)) ;
#75673=CARTESIAN_POINT('Ctrl Pts',(3.11946402361198,-0.760518781992785,
7.16374175989977)) ;
#75674=CARTESIAN_POINT('Ctrl Pts',(3.11411364459364,-0.761651866001623,
7.17250976794735)) ;
#75675=CARTESIAN_POINT('Ctrl Pts',(3.11182848381899,-0.761881721124906,
7.17599764811772)) ;
#75676=CARTESIAN_POINT('Ctrl Pts',(3.10892339826902,-0.761989452759989,
7.18009191988114)) ;
#75677=CARTESIAN_POINT('Ctrl Pts',(3.10830547182207,-0.761999857537325,
7.18094601394084)) ;
#75678=CARTESIAN_POINT('Ctrl Pts',(3.1076875453681,-0.761999999459305,7.181791335163)) ;
#75679=CARTESIAN_POINT('',(3.14953687287001,-0.762,7.1818)) ;
#75680=CARTESIAN_POINT('',(3.1076875453681,-0.761999999459305,7.181791335163)) ;
#75681=CARTESIAN_POINT('Origin',(3.14953687287001,-0.661999999999999,7.1818)) ;
#75682=CARTESIAN_POINT('Ctrl Pts',(3.17121692101567,-0.762,7.1818)) ;
#75683=CARTESIAN_POINT('Ctrl Pts',(3.16399023830045,-0.762,7.1818)) ;
#75684=CARTESIAN_POINT('Ctrl Pts',(3.15676355558524,-0.762,7.1818)) ;
#75685=CARTESIAN_POINT('Ctrl Pts',(3.14953687287003,-0.762,7.1818)) ;
#75686=CARTESIAN_POINT('Ctrl Pts',(3.17121692101567,-0.762,7.16049051462243)) ;
#75687=CARTESIAN_POINT('Ctrl Pts',(3.16399023830045,-0.761980537877959,
7.16173716654572)) ;
#75688=CARTESIAN_POINT('Ctrl Pts',(3.15676355558524,-0.762015837610647,
7.16371429760845)) ;
#75689=CARTESIAN_POINT('Ctrl Pts',(3.14953687287003,-0.762,7.16625960724294)) ;
#75690=CARTESIAN_POINT('Ctrl Pts',(3.17121692101567,-0.749661462765229,
7.12329552595192)) ;
#75691=CARTESIAN_POINT('Ctrl Pts',(3.16399023830045,-0.751152261593368,
7.12667195918439)) ;
#75692=CARTESIAN_POINT('Ctrl Pts',(3.15676355558524,-0.753383043736888,
7.13211431434399)) ;
#75693=CARTESIAN_POINT('Ctrl Pts',(3.14953687287003,-0.755540893518777,
7.1390837819811)) ;
#75694=CARTESIAN_POINT('Ctrl Pts',(3.17121692101567,-0.720057683295034,
7.09882570651471)) ;
#75695=CARTESIAN_POINT('Ctrl Pts',(3.16399023830045,-0.724623549182783,
7.10220324165009)) ;
#75696=CARTESIAN_POINT('Ctrl Pts',(3.15676355558524,-0.731748787702946,
7.10798226702609)) ;
#75697=CARTESIAN_POINT('Ctrl Pts',(3.14953687287003,-0.739012268865874,
7.11695436533126)) ;
#75698=CARTESIAN_POINT('Ctrl Pts',(3.17121692101567,-0.705680904617081,
7.09184457452808)) ;
#75699=CARTESIAN_POINT('Ctrl Pts',(3.16399023830045,-0.711535796534346,
7.09468761566807)) ;
#75700=CARTESIAN_POINT('Ctrl Pts',(3.15676355558524,-0.720806263628127,
7.09982543575315)) ;
#75701=CARTESIAN_POINT('Ctrl Pts',(3.14953687287002,-0.730523456132438,
7.10896775467099)) ;
#75702=CARTESIAN_POINT('',(3.17121692101567,-0.762,7.1818)) ;
#75703=CARTESIAN_POINT('',(3.14953687287003,-0.762,7.1818)) ;
#75704=CARTESIAN_POINT('',(3.17121692101567,-0.70568090461708,7.09184457452808)) ;
#75705=CARTESIAN_POINT('Origin',(3.17121692101567,-0.662000000000001,7.1818)) ;
#75706=CARTESIAN_POINT('Ctrl Pts',(3.17121692101567,-0.705680904617081,
7.09184457452808)) ;
#75707=CARTESIAN_POINT('Ctrl Pts',(3.16399023830045,-0.711535796534346,
7.09468761566807)) ;
#75708=CARTESIAN_POINT('Ctrl Pts',(3.15676355558524,-0.720806263628127,
7.09982543575315)) ;
#75709=CARTESIAN_POINT('Ctrl Pts',(3.14953687287002,-0.730523456132438,
7.10896775467099)) ;
#75710=CARTESIAN_POINT('Ctrl Pts',(3.20512388881546,-0.762,7.1818)) ;
#75711=CARTESIAN_POINT('Ctrl Pts',(3.2047202344369,-0.762,7.1818)) ;
#75712=CARTESIAN_POINT('Ctrl Pts',(3.20391292567976,-0.762,7.1818)) ;
#75713=CARTESIAN_POINT('Ctrl Pts',(3.20270196254405,-0.762,7.1818)) ;
#75714=CARTESIAN_POINT('Ctrl Pts',(3.20149099940834,-0.762,7.1818)) ;
#75715=CARTESIAN_POINT('Ctrl Pts',(3.19745445562265,-0.762,7.1818)) ;
#75716=CARTESIAN_POINT('Ctrl Pts',(3.18736309615843,-0.762,7.1818)) ;
#75717=CARTESIAN_POINT('Ctrl Pts',(3.17767539107277,-0.762,7.1818)) ;
#75718=CARTESIAN_POINT('Ctrl Pts',(3.17121692101566,-0.762,7.1818)) ;
#75719=CARTESIAN_POINT('Ctrl Pts',(3.20512388881546,-0.762,7.15188006996578)) ;
#75720=CARTESIAN_POINT('Ctrl Pts',(3.2047202344369,-0.761992330181026,7.1520702301264)) ;
#75721=CARTESIAN_POINT('Ctrl Pts',(3.20391292567976,-0.76197980992607,7.15243005278884)) ;
#75722=CARTESIAN_POINT('Ctrl Pts',(3.20270196254405,-0.761963555547577,
7.15292464422255)) ;
#75723=CARTESIAN_POINT('Ctrl Pts',(3.20149099940834,-0.761947562028464,
7.15338566691011)) ;
#75724=CARTESIAN_POINT('Ctrl Pts',(3.19745445562265,-0.76191470846392,7.15481366906456)) ;
#75725=CARTESIAN_POINT('Ctrl Pts',(3.18736309615843,-0.761861071074269,
7.15758629528363)) ;
#75726=CARTESIAN_POINT('Ctrl Pts',(3.17767539107277,-0.76201739325461,7.15937638460794)) ;
#75727=CARTESIAN_POINT('Ctrl Pts',(3.17121692101566,-0.762,7.16049051462243)) ;
#75728=CARTESIAN_POINT('Ctrl Pts',(3.20512388881546,-0.736911811379185,
7.100050335275)) ;
#75729=CARTESIAN_POINT('Ctrl Pts',(3.2047202344369,-0.737245219347507,7.10054319817604)) ;
#75730=CARTESIAN_POINT('Ctrl Pts',(3.20391292567976,-0.737869883520251,
7.10148033026225)) ;
#75731=CARTESIAN_POINT('Ctrl Pts',(3.20270196254405,-0.738711770607015,
7.10277348618571)) ;
#75732=CARTESIAN_POINT('Ctrl Pts',(3.20149099940834,-0.73948195346955,7.10398042484261)) ;
#75733=CARTESIAN_POINT('Ctrl Pts',(3.19745445562265,-0.74182919721765,7.10775251408813)) ;
#75734=CARTESIAN_POINT('Ctrl Pts',(3.18736309615843,-0.746011102788114,
7.11515718689346)) ;
#75735=CARTESIAN_POINT('Ctrl Pts',(3.17767539107277,-0.748329114460406,
7.12027803292724)) ;
#75736=CARTESIAN_POINT('Ctrl Pts',(3.17121692101566,-0.749661438013567,
7.12329554369824)) ;
#75737=CARTESIAN_POINT('Ctrl Pts',(3.20512388881546,-0.684439947525498,
7.08179999999996)) ;
#75738=CARTESIAN_POINT('Ctrl Pts',(3.20472023443689,-0.685279518511759,
7.08202134573632)) ;
#75739=CARTESIAN_POINT('Ctrl Pts',(3.20391292567976,-0.686865903002592,
7.08246093200817)) ;
#75740=CARTESIAN_POINT('Ctrl Pts',(3.20270196254405,-0.689032722166202,
7.08311409360665)) ;
#75741=CARTESIAN_POINT('Ctrl Pts',(3.20149099940834,-0.691037008739266,
7.08376272980254)) ;
#75742=CARTESIAN_POINT('Ctrl Pts',(3.19745445562265,-0.697229783074603,
7.08590527875505)) ;
#75743=CARTESIAN_POINT('Ctrl Pts',(3.18736309615843,-0.708839952636616,
7.09112838260725)) ;
#75744=CARTESIAN_POINT('Ctrl Pts',(3.17767539107277,-0.715977179240427,
7.09580721097557)) ;
#75745=CARTESIAN_POINT('Ctrl Pts',(3.17121692101566,-0.720057683295033,
7.09882570651471)) ;
#75746=CARTESIAN_POINT('Ctrl Pts',(3.20512388881546,-0.661999999999833,
7.0818)) ;
#75747=CARTESIAN_POINT('Ctrl Pts',(3.20472023443689,-0.662977161851482,
7.0818)) ;
#75748=CARTESIAN_POINT('Ctrl Pts',(3.20391292567976,-0.664831438935667,
7.0818281326209)) ;
#75749=CARTESIAN_POINT('Ctrl Pts',(3.20270196254405,-0.667381960953569,
7.08193509059619)) ;
#75750=CARTESIAN_POINT('Ctrl Pts',(3.20149099940834,-0.669755131272071,
7.08209149598161)) ;
#75751=CARTESIAN_POINT('Ctrl Pts',(3.19745445562265,-0.677136096351082,
7.08275930201879)) ;
#75752=CARTESIAN_POINT('Ctrl Pts',(3.18736309615843,-0.691331994006369,
7.08558723772615)) ;
#75753=CARTESIAN_POINT('Ctrl Pts',(3.17767539107277,-0.700448400904743,
7.08930375506814)) ;
#75754=CARTESIAN_POINT('Ctrl Pts',(3.17121692101566,-0.70568090461708,7.09184457452808)) ;
#75755=CARTESIAN_POINT('',(3.17121692101566,-0.762,7.1818)) ;
#75756=CARTESIAN_POINT('Ctrl Pts',(3.20512388881546,-0.661999999999834,
7.0818)) ;
#75757=CARTESIAN_POINT('Ctrl Pts',(3.20472023443689,-0.662977161851484,
7.0818)) ;
#75758=CARTESIAN_POINT('Ctrl Pts',(3.20431658005833,-0.6639042979399,7.08181418112561)) ;
#75759=CARTESIAN_POINT('Ctrl Pts',(3.2035092713012,-0.665681610657573,7.08186384002979)) ;
#75760=CARTESIAN_POINT('Ctrl Pts',(3.20310561692262,-0.666531791312273,
7.08189935834228)) ;
#75761=CARTESIAN_POINT('Ctrl Pts',(3.20229830816548,-0.668173012083287,
7.08198732917139)) ;
#75762=CARTESIAN_POINT('Ctrl Pts',(3.20189465378691,-0.66896403985732,7.0820398363167)) ;
#75763=CARTESIAN_POINT('Ctrl Pts',(3.20108734502978,-0.670493217907201,
7.08215837537036)) ;
#75764=CARTESIAN_POINT('Ctrl Pts',(3.20068369065121,-0.671231386902573,
7.08222438102225)) ;
#75765=CARTESIAN_POINT('Ctrl Pts',(3.1984790488068,-0.67515936222752,7.08261718651246)) ;
#75766=CARTESIAN_POINT('Ctrl Pts',(3.19667806134095,-0.677991390732913,
7.08305203429456)) ;
#75767=CARTESIAN_POINT('Ctrl Pts',(3.19344882631238,-0.682614461197469,
7.08392572248013)) ;
#75768=CARTESIAN_POINT('Ctrl Pts',(3.19202057874967,-0.684499933880204,
7.08434667817419)) ;
#75769=CARTESIAN_POINT('Ctrl Pts',(3.18778558324308,-0.689801348801288,
7.08567402178887)) ;
#75770=CARTESIAN_POINT('Ctrl Pts',(3.1849788352992,-0.692934482334868,7.0866568114692)) ;
#75771=CARTESIAN_POINT('Ctrl Pts',(3.17911128623295,-0.698892281462462,
7.08879536039987)) ;
#75772=CARTESIAN_POINT('Ctrl Pts',(3.17605048511059,-0.701664122709342,
7.08995925874846)) ;
#75773=CARTESIAN_POINT('Ctrl Pts',(3.17239876299736,-0.704716249384931,
7.09138087098935)) ;
#75774=CARTESIAN_POINT('Ctrl Pts',(3.17180784200651,-0.70520215403823,7.09161210096398)) ;
#75775=CARTESIAN_POINT('Ctrl Pts',(3.17121692101566,-0.70568090461708,7.09184457452808)) ;
#75776=CARTESIAN_POINT('Origin',(3.21546217517793,-0.861999999999999,0.)) ;
#75777=CARTESIAN_POINT('',(3.21546217517793,-0.762,7.36730649953872)) ;
#75778=CARTESIAN_POINT('',(3.21546217517793,-0.762,0.)) ;
#75779=CARTESIAN_POINT('',(3.31205160669424,-0.887893661760288,7.36730649953872)) ;
#75780=CARTESIAN_POINT('Origin',(3.21546217517793,-0.862,7.36730649953872)) ;
#75781=CARTESIAN_POINT('',(3.31205160669424,-0.887893661760288,0.)) ;
#75782=CARTESIAN_POINT('Origin',(-9.525,-0.762,8.72161438184689)) ;
#75783=CARTESIAN_POINT('',(0.598228027472807,-0.762,7.1818)) ;
#75784=CARTESIAN_POINT('',(0.,-0.762,7.1818)) ;
#75785=CARTESIAN_POINT('',(0.731723284002018,-0.762,8.59150875795967)) ;
#75786=CARTESIAN_POINT('',(0.703226309181215,-0.762,8.29058094955136)) ;
#75787=CARTESIAN_POINT('',(3.07434158440252,-0.762,7.64111756647598)) ;
#75788=CARTESIAN_POINT('Origin',(0.,-0.762,3.42553041237115)) ;
#75789=CARTESIAN_POINT('Origin',(2.94523160007116,-0.762,7.40850915739415)) ;
#75790=CARTESIAN_POINT('Ctrl Pts',(0.233145498782351,-1.13595304047784,
6.71957)) ;
#75791=CARTESIAN_POINT('Ctrl Pts',(0.282596494255523,-1.15562586963554,
6.71957)) ;
#75792=CARTESIAN_POINT('Ctrl Pts',(0.32845503035145,-1.17386952959435,6.7615916062195)) ;
#75793=CARTESIAN_POINT('Ctrl Pts',(0.332764968591525,-1.17558412963154,
6.81085442572523)) ;
#75794=CARTESIAN_POINT('Ctrl Pts',(0.233145498782351,-1.13595304047784,
6.71957)) ;
#75795=CARTESIAN_POINT('Ctrl Pts',(0.283851238553257,-1.14931784407503,
6.71957)) ;
#75796=CARTESIAN_POINT('Ctrl Pts',(0.328698029275161,-1.16142573132119,
6.76307285057327)) ;
#75797=CARTESIAN_POINT('Ctrl Pts',(0.332784667850019,-1.16254657695484,
6.81107958928014)) ;
#75798=CARTESIAN_POINT('Ctrl Pts',(0.233145498782351,-1.13595304047784,
6.71957)) ;
#75799=CARTESIAN_POINT('Ctrl Pts',(0.28510598285099,-1.14300981851451,6.71957)) ;
#75800=CARTESIAN_POINT('Ctrl Pts',(0.331172502747825,-1.14898571310985,
6.76307285057327)) ;
#75801=CARTESIAN_POINT('Ctrl Pts',(0.335376993538143,-1.14951407564648,
6.81107958928014)) ;
#75802=CARTESIAN_POINT('Ctrl Pts',(0.233145498782351,-1.13595304047784,
6.71957)) ;
#75803=CARTESIAN_POINT('Ctrl Pts',(0.286360727148723,-1.136701792954,6.71957)) ;
#75804=CARTESIAN_POINT('Ctrl Pts',(0.33571003645062,-1.13739615091638,6.7615916062195)) ;
#75805=CARTESIAN_POINT('Ctrl Pts',(0.340348049204377,-1.13746140899458,
6.81085442572523)) ;
#75806=CARTESIAN_POINT('',(0.332764968591525,-1.17558412963154,6.81085442572523)) ;
#75807=CARTESIAN_POINT('',(0.340348049204377,-1.13746140899458,6.81085442572523)) ;
#75808=CARTESIAN_POINT('Origin',(0.4323844384007,-1.17558412963154,6.80213885145047)) ;
#75809=CARTESIAN_POINT('',(0.233145498782351,-1.13595304047784,6.71957)) ;
#75810=CARTESIAN_POINT('Origin',(0.233145498782351,-1.13595304047784,6.81957)) ;
#75811=CARTESIAN_POINT('Origin',(0.233145498782351,-1.13595304047784,6.81957)) ;
#75812=CARTESIAN_POINT('Origin',(0.607374264964752,-1.21039177030075,8.80228172152873)) ;
#75813=CARTESIAN_POINT('',(0.484912864018598,-1.20584822770277,8.54991282821175)) ;
#75814=CARTESIAN_POINT('',(0.507754795155577,-1.21039177030075,8.81099729580349)) ;
#75815=CARTESIAN_POINT('',(0.49249594463145,-1.16772550706581,8.54991282821175)) ;
#75816=CARTESIAN_POINT('Origin',(0.584532333827773,-1.20584822770277,8.54119725393698)) ;
#75817=CARTESIAN_POINT('',(0.515337875768429,-1.17226904966379,8.81099729580349)) ;
#75818=CARTESIAN_POINT('Origin',(0.584532333827771,-1.20584822770278,8.54119725393698)) ;
#75819=CARTESIAN_POINT('',(0.595585710062509,-1.22865054909962,8.63793337445424)) ;
#75820=CARTESIAN_POINT('Origin',(0.584532333827771,-1.20584822770278,8.54119725393698)) ;
#75821=CARTESIAN_POINT('Origin',(0.584532333827771,-1.20584822770278,8.54119725393698)) ;
#75822=CARTESIAN_POINT('Origin',(0.135929041739323,-4.80294522256305E-16,
3.41363816217501)) ;
#75823=CARTESIAN_POINT('',(0.459053285493802,-2.10247651427315,8.254336493146)) ;
#75824=CARTESIAN_POINT('Origin',(0.0363095719301483,-1.2829700173246E-16,
3.42235373644978)) ;
#75825=CARTESIAN_POINT('',(0.563402527094027,-2.29049913469776,8.27007790985519)) ;
#75826=CARTESIAN_POINT('Ctrl Pts',(0.563402527094027,-2.29049913469776,
8.27007790985519)) ;
#75827=CARTESIAN_POINT('Ctrl Pts',(0.563094639607243,-2.29005173251521,
8.27032524748595)) ;
#75828=CARTESIAN_POINT('Ctrl Pts',(0.562783526294646,-2.28959637341817,
8.27056977508129)) ;
#75829=CARTESIAN_POINT('Ctrl Pts',(0.518363588386159,-2.22542344757913,
8.30657277835385)) ;
#75830=CARTESIAN_POINT('Ctrl Pts',(0.463831241820141,-2.12754376098305,
8.30894878385637)) ;
#75831=CARTESIAN_POINT('Ctrl Pts',(0.459053285493802,-2.10247651427315,
8.254336493146)) ;
#75832=CARTESIAN_POINT('Origin',(0.138499429641961,-4.89376784692015E-16,
3.41341328237267)) ;
#75833=CARTESIAN_POINT('Origin',(0.507999999999992,2.45141482417775E-15,
8.8138)) ;
#75834=CARTESIAN_POINT('',(0.33276496859165,-1.72771014821123,6.81085442572668)) ;
#75835=CARTESIAN_POINT('',(0.332764968591529,9.47397622833151E-16,6.81085442572523)) ;
#75836=CARTESIAN_POINT('',(0.456330681975393,-2.09161206695506,8.2232169925309)) ;
#75837=CARTESIAN_POINT('Ctrl Pts',(0.456330681975393,-2.09161206695506,
8.2232169925309)) ;
#75838=CARTESIAN_POINT('Ctrl Pts',(0.415134631297314,-1.97064606309627,
7.75234397861325)) ;
#75839=CARTESIAN_POINT('Ctrl Pts',(0.373944470214011,-1.84941569039825,
7.28153828307192)) ;
#75840=CARTESIAN_POINT('Ctrl Pts',(0.332764968591776,-1.72771014821123,
6.81085442572812)) ;
#75841=CARTESIAN_POINT('Origin',(0.453427128991176,-2.23537208573896,8.19002923005734)) ;
#75842=CARTESIAN_POINT('Origin',(0.233145498782355,1.299395143357E-15,6.81957)) ;
#75843=CARTESIAN_POINT('',(0.233145498782349,-1.72771014821048,6.71957)) ;
#75844=CARTESIAN_POINT('',(0.233145498782355,1.299395143357E-15,6.71957)) ;
#75845=CARTESIAN_POINT('Origin',(0.233145498782349,-1.72771014821048,6.81957)) ;
#75846=CARTESIAN_POINT('Ctrl Pts',(0.459053285493802,-2.10247651427315,
8.254336493146)) ;
#75847=CARTESIAN_POINT('Ctrl Pts',(0.463831241820141,-2.12754376098305,
8.30894878385637)) ;
#75848=CARTESIAN_POINT('Ctrl Pts',(0.518363588386159,-2.22542344757913,
8.30657277835385)) ;
#75849=CARTESIAN_POINT('Ctrl Pts',(0.562783526294646,-2.28959637341817,
8.27056977508129)) ;
#75850=CARTESIAN_POINT('Ctrl Pts',(0.563094639607243,-2.29005173251521,
8.27032524748595)) ;
#75851=CARTESIAN_POINT('Ctrl Pts',(0.563402527094027,-2.29049913469776,
8.27007790985519)) ;
#75852=CARTESIAN_POINT('Ctrl Pts',(0.458120821927424,-2.12650219752326,
8.24367838581188)) ;
#75853=CARTESIAN_POINT('Ctrl Pts',(0.461688966624489,-2.14596370314819,
8.28635124743027)) ;
#75854=CARTESIAN_POINT('Ctrl Pts',(0.509788465353625,-2.2323671087866,8.30425543138927)) ;
#75855=CARTESIAN_POINT('Ctrl Pts',(0.562697273737575,-2.28970714738724,
8.27052649306718)) ;
#75856=CARTESIAN_POINT('Ctrl Pts',(0.563047685007142,-2.29010501322995,
8.27030551703833)) ;
#75857=CARTESIAN_POINT('Ctrl Pts',(0.563402527094027,-2.29049913469776,
8.27007790985519)) ;
#75858=CARTESIAN_POINT('Ctrl Pts',(0.437455203934562,-2.16829359261983,
8.22680527958952)) ;
#75859=CARTESIAN_POINT('Ctrl Pts',(0.440261201157157,-2.18279718179887,
8.25963785655292)) ;
#75860=CARTESIAN_POINT('Ctrl Pts',(0.497044842085689,-2.24468622633794,
8.30004865938944)) ;
#75861=CARTESIAN_POINT('Ctrl Pts',(0.562535491219473,-2.28990061909155,
8.27045236517641)) ;
#75862=CARTESIAN_POINT('Ctrl Pts',(0.562965514456966,-2.29019825448075,
8.27027098875499)) ;
#75863=CARTESIAN_POINT('Ctrl Pts',(0.563402527094027,-2.29049913469776,
8.27007790985519)) ;
#75864=CARTESIAN_POINT('Ctrl Pts',(0.394198333198201,-2.18878000295551,
8.22143216354669)) ;
#75865=CARTESIAN_POINT('Ctrl Pts',(0.398660306869003,-2.20910331550188,
8.2673898581129)) ;
#75866=CARTESIAN_POINT('Ctrl Pts',(0.486848771498274,-2.25930922281487,
8.29418858273012)) ;
#75867=CARTESIAN_POINT('Ctrl Pts',(0.562361505034938,-2.29008362295378,
8.27038779969869)) ;
#75868=CARTESIAN_POINT('Ctrl Pts',(0.56288334390679,-2.29029149573155,8.27023646047164)) ;
#75869=CARTESIAN_POINT('Ctrl Pts',(0.563402527094027,-2.29049913469776,
8.27007790985519)) ;
#75870=CARTESIAN_POINT('Ctrl Pts',(0.374769931517255,-2.19218377594761,
8.22161041260296)) ;
#75871=CARTESIAN_POINT('Ctrl Pts',(0.38020887226914,-2.21659247451535,8.27645980857715)) ;
#75872=CARTESIAN_POINT('Ctrl Pts',(0.482581338415516,-2.266212758132,8.29146057868529)) ;
#75873=CARTESIAN_POINT('Ctrl Pts',(0.562286478119671,-2.29015910661772,
8.27036146369334)) ;
#75874=CARTESIAN_POINT('Ctrl Pts',(0.562848127956715,-2.2903314562676,8.27022166263593)) ;
#75875=CARTESIAN_POINT('Ctrl Pts',(0.563402527094027,-2.29049913469776,
8.27007790985519)) ;
#75876=CARTESIAN_POINT('',(0.374769931517255,-2.19218377594761,8.22161041260296)) ;
#75877=CARTESIAN_POINT('Ctrl Pts',(0.374769931517255,-2.19218377594761,
8.22161041260296)) ;
#75878=CARTESIAN_POINT('Ctrl Pts',(0.38020887226914,-2.21659247451535,8.27645980857715)) ;
#75879=CARTESIAN_POINT('Ctrl Pts',(0.482581338415516,-2.266212758132,8.29146057868529)) ;
#75880=CARTESIAN_POINT('Ctrl Pts',(0.562286478119671,-2.29015910661772,
8.27036146369334)) ;
#75881=CARTESIAN_POINT('Ctrl Pts',(0.562848127956715,-2.2903314562676,8.27022166263593)) ;
#75882=CARTESIAN_POINT('Ctrl Pts',(0.563402527094027,-2.29049913469776,
8.27007790985519)) ;
#75883=CARTESIAN_POINT('Origin',(0.359433815684627,-2.10247651427315,8.26305206742076)) ;
#75884=CARTESIAN_POINT('Ctrl Pts',(0.374769931517254,-2.19218377594761,
8.22161041260296)) ;
#75885=CARTESIAN_POINT('Ctrl Pts',(0.374271909287347,-2.18994876824218,
8.21658807098568)) ;
#75886=CARTESIAN_POINT('Ctrl Pts',(0.373662616506299,-2.18815607354194,
8.21137680913461)) ;
#75887=CARTESIAN_POINT('Ctrl Pts',(0.37295000513728,-2.18682986267501,8.20605066229541)) ;
#75888=CARTESIAN_POINT('Ctrl Pts',(0.400674467091849,-2.18764541195813,
8.2213727471946)) ;
#75889=CARTESIAN_POINT('Ctrl Pts',(0.400168655131402,-2.18531329532944,
8.21609868976098)) ;
#75890=CARTESIAN_POINT('Ctrl Pts',(0.399569847844621,-2.18345309008412,
8.21059040433855)) ;
#75891=CARTESIAN_POINT('Ctrl Pts',(0.398892978130845,-2.18211755991818,
8.20499152409472)) ;
#75892=CARTESIAN_POINT('Ctrl Pts',(0.442802799136141,-2.16260269917149,
8.22888130401443)) ;
#75893=CARTESIAN_POINT('Ctrl Pts',(0.442204751807135,-2.15964157072195,
8.22218874465404)) ;
#75894=CARTESIAN_POINT('Ctrl Pts',(0.441564708190408,-2.15729533880903,
8.21524061522765)) ;
#75895=CARTESIAN_POINT('Ctrl Pts',(0.440889933449587,-2.15559078214374,
8.20813192407365)) ;
#75896=CARTESIAN_POINT('Ctrl Pts',(0.458353937819018,-2.12049577671073,
8.2463429126454)) ;
#75897=CARTESIAN_POINT('Ctrl Pts',(0.457563066882837,-2.11646373803811,
8.23730217497138)) ;
#75898=CARTESIAN_POINT('Ctrl Pts',(0.456741824116299,-2.11321321015441,
8.22792080639222)) ;
#75899=CARTESIAN_POINT('Ctrl Pts',(0.455903016748525,-2.11078568946555,
8.21832875661974)) ;
#75900=CARTESIAN_POINT('Ctrl Pts',(0.459053285493801,-2.10247651427315,
8.25433649314599)) ;
#75901=CARTESIAN_POINT('Ctrl Pts',(0.458174489582068,-2.09798645436108,
8.24429180991142)) ;
#75902=CARTESIAN_POINT('Ctrl Pts',(0.4572626369128,-2.09434861239325,8.23386928620929)) ;
#75903=CARTESIAN_POINT('Ctrl Pts',(0.456330681975393,-2.09161206695506,
8.2232169925309)) ;
#75904=CARTESIAN_POINT('',(0.37295000513728,-2.18682986267501,8.20605066229541)) ;
#75905=CARTESIAN_POINT('Origin',(0.356711212166218,-2.09161206695506,8.23193256680567)) ;
#75906=CARTESIAN_POINT('Origin',(0.356848236200114,-2.26130448598471,8.18949965412146)) ;
#75907=CARTESIAN_POINT('Ctrl Pts',(0.332575554792171,-1.7271503343366,6.80868941609177)) ;
#75908=CARTESIAN_POINT('Ctrl Pts',(0.373881299532484,-1.84923054559942,
7.28081623887807)) ;
#75909=CARTESIAN_POINT('Ctrl Pts',(0.415197776566303,-1.97083234352155,
7.75306573234047)) ;
#75910=CARTESIAN_POINT('Ctrl Pts',(0.456520172012611,-2.09216847395032,
8.22538287356716)) ;
#75911=CARTESIAN_POINT('Ctrl Pts',(0.331987953017615,-1.75332513240999,
6.80197267219288)) ;
#75912=CARTESIAN_POINT('Ctrl Pts',(0.373292933712475,-1.87515504373648,
7.27418379019747)) ;
#75913=CARTESIAN_POINT('Ctrl Pts',(0.414627967367415,-1.99656668249708,
7.74649382983075)) ;
#75914=CARTESIAN_POINT('Ctrl Pts',(0.455949949949699,-2.11773252293444,
8.21886547566713)) ;
#75915=CARTESIAN_POINT('Ctrl Pts',(0.310793595327402,-1.79883340137849,
6.79205963153165)) ;
#75916=CARTESIAN_POINT('Ctrl Pts',(0.352528666728234,-1.92025230099924,
7.26437312176635)) ;
#75917=CARTESIAN_POINT('Ctrl Pts',(0.394171753364285,-2.04132212887046,
7.73676749348942)) ;
#75918=CARTESIAN_POINT('Ctrl Pts',(0.435777022314021,-2.16220666599519,
8.20920517618971)) ;
#75919=CARTESIAN_POINT('Ctrl Pts',(0.265876600167924,-1.81991774820283,
6.79053747107829)) ;
#75920=CARTESIAN_POINT('Ctrl Pts',(0.308308238839946,-1.94157711521186,
7.26274358539733)) ;
#75921=CARTESIAN_POINT('Ctrl Pts',(0.350504776847073,-2.06283206919883,
7.73505295857787)) ;
#75922=CARTESIAN_POINT('Ctrl Pts',(0.392580797820033,-2.18386034844095,
8.20742162540622)) ;
#75923=CARTESIAN_POINT('Ctrl Pts',(0.245836003043331,-1.82288076242879,
6.79152463448741)) ;
#75924=CARTESIAN_POINT('Ctrl Pts',(0.28849419488381,-1.94477897268376,7.26365133260709)) ;
#75925=CARTESIAN_POINT('Ctrl Pts',(0.330878372341273,-2.06621032168341,
7.73590073192183)) ;
#75926=CARTESIAN_POINT('Ctrl Pts',(0.373113112727488,-2.18739110458305,
8.20821779213733)) ;
#75927=CARTESIAN_POINT('',(0.246063080839075,-1.82343508275148,6.79368809549119)) ;
#75928=CARTESIAN_POINT('Origin',(0.233145498782601,-1.72771014821123,6.81957000000289)) ;
#75929=CARTESIAN_POINT('Ctrl Pts',(0.246063080839076,-1.82343508275148,
6.79368809549264)) ;
#75930=CARTESIAN_POINT('Ctrl Pts',(0.263106778000548,-1.87213905946258,
6.98232754964158)) ;
#75931=CARTESIAN_POINT('Ctrl Pts',(0.280128754030394,-1.92076304376671,
7.17098657374969)) ;
#75932=CARTESIAN_POINT('Ctrl Pts',(0.314082706993329,-2.0179348788448,7.54848217854548)) ;
#75933=CARTESIAN_POINT('Ctrl Pts',(0.331014637616594,-2.06648276270083,
7.73731878400216)) ;
#75934=CARTESIAN_POINT('Ctrl Pts',(0.356264911138867,-2.13894444267106,
8.01945926643602)) ;
#75935=CARTESIAN_POINT('Ctrl Pts',(0.364607313003592,-2.16289285302724,
8.11275364297402)) ;
#75936=CARTESIAN_POINT('Ctrl Pts',(0.372950005137279,-2.18682986267501,
8.20605066229541)) ;
#75937=CARTESIAN_POINT('Origin',(0.233145498782349,-1.72771014821048,6.81957)) ;
#75938=CARTESIAN_POINT('Origin',(0.233145498782349,-1.72771014821048,6.81957)) ;
#75939=CARTESIAN_POINT('Origin',(-0.233145498782373,-1.72771014821048,6.81957)) ;
#75940=CARTESIAN_POINT('',(-0.332764968591548,-1.72771014821048,6.81085442572523)) ;
#75941=CARTESIAN_POINT('',(-0.246063080838839,-1.82343508275073,6.79368809548975)) ;
#75942=CARTESIAN_POINT('Origin',(-0.233145498782373,-1.72771014821048,6.81957)) ;
#75943=CARTESIAN_POINT('',(-0.233145498782373,-1.72771014821048,6.71957)) ;
#75944=CARTESIAN_POINT('Origin',(-0.233145498782373,-1.72771014821048,6.81957)) ;
#75945=CARTESIAN_POINT('Origin',(-0.233145498782373,-1.72771014821048,6.81957)) ;
#75946=CARTESIAN_POINT('Ctrl Pts',(-0.245836001151034,-1.8228807580253,
6.79152461794378)) ;
#75947=CARTESIAN_POINT('Ctrl Pts',(-0.288494198953793,-1.9447789779916,
7.26365132481474)) ;
#75948=CARTESIAN_POINT('Ctrl Pts',(-0.330878369254937,-2.06621031878769,
7.73590073893123)) ;
#75949=CARTESIAN_POINT('Ctrl Pts',(-0.373113113874326,-2.18739110879812,
8.20821780878249)) ;
#75950=CARTESIAN_POINT('Ctrl Pts',(-0.272553537556922,-1.8189308194855,
6.79020849164427)) ;
#75951=CARTESIAN_POINT('Ctrl Pts',(-0.314905492765294,-1.94050480823612,
7.26244303990738)) ;
#75952=CARTESIAN_POINT('Ctrl Pts',(-0.357046431870861,-2.06171037042116,
7.7347692407966)) ;
#75953=CARTESIAN_POINT('Ctrl Pts',(-0.399066819643649,-2.18268421515255,
8.20715633330629)) ;
#75954=CARTESIAN_POINT('Ctrl Pts',(-0.316376716060902,-1.79267106091927,
6.79316458204583)) ;
#75955=CARTESIAN_POINT('Ctrl Pts',(-0.357994391162648,-1.91413489045563,
7.26547214219855)) ;
#75956=CARTESIAN_POINT('Ctrl Pts',(-0.399548971339301,-2.03523918647868,
7.73786227286182)) ;
#75957=CARTESIAN_POINT('Ctrl Pts',(-0.44107705424413,-2.15615536078617,
8.21029605360252)) ;
#75958=CARTESIAN_POINT('Ctrl Pts',(-0.332134835417109,-1.74678141058242,
6.80365184795983)) ;
#75959=CARTESIAN_POINT('Ctrl Pts',(-0.373443640775722,-1.86867784543941,
7.27584050139373)) ;
#75960=CARTESIAN_POINT('Ctrl Pts',(-0.414768073581027,-1.99013064875018,
7.74813767788189)) ;
#75961=CARTESIAN_POINT('Ctrl Pts',(-0.456092517669814,-2.11134152617596,
8.22049483777629)) ;
#75962=CARTESIAN_POINT('Ctrl Pts',(-0.332575553339162,-1.72715033004212,
6.80868939948353)) ;
#75963=CARTESIAN_POINT('Ctrl Pts',(-0.373881299047604,-1.84923054417823,
7.28081623333557)) ;
#75964=CARTESIAN_POINT('Ctrl Pts',(-0.415197777050109,-1.97083234494871,
7.75306573787008)) ;
#75965=CARTESIAN_POINT('Ctrl Pts',(-0.456520173465327,-2.09216847821589,
8.22538289017144)) ;
#75966=CARTESIAN_POINT('',(-0.456330681975422,-2.09161206695506,8.2232169925309)) ;
#75967=CARTESIAN_POINT('',(-0.37295000513731,-2.186829862675,8.20605066229541)) ;
#75968=CARTESIAN_POINT('Origin',(-0.356711212166247,-2.09161206695506,8.23193256680567)) ;
#75969=CARTESIAN_POINT('Ctrl Pts',(-0.37295000513731,-2.186829862675,8.20605066229541)) ;
#75970=CARTESIAN_POINT('Ctrl Pts',(-0.356060675112372,-2.13837067836461,
8.01717588130003)) ;
#75971=CARTESIAN_POINT('Ctrl Pts',(-0.33916937336606,-2.08986565451448,
7.82831193143985)) ;
#75972=CARTESIAN_POINT('Ctrl Pts',(-0.305304200525196,-1.99279235652918,
7.45075381522733)) ;
#75973=CARTESIAN_POINT('Ctrl Pts',(-0.288330373027804,-1.94422406244455,
7.26205962744251)) ;
#75974=CARTESIAN_POINT('Ctrl Pts',(-0.262904814260684,-1.87155513860969,
6.98014705352749)) ;
#75975=CARTESIAN_POINT('Ctrl Pts',(-0.254486208871171,-1.84750496780177,
6.88691518461202)) ;
#75976=CARTESIAN_POINT('Ctrl Pts',(-0.246063080838839,-1.82343508275073,
6.79368809548975)) ;
#75977=CARTESIAN_POINT('Ctrl Pts',(-0.332764968590868,-1.72771014820847,
6.81085442571747)) ;
#75978=CARTESIAN_POINT('Ctrl Pts',(-0.373944470213416,-1.84941569039642,
7.28153828306482)) ;
#75979=CARTESIAN_POINT('Ctrl Pts',(-0.41513463129703,-1.97064606309535,
7.75234397860969)) ;
#75980=CARTESIAN_POINT('Ctrl Pts',(-0.456330681975422,-2.09161206695506,
8.2232169925309)) ;
#75981=CARTESIAN_POINT('Ctrl Pts',(-0.37295000513731,-2.186829862675,8.20605066229541)) ;
#75982=CARTESIAN_POINT('Ctrl Pts',(-0.373662616506329,-2.18815607354194,
8.21137680913461)) ;
#75983=CARTESIAN_POINT('Ctrl Pts',(-0.374271909287377,-2.18994876824218,
8.21658807098568)) ;
#75984=CARTESIAN_POINT('Ctrl Pts',(-0.374769931517285,-2.19218377594761,
8.22161041260296)) ;
#75985=CARTESIAN_POINT('Ctrl Pts',(-0.398892978130875,-2.18211755991818,
8.20499152409472)) ;
#75986=CARTESIAN_POINT('Ctrl Pts',(-0.399569847844652,-2.18345309008412,
8.21059040433855)) ;
#75987=CARTESIAN_POINT('Ctrl Pts',(-0.400168655131432,-2.18531329532943,
8.21609868976098)) ;
#75988=CARTESIAN_POINT('Ctrl Pts',(-0.400674467091879,-2.18764541195813,
8.2213727471946)) ;
#75989=CARTESIAN_POINT('Ctrl Pts',(-0.440889933449617,-2.15559078214374,
8.20813192407365)) ;
#75990=CARTESIAN_POINT('Ctrl Pts',(-0.441564708190438,-2.15729533880902,
8.21524061522766)) ;
#75991=CARTESIAN_POINT('Ctrl Pts',(-0.442204751807165,-2.15964157072194,
8.22218874465405)) ;
#75992=CARTESIAN_POINT('Ctrl Pts',(-0.442802799136171,-2.16260269917149,
8.22888130401443)) ;
#75993=CARTESIAN_POINT('Ctrl Pts',(-0.455903016748555,-2.11078568946554,
8.21832875661974)) ;
#75994=CARTESIAN_POINT('Ctrl Pts',(-0.456741824116329,-2.11321321015441,
8.22792080639222)) ;
#75995=CARTESIAN_POINT('Ctrl Pts',(-0.457563066882866,-2.11646373803811,
8.23730217497138)) ;
#75996=CARTESIAN_POINT('Ctrl Pts',(-0.458353937819047,-2.12049577671073,
8.24634291264541)) ;
#75997=CARTESIAN_POINT('Ctrl Pts',(-0.456330681975422,-2.09161206695506,
8.2232169925309)) ;
#75998=CARTESIAN_POINT('Ctrl Pts',(-0.45726263691283,-2.09434861239325,
8.23386928620929)) ;
#75999=CARTESIAN_POINT('Ctrl Pts',(-0.458174489582097,-2.09798645436108,
8.24429180991143)) ;
#76000=CARTESIAN_POINT('Ctrl Pts',(-0.459053285493831,-2.10247651427315,
8.254336493146)) ;
#76001=CARTESIAN_POINT('',(-0.459053285493831,-2.10247651427315,8.254336493146)) ;
#76002=CARTESIAN_POINT('',(-0.374769931517285,-2.19218377594761,8.22161041260296)) ;
#76003=CARTESIAN_POINT('Origin',(-0.359433815684656,-2.10247651427315,8.26305206742076)) ;
#76004=CARTESIAN_POINT('Origin',(-0.356848236064802,-2.26130448655063,8.18949965392306)) ;
#76005=CARTESIAN_POINT('Origin',(-0.453427128997611,-2.2353720855235,8.19002923013049)) ;
#76006=CARTESIAN_POINT('Ctrl Pts',(-0.374769931517285,-2.19218377594761,
8.22161041260296)) ;
#76007=CARTESIAN_POINT('Ctrl Pts',(-0.380213170855601,-2.21661176556948,
8.27650315798654)) ;
#76008=CARTESIAN_POINT('Ctrl Pts',(-0.482714730389439,-2.26627787671364,
8.29148068543043)) ;
#76009=CARTESIAN_POINT('Ctrl Pts',(-0.562407667359032,-2.29019609072325,
8.27033080756506)) ;
#76010=CARTESIAN_POINT('Ctrl Pts',(-0.56290832709327,-2.29034966353957,
8.27020605331712)) ;
#76011=CARTESIAN_POINT('Ctrl Pts',(-0.563402527094058,-2.29049913469776,
8.27007790985519)) ;
#76012=CARTESIAN_POINT('Ctrl Pts',(-0.40067446709188,-2.18764541195813,
8.2213727471946)) ;
#76013=CARTESIAN_POINT('Ctrl Pts',(-0.404799111719599,-2.2065637149284,
8.26428096643201)) ;
#76014=CARTESIAN_POINT('Ctrl Pts',(-0.488360100298001,-2.25706718969874,
8.29516164779624)) ;
#76015=CARTESIAN_POINT('Ctrl Pts',(-0.562496982169543,-2.29010647931439,
8.2703619964159)) ;
#76016=CARTESIAN_POINT('Ctrl Pts',(-0.56295018315296,-2.29030216828318,
8.27022364134446)) ;
#76017=CARTESIAN_POINT('Ctrl Pts',(-0.563402527094058,-2.29049913469776,
8.27007790985519)) ;
#76018=CARTESIAN_POINT('Ctrl Pts',(-0.442802313774365,-2.16260237888701,
8.22888148964801)) ;
#76019=CARTESIAN_POINT('Ctrl Pts',(-0.445542573614775,-2.17718689461036,
8.26171487422345)) ;
#76020=CARTESIAN_POINT('Ctrl Pts',(-0.498696522006183,-2.24300782595838,
8.3007470146104)) ;
#76021=CARTESIAN_POINT('Ctrl Pts',(-0.562651405462978,-2.28994112152854,
8.2704209692529)) ;
#76022=CARTESIAN_POINT('Ctrl Pts',(-0.563023431257417,-2.29021905158449,
8.27025442039232)) ;
#76023=CARTESIAN_POINT('Ctrl Pts',(-0.563402527094058,-2.29049913469776,
8.27007790985519)) ;
#76024=CARTESIAN_POINT('Ctrl Pts',(-0.458353937819048,-2.12049577671072,
8.24634291264541)) ;
#76025=CARTESIAN_POINT('Ctrl Pts',(-0.462239142304945,-2.1414184975613,
8.2921265128678)) ;
#76026=CARTESIAN_POINT('Ctrl Pts',(-0.512038168824972,-2.2307677807854,
8.30482405986502)) ;
#76027=CARTESIAN_POINT('Ctrl Pts',(-0.562792975700759,-2.28976846564434,
8.27048768141226)) ;
#76028=CARTESIAN_POINT('Ctrl Pts',(-0.563096679361875,-2.29013593488581,
8.27028519944017)) ;
#76029=CARTESIAN_POINT('Ctrl Pts',(-0.563402527094058,-2.29049913469776,
8.27007790985519)) ;
#76030=CARTESIAN_POINT('Ctrl Pts',(-0.459053285493832,-2.10247651427314,
8.254336493146)) ;
#76031=CARTESIAN_POINT('Ctrl Pts',(-0.463835018007331,-2.12756357251097,
8.30899194587312)) ;
#76032=CARTESIAN_POINT('Ctrl Pts',(-0.518436488407001,-2.22555128588009,
8.30657023215015)) ;
#76033=CARTESIAN_POINT('Ctrl Pts',(-0.562850741456301,-2.28969445189011,
8.27051650453023)) ;
#76034=CARTESIAN_POINT('Ctrl Pts',(-0.563128071406643,-2.29010031344351,
8.27029839046068)) ;
#76035=CARTESIAN_POINT('Ctrl Pts',(-0.563402527094058,-2.29049913469776,
8.27007790985519)) ;
#76036=CARTESIAN_POINT('',(-0.563402527094058,-2.29049913469776,8.27007790985519)) ;
#76037=CARTESIAN_POINT('Ctrl Pts',(-0.459053285493832,-2.10247651427314,
8.254336493146)) ;
#76038=CARTESIAN_POINT('Ctrl Pts',(-0.463835018007331,-2.12756357251097,
8.30899194587312)) ;
#76039=CARTESIAN_POINT('Ctrl Pts',(-0.518436488407001,-2.22555128588009,
8.30657023215015)) ;
#76040=CARTESIAN_POINT('Ctrl Pts',(-0.562850741456301,-2.28969445189011,
8.27051650453023)) ;
#76041=CARTESIAN_POINT('Ctrl Pts',(-0.563128071406643,-2.29010031344351,
8.27029839046068)) ;
#76042=CARTESIAN_POINT('Ctrl Pts',(-0.563402527094058,-2.29049913469776,
8.27007790985519)) ;
#76043=CARTESIAN_POINT('Ctrl Pts',(-0.563402527094058,-2.29049913469776,
8.27007790985519)) ;
#76044=CARTESIAN_POINT('Ctrl Pts',(-0.56290832709327,-2.29034966353957,
8.27020605331712)) ;
#76045=CARTESIAN_POINT('Ctrl Pts',(-0.562407667359032,-2.29019609072325,
8.27033080756506)) ;
#76046=CARTESIAN_POINT('Ctrl Pts',(-0.482714730389439,-2.26627787671364,
8.29148068543043)) ;
#76047=CARTESIAN_POINT('Ctrl Pts',(-0.380213170855601,-2.21661176556948,
8.27650315798654)) ;
#76048=CARTESIAN_POINT('Ctrl Pts',(-0.374769931517285,-2.19218377594761,
8.22161041260296)) ;
#76049=CARTESIAN_POINT('Origin',(-0.135929041739328,8.98859866704575E-16,
3.41363816217501)) ;
#76050=CARTESIAN_POINT('',(-0.484912864018618,-1.20584822770276,8.54991282821175)) ;
#76051=CARTESIAN_POINT('Origin',(-0.0363095719301537,2.4010481180193E-16,
3.42235373644978)) ;
#76052=CARTESIAN_POINT('',(-0.59558571006253,-1.2286505490996,8.63793337445424)) ;
#76053=CARTESIAN_POINT('Origin',(-0.584532333827793,-1.20584822770276,8.54119725393699)) ;
#76054=CARTESIAN_POINT('Origin',(-0.138499429641967,9.15857106573119E-16,
3.41341328237267)) ;
#76055=CARTESIAN_POINT('Origin',(-0.508,1.1852043994395E-14,8.8138)) ;
#76056=CARTESIAN_POINT('',(-0.332764968591544,-1.17558412963153,6.81085442572523)) ;
#76057=CARTESIAN_POINT('',(-0.332764968591536,6.44687220156331E-15,6.81085442572523)) ;
#76058=CARTESIAN_POINT('',(-0.507754795155597,-1.21039177030074,8.81099729580349)) ;
#76059=CARTESIAN_POINT('Origin',(-0.233145498782362,5.78811714666067E-15,
6.81957)) ;
#76060=CARTESIAN_POINT('',(-0.233145498782369,-1.13595304047784,6.71957)) ;
#76061=CARTESIAN_POINT('',(-0.233145498782362,5.78811714666067E-15,6.71957)) ;
#76062=CARTESIAN_POINT('Origin',(-0.233145498782369,-1.13595304047784,6.81957)) ;
#76063=CARTESIAN_POINT('Ctrl Pts',(-0.233145498782369,-1.13595304047784,
6.71957)) ;
#76064=CARTESIAN_POINT('Ctrl Pts',(-0.286360727148742,-1.13670179295399,
6.71957)) ;
#76065=CARTESIAN_POINT('Ctrl Pts',(-0.335710036450638,-1.13739615091637,
6.7615916062195)) ;
#76066=CARTESIAN_POINT('Ctrl Pts',(-0.340348049204396,-1.13746140899457,
6.81085442572523)) ;
#76067=CARTESIAN_POINT('Ctrl Pts',(-0.233145498782369,-1.13595304047784,
6.71957)) ;
#76068=CARTESIAN_POINT('Ctrl Pts',(-0.285105982851009,-1.14300981851451,
6.71957)) ;
#76069=CARTESIAN_POINT('Ctrl Pts',(-0.331172502747844,-1.14898571310984,
6.76307285057327)) ;
#76070=CARTESIAN_POINT('Ctrl Pts',(-0.335376993538162,-1.14951407564647,
6.81107958928014)) ;
#76071=CARTESIAN_POINT('Ctrl Pts',(-0.233145498782369,-1.13595304047784,
6.71957)) ;
#76072=CARTESIAN_POINT('Ctrl Pts',(-0.283851238553276,-1.14931784407502,
6.71957)) ;
#76073=CARTESIAN_POINT('Ctrl Pts',(-0.328698029275179,-1.16142573132118,
6.76307285057327)) ;
#76074=CARTESIAN_POINT('Ctrl Pts',(-0.332784667850038,-1.16254657695483,
6.81107958928014)) ;
#76075=CARTESIAN_POINT('Ctrl Pts',(-0.233145498782369,-1.13595304047784,
6.71957)) ;
#76076=CARTESIAN_POINT('Ctrl Pts',(-0.282596494255542,-1.15562586963553,
6.71957)) ;
#76077=CARTESIAN_POINT('Ctrl Pts',(-0.328455030351469,-1.17386952959435,
6.7615916062195)) ;
#76078=CARTESIAN_POINT('Ctrl Pts',(-0.332764968591544,-1.17558412963153,
6.81085442572523)) ;
#76079=CARTESIAN_POINT('',(-0.340348049204396,-1.13746140899457,6.81085442572523)) ;
#76080=CARTESIAN_POINT('Origin',(-0.432384438400719,-1.17558412963153,6.80213885145047)) ;
#76081=CARTESIAN_POINT('Origin',(-0.23314549878237,-1.13595304047784,6.81957)) ;
#76082=CARTESIAN_POINT('Origin',(-0.607374264964772,-1.21039177030074,8.80228172152873)) ;
#76083=CARTESIAN_POINT('',(-0.49249594463147,-1.1677255070658,8.54991282821175)) ;
#76084=CARTESIAN_POINT('',(-0.515337875768449,-1.17226904966378,8.81099729580349)) ;
#76085=CARTESIAN_POINT('Origin',(-0.584532333827793,-1.20584822770276,8.54119725393698)) ;
#76086=CARTESIAN_POINT('Origin',(-0.584532333827793,-1.20584822770276,8.54119725393699)) ;
#76087=CARTESIAN_POINT('Origin',(-0.584532333827793,-1.20584822770276,8.54119725393699)) ;
#76088=CARTESIAN_POINT('Origin',(-0.854554628096497,-0.353968116746241,
8.8138)) ;
#76089=CARTESIAN_POINT('',(-0.558026198990151,-0.611939867549493,6.81085442572523)) ;
#76090=CARTESIAN_POINT('',(-0.692658569199243,-0.286908573456252,6.81085442572523)) ;
#76091=CARTESIAN_POINT('',(-0.570056476111077,-0.623970147580643,6.99051559579716)) ;
#76092=CARTESIAN_POINT('',(-0.691124600663692,-0.74503826922303,8.7985570068643)) ;
#76093=CARTESIAN_POINT('',(-0.506191638276494,-0.823877279363036,7.19051557427477)) ;
#76094=CARTESIAN_POINT('Origin',(-0.589034350751109,-0.623877279363036,
7.19051557427477)) ;
#76095=CARTESIAN_POINT('',(-0.639686894805704,-0.823877279363037,8.60022433223444)) ;
#76096=CARTESIAN_POINT('',(-0.695846489640238,-0.823877279363037,9.19326916948217)) ;
#76097=CARTESIAN_POINT('Origin',(-0.415843288169372,-0.172247929781569,
3.38615128096072)) ;
#76098=CARTESIAN_POINT('Origin',(-0.60062218000292,-0.248785852819288,6.81957)) ;
#76099=CARTESIAN_POINT('',(-0.497571705638611,-0.497571705638596,6.71957)) ;
#76100=CARTESIAN_POINT('',(-0.60062218000292,-0.248785852819288,6.71957)) ;
#76101=CARTESIAN_POINT('Origin',(-0.497571705638611,-0.497571705638596,
6.81957)) ;
#76102=CARTESIAN_POINT('Origin',(-0.233145498782337,1.72771014821048,6.81957)) ;
#76103=CARTESIAN_POINT('',(-0.246063080838801,1.82343508275074,6.79368809548975)) ;
#76104=CARTESIAN_POINT('',(-0.332764968591511,1.72771014821048,6.81085442572523)) ;
#76105=CARTESIAN_POINT('Origin',(-0.233145498782337,1.72771014821048,6.81957)) ;
#76106=CARTESIAN_POINT('',(-0.233145498782337,1.72771014821048,6.71957)) ;
#76107=CARTESIAN_POINT('Origin',(-0.233145498782337,1.72771014821048,6.81957)) ;
#76108=CARTESIAN_POINT('Origin',(-0.233145498782337,1.72771014821048,6.81957)) ;
#76109=CARTESIAN_POINT('Ctrl Pts',(-0.332575554791901,1.72715033433584,
6.80868941608882)) ;
#76110=CARTESIAN_POINT('Ctrl Pts',(-0.373881299532302,1.84923054559893,
7.28081623887613)) ;
#76111=CARTESIAN_POINT('Ctrl Pts',(-0.415197776566207,1.97083234352132,
7.75306573233952)) ;
#76112=CARTESIAN_POINT('Ctrl Pts',(-0.456520172012602,2.09216847395034,
8.22538287356722)) ;
#76113=CARTESIAN_POINT('Ctrl Pts',(-0.331987953017345,1.75332513240923,
6.80197267218993)) ;
#76114=CARTESIAN_POINT('Ctrl Pts',(-0.373292933712292,1.87515504373599,
7.27418379019553)) ;
#76115=CARTESIAN_POINT('Ctrl Pts',(-0.414627967367319,1.99656668249683,
7.74649382982981)) ;
#76116=CARTESIAN_POINT('Ctrl Pts',(-0.455949949949689,2.11773252293446,
8.21886547566719)) ;
#76117=CARTESIAN_POINT('Ctrl Pts',(-0.310793595327128,1.79883340137775,
6.7920596315287)) ;
#76118=CARTESIAN_POINT('Ctrl Pts',(-0.352528666728049,1.92025230099876,
7.26437312176441)) ;
#76119=CARTESIAN_POINT('Ctrl Pts',(-0.394171753364188,2.04132212887022,
7.73676749348846)) ;
#76120=CARTESIAN_POINT('Ctrl Pts',(-0.435777022314011,2.16220666599522,
8.20920517618977)) ;
#76121=CARTESIAN_POINT('Ctrl Pts',(-0.265876600167646,1.81991774820208,
6.79053747107535)) ;
#76122=CARTESIAN_POINT('Ctrl Pts',(-0.308308238839758,1.94157711521136,
7.26274358539539)) ;
#76123=CARTESIAN_POINT('Ctrl Pts',(-0.350504776846974,2.0628320691986,7.73505295857692)) ;
#76124=CARTESIAN_POINT('Ctrl Pts',(-0.392580797820023,2.18386034844097,
8.20742162540629)) ;
#76125=CARTESIAN_POINT('Ctrl Pts',(-0.245836003043051,1.82288076242804,
6.79152463448446)) ;
#76126=CARTESIAN_POINT('Ctrl Pts',(-0.288494194883621,1.94477897268327,
7.26365133260514)) ;
#76127=CARTESIAN_POINT('Ctrl Pts',(-0.330878372341174,2.06621032168316,
7.73590073192088)) ;
#76128=CARTESIAN_POINT('Ctrl Pts',(-0.373113112727478,2.18739110458306,
8.20821779213739)) ;
#76129=CARTESIAN_POINT('',(-0.372950005137265,2.18682986267501,8.20605066229541)) ;
#76130=CARTESIAN_POINT('',(-0.456330681975378,2.09161206695507,8.2232169925309)) ;
#76131=CARTESIAN_POINT('Origin',(-0.356711212166204,2.09161206695507,8.23193256680567)) ;
#76132=CARTESIAN_POINT('Ctrl Pts',(-0.456330681975378,2.09161206695507,
8.2232169925309)) ;
#76133=CARTESIAN_POINT('Ctrl Pts',(-0.415134631297216,1.97064606309603,
7.75234397861228)) ;
#76134=CARTESIAN_POINT('Ctrl Pts',(-0.37394447021383,1.84941569039776,7.28153828307)) ;
#76135=CARTESIAN_POINT('Ctrl Pts',(-0.332764968591511,1.72771014821048,
6.81085442572523)) ;
#76136=CARTESIAN_POINT('Ctrl Pts',(-0.246063080838802,1.82343508275074,
6.79368809548975)) ;
#76137=CARTESIAN_POINT('Ctrl Pts',(-0.263106778000196,1.87213905946162,
6.98232754963782)) ;
#76138=CARTESIAN_POINT('Ctrl Pts',(-0.280128754029967,1.92076304376552,
7.17098657374507)) ;
#76139=CARTESIAN_POINT('Ctrl Pts',(-0.314082706992799,2.01793487884333,
7.54848217853971)) ;
#76140=CARTESIAN_POINT('Ctrl Pts',(-0.331014637616039,2.06648276269927,
7.7373187839961)) ;
#76141=CARTESIAN_POINT('Ctrl Pts',(-0.356264911138476,2.13894444266998,
8.01945926643178)) ;
#76142=CARTESIAN_POINT('Ctrl Pts',(-0.36460731300339,2.1628928530267,8.1127536429719)) ;
#76143=CARTESIAN_POINT('Ctrl Pts',(-0.372950005137265,2.18682986267501,
8.20605066229541)) ;
#76144=CARTESIAN_POINT('Ctrl Pts',(-0.37476993151724,2.19218377594762,8.22161041260296)) ;
#76145=CARTESIAN_POINT('Ctrl Pts',(-0.374271909287332,2.18994876824219,
8.21658807098568)) ;
#76146=CARTESIAN_POINT('Ctrl Pts',(-0.373662616506283,2.18815607354195,
8.21137680913461)) ;
#76147=CARTESIAN_POINT('Ctrl Pts',(-0.372950005137264,2.18682986267501,
8.20605066229541)) ;
#76148=CARTESIAN_POINT('Ctrl Pts',(-0.400674467091834,2.18764541195814,
8.2213727471946)) ;
#76149=CARTESIAN_POINT('Ctrl Pts',(-0.400168655131387,2.18531329532944,
8.21609868976098)) ;
#76150=CARTESIAN_POINT('Ctrl Pts',(-0.399569847844606,2.18345309008413,
8.21059040433855)) ;
#76151=CARTESIAN_POINT('Ctrl Pts',(-0.39889297813083,2.18211755991819,8.20499152409472)) ;
#76152=CARTESIAN_POINT('Ctrl Pts',(-0.442802799136127,2.1626026991715,8.22888130401443)) ;
#76153=CARTESIAN_POINT('Ctrl Pts',(-0.44220475180712,2.15964157072196,8.22218874465405)) ;
#76154=CARTESIAN_POINT('Ctrl Pts',(-0.441564708190393,2.15729533880903,
8.21524061522765)) ;
#76155=CARTESIAN_POINT('Ctrl Pts',(-0.440889933449573,2.15559078214375,
8.20813192407365)) ;
#76156=CARTESIAN_POINT('Ctrl Pts',(-0.458353937819003,2.12049577671074,
8.24634291264541)) ;
#76157=CARTESIAN_POINT('Ctrl Pts',(-0.457563066882822,2.11646373803812,
8.23730217497138)) ;
#76158=CARTESIAN_POINT('Ctrl Pts',(-0.456741824116285,2.11321321015442,
8.22792080639222)) ;
#76159=CARTESIAN_POINT('Ctrl Pts',(-0.455903016748511,2.11078568946555,
8.21832875661974)) ;
#76160=CARTESIAN_POINT('Ctrl Pts',(-0.459053285493787,2.10247651427316,
8.254336493146)) ;
#76161=CARTESIAN_POINT('Ctrl Pts',(-0.458174489582053,2.09798645436109,
8.24429180991143)) ;
#76162=CARTESIAN_POINT('Ctrl Pts',(-0.457262636912786,2.09434861239326,
8.23386928620929)) ;
#76163=CARTESIAN_POINT('Ctrl Pts',(-0.456330681975378,2.09161206695507,
8.2232169925309)) ;
#76164=CARTESIAN_POINT('',(-0.37476993151724,2.19218377594762,8.22161041260296)) ;
#76165=CARTESIAN_POINT('Origin',(-0.356848236134331,2.26130448626201,8.18949965402755)) ;
#76166=CARTESIAN_POINT('',(-0.459053285493787,2.10247651427316,8.254336493146)) ;
#76167=CARTESIAN_POINT('Origin',(-0.359433815684613,2.10247651427315,8.26305206742076)) ;
#76168=CARTESIAN_POINT('Origin',(-0.453427128997903,2.23537208552098,8.19002923013433)) ;
#76169=CARTESIAN_POINT('Ctrl Pts',(-0.459053285493787,2.10247651427316,
8.254336493146)) ;
#76170=CARTESIAN_POINT('Ctrl Pts',(-0.463831274313048,2.12754393145512,
8.30894915525216)) ;
#76171=CARTESIAN_POINT('Ctrl Pts',(-0.518364204358841,2.22542453008761,
8.30657276282558)) ;
#76172=CARTESIAN_POINT('Ctrl Pts',(-0.562784097682946,2.28959720721989,
8.27056932236647)) ;
#76173=CARTESIAN_POINT('Ctrl Pts',(-0.563094923804728,2.29005214549267,
8.27032501917936)) ;
#76174=CARTESIAN_POINT('Ctrl Pts',(-0.563402527094011,2.29049913469777,
8.27007790985519)) ;
#76175=CARTESIAN_POINT('Ctrl Pts',(-0.458120821927409,2.12650219752326,
8.24367838581188)) ;
#76176=CARTESIAN_POINT('Ctrl Pts',(-0.461688990889963,2.14596383549791,
8.2863515376309)) ;
#76177=CARTESIAN_POINT('Ctrl Pts',(-0.509789157873014,2.23236813286337,
8.30425558488427)) ;
#76178=CARTESIAN_POINT('Ctrl Pts',(-0.562697924855537,2.28970787909533,
8.27052608050501)) ;
#76179=CARTESIAN_POINT('Ctrl Pts',(-0.563048012546372,2.29010537702631,
8.27030530694405)) ;
#76180=CARTESIAN_POINT('Ctrl Pts',(-0.563402527094011,2.29049913469777,
8.27007790985519)) ;
#76181=CARTESIAN_POINT('Ctrl Pts',(-0.437455203934548,2.16829359261983,
8.22680527958952)) ;
#76182=CARTESIAN_POINT('Ctrl Pts',(-0.440261220239578,2.18279728043183,
8.2596380798338)) ;
#76183=CARTESIAN_POINT('Ctrl Pts',(-0.497045700566893,2.24468709263695,
8.30004898389791)) ;
#76184=CARTESIAN_POINT('Ctrl Pts',(-0.562536291712692,2.28990117236503,
8.27045202116462)) ;
#76185=CARTESIAN_POINT('Ctrl Pts',(-0.562965917844249,2.29019853221018,
8.27027081053226)) ;
#76186=CARTESIAN_POINT('Ctrl Pts',(-0.563402527094011,2.29049913469777,
8.27007790985519)) ;
#76187=CARTESIAN_POINT('Ctrl Pts',(-0.394198333198186,2.18878000295551,
8.22143216354669)) ;
#76188=CARTESIAN_POINT('Ctrl Pts',(-0.398660337213041,2.2091034537124,8.26739017065233)) ;
#76189=CARTESIAN_POINT('Ctrl Pts',(-0.486849819185561,2.25930987312264,
8.29418883400901)) ;
#76190=CARTESIAN_POINT('Ctrl Pts',(-0.562362466050226,2.2900840072024,8.27038751506786)) ;
#76191=CARTESIAN_POINT('Ctrl Pts',(-0.562883823142126,2.29029168739404,
8.27023631412047)) ;
#76192=CARTESIAN_POINT('Ctrl Pts',(-0.563402527094011,2.29049913469777,
8.27007790985519)) ;
#76193=CARTESIAN_POINT('Ctrl Pts',(-0.37476993151724,2.19218377594762,8.22161041260296)) ;
#76194=CARTESIAN_POINT('Ctrl Pts',(-0.38020890925713,2.2165926405089,8.27646018158539)) ;
#76195=CARTESIAN_POINT('Ctrl Pts',(-0.482582465715569,2.26621331095889,
8.29146075442296)) ;
#76196=CARTESIAN_POINT('Ctrl Pts',(-0.562287508336611,2.29015942107408,
8.27036120321575)) ;
#76197=CARTESIAN_POINT('Ctrl Pts',(-0.562848639698359,2.29033161104427,
8.27022152994399)) ;
#76198=CARTESIAN_POINT('Ctrl Pts',(-0.563402527094011,2.29049913469777,
8.27007790985519)) ;
#76199=CARTESIAN_POINT('',(-0.563402527094011,2.29049913469777,8.27007790985519)) ;
#76200=CARTESIAN_POINT('Ctrl Pts',(-0.37476993151724,2.19218377594762,8.22161041260296)) ;
#76201=CARTESIAN_POINT('Ctrl Pts',(-0.38020890925713,2.2165926405089,8.27646018158539)) ;
#76202=CARTESIAN_POINT('Ctrl Pts',(-0.482582465715569,2.26621331095889,
8.29146075442296)) ;
#76203=CARTESIAN_POINT('Ctrl Pts',(-0.562287508336611,2.29015942107408,
8.27036120321575)) ;
#76204=CARTESIAN_POINT('Ctrl Pts',(-0.562848639698359,2.29033161104427,
8.27022152994399)) ;
#76205=CARTESIAN_POINT('Ctrl Pts',(-0.563402527094011,2.29049913469777,
8.27007790985519)) ;
#76206=CARTESIAN_POINT('Ctrl Pts',(-0.563402527094011,2.29049913469777,
8.27007790985519)) ;
#76207=CARTESIAN_POINT('Ctrl Pts',(-0.563094923804728,2.29005214549267,
8.27032501917936)) ;
#76208=CARTESIAN_POINT('Ctrl Pts',(-0.562784097682946,2.28959720721989,
8.27056932236647)) ;
#76209=CARTESIAN_POINT('Ctrl Pts',(-0.518364204358841,2.22542453008761,
8.30657276282558)) ;
#76210=CARTESIAN_POINT('Ctrl Pts',(-0.463831274313048,2.12754393145512,
8.30894915525216)) ;
#76211=CARTESIAN_POINT('Ctrl Pts',(-0.459053285493787,2.10247651427316,
8.254336493146)) ;
#76212=CARTESIAN_POINT('Origin',(0.,0.,8.18016875778516)) ;
#76213=CARTESIAN_POINT('',(0.372950005137295,2.18682986267501,8.20605066229541)) ;
#76214=CARTESIAN_POINT('Origin',(-1.10454254757634E-16,0.,8.20605066229541)) ;
#76215=CARTESIAN_POINT('',(0.374769931517269,2.19218377594761,8.22161041260296)) ;
#76216=CARTESIAN_POINT('Origin',(0.356848236098008,2.26130448641591,8.18949965397682)) ;
#76217=CARTESIAN_POINT('',(0.563402527094043,2.29049913469776,8.27007790985519)) ;
#76218=CARTESIAN_POINT('Ctrl Pts',(0.563402527094042,2.29049913469776,8.27007790985519)) ;
#76219=CARTESIAN_POINT('Ctrl Pts',(0.562908327135226,2.29034966355222,8.27020605330626)) ;
#76220=CARTESIAN_POINT('Ctrl Pts',(0.562407667443435,2.29019609074898,8.27033080754371)) ;
#76221=CARTESIAN_POINT('Ctrl Pts',(0.482714730480227,2.26627787676058,8.29148068544431)) ;
#76222=CARTESIAN_POINT('Ctrl Pts',(0.380213170858573,2.21661176558288,8.27650315801665)) ;
#76223=CARTESIAN_POINT('Ctrl Pts',(0.374769931517269,2.19218377594761,8.22161041260296)) ;
#76224=CARTESIAN_POINT('Origin',(0.,0.,8.27007790985519)) ;
#76225=CARTESIAN_POINT('Origin',(0.,0.,8.8138)) ;
#76226=CARTESIAN_POINT('',(0.246063080838827,1.82343508275074,6.79368809548975)) ;
#76227=CARTESIAN_POINT('Origin',(-9.16116711833935E-17,0.,6.79368809548975)) ;
#76228=CARTESIAN_POINT('Ctrl Pts',(0.372950005137295,2.18682986267501,8.20605066229541)) ;
#76229=CARTESIAN_POINT('Ctrl Pts',(0.356060675112335,2.13837067836455,8.01717588129979)) ;
#76230=CARTESIAN_POINT('Ctrl Pts',(0.339169373366003,2.08986565451436,7.82831193143937)) ;
#76231=CARTESIAN_POINT('Ctrl Pts',(0.305304200525137,1.99279235652906,7.45075381522683)) ;
#76232=CARTESIAN_POINT('Ctrl Pts',(0.288330373027766,1.94422406244447,7.26205962744222)) ;
#76233=CARTESIAN_POINT('Ctrl Pts',(0.262904814260669,1.87155513860968,6.98014705352744)) ;
#76234=CARTESIAN_POINT('Ctrl Pts',(0.254486208871158,1.84750496780177,6.886915184612)) ;
#76235=CARTESIAN_POINT('Ctrl Pts',(0.246063080838828,1.82343508275074,6.79368809548975)) ;
#76236=CARTESIAN_POINT('Origin',(0.,0.,6.81957)) ;
#76237=CARTESIAN_POINT('',(0.233145498782361,1.72771014821048,6.71957)) ;
#76238=CARTESIAN_POINT('Origin',(0.,0.,6.71957)) ;
#76239=CARTESIAN_POINT('Origin',(0.233145498782361,1.72771014821048,6.81957)) ;
#76240=CARTESIAN_POINT('Origin',(-0.233145498782355,4.55548777629246E-15,
6.81957)) ;
#76241=CARTESIAN_POINT('',(-0.332764968591517,1.17558412963155,6.81085442572523)) ;
#76242=CARTESIAN_POINT('',(-0.332764968591529,5.59476833506534E-15,6.81085442572523)) ;
#76243=CARTESIAN_POINT('',(-0.233145498782343,1.13595304047785,6.71957)) ;
#76244=CARTESIAN_POINT('Origin',(-0.233145498782343,1.13595304047785,6.81957)) ;
#76245=CARTESIAN_POINT('',(-0.233145498782355,4.55548777629246E-15,6.71957)) ;
#76246=CARTESIAN_POINT('Origin',(0.233145498782361,1.72771014821048,6.81957)) ;
#76247=CARTESIAN_POINT('',(0.332764968591536,1.72771014821048,6.81085442572523)) ;
#76248=CARTESIAN_POINT('Origin',(0.233145498782361,1.72771014821048,6.81957)) ;
#76249=CARTESIAN_POINT('Origin',(0.233145498782361,1.72771014821048,6.81957)) ;
#76250=CARTESIAN_POINT('Ctrl Pts',(0.245836001151724,1.82288075802732,6.79152461795156)) ;
#76251=CARTESIAN_POINT('Ctrl Pts',(0.288494198954246,1.94477897799293,7.26365132481993)) ;
#76252=CARTESIAN_POINT('Ctrl Pts',(0.330878369255154,2.06621031878836,7.73590073893382)) ;
#76253=CARTESIAN_POINT('Ctrl Pts',(0.373113113874311,2.18739110879813,8.20821780878248)) ;
#76254=CARTESIAN_POINT('Ctrl Pts',(0.272553537557606,1.81893081948751,6.79020849165203)) ;
#76255=CARTESIAN_POINT('Ctrl Pts',(0.314905492765744,1.94050480823746,7.26244303991256)) ;
#76256=CARTESIAN_POINT('Ctrl Pts',(0.357046431871077,2.06171037042182,7.73476924079919)) ;
#76257=CARTESIAN_POINT('Ctrl Pts',(0.399066819643634,2.18268421515255,8.20715633330628)) ;
#76258=CARTESIAN_POINT('Ctrl Pts',(0.316376716061575,1.79267106092127,6.7931645820536)) ;
#76259=CARTESIAN_POINT('Ctrl Pts',(0.35799439116309,1.91413489045696,7.26547214220374)) ;
#76260=CARTESIAN_POINT('Ctrl Pts',(0.399548971339515,2.03523918647934,7.73786227286442)) ;
#76261=CARTESIAN_POINT('Ctrl Pts',(0.441077054244115,2.15615536078618,8.21029605360251)) ;
#76262=CARTESIAN_POINT('Ctrl Pts',(0.332134835417778,1.74678141058443,6.80365184796761)) ;
#76263=CARTESIAN_POINT('Ctrl Pts',(0.373443640776162,1.86867784544074,7.2758405013989)) ;
#76264=CARTESIAN_POINT('Ctrl Pts',(0.414768073581239,1.99013064875085,7.74813767788448)) ;
#76265=CARTESIAN_POINT('Ctrl Pts',(0.4560925176698,2.11134152617597,8.22049483777628)) ;
#76266=CARTESIAN_POINT('Ctrl Pts',(0.33257555333983,1.72715033004413,6.80868939949129)) ;
#76267=CARTESIAN_POINT('Ctrl Pts',(0.373881299048044,1.84923054417957,7.28081623334075)) ;
#76268=CARTESIAN_POINT('Ctrl Pts',(0.415197777050322,1.97083234494938,7.75306573787267)) ;
#76269=CARTESIAN_POINT('Ctrl Pts',(0.456520173465311,2.09216847821588,8.22538289017143)) ;
#76270=CARTESIAN_POINT('',(0.456330681975407,2.09161206695506,8.2232169925309)) ;
#76271=CARTESIAN_POINT('Origin',(0.356711212166233,2.09161206695506,8.23193256680567)) ;
#76272=CARTESIAN_POINT('Ctrl Pts',(0.332764968591536,1.72771014821048,6.81085442572523)) ;
#76273=CARTESIAN_POINT('Ctrl Pts',(0.373944470213856,1.84941569039776,7.28153828307)) ;
#76274=CARTESIAN_POINT('Ctrl Pts',(0.415134631297243,1.97064606309602,7.75234397861228)) ;
#76275=CARTESIAN_POINT('Ctrl Pts',(0.456330681975407,2.09161206695506,8.2232169925309)) ;
#76276=CARTESIAN_POINT('Ctrl Pts',(0.372950005137295,2.18682986267501,8.20605066229542)) ;
#76277=CARTESIAN_POINT('Ctrl Pts',(0.373662616506314,2.18815607354194,8.21137680913461)) ;
#76278=CARTESIAN_POINT('Ctrl Pts',(0.374271909287362,2.18994876824218,8.21658807098568)) ;
#76279=CARTESIAN_POINT('Ctrl Pts',(0.374769931517269,2.19218377594761,8.22161041260296)) ;
#76280=CARTESIAN_POINT('Ctrl Pts',(0.39889297813086,2.18211755991818,8.20499152409472)) ;
#76281=CARTESIAN_POINT('Ctrl Pts',(0.399569847844636,2.18345309008412,8.21059040433856)) ;
#76282=CARTESIAN_POINT('Ctrl Pts',(0.400168655131417,2.18531329532944,8.21609868976098)) ;
#76283=CARTESIAN_POINT('Ctrl Pts',(0.400674467091864,2.18764541195814,8.2213727471946)) ;
#76284=CARTESIAN_POINT('Ctrl Pts',(0.440889933449603,2.15559078214375,8.20813192407366)) ;
#76285=CARTESIAN_POINT('Ctrl Pts',(0.441564708190423,2.15729533880903,8.21524061522766)) ;
#76286=CARTESIAN_POINT('Ctrl Pts',(0.44220475180715,2.15964157072195,8.22218874465405)) ;
#76287=CARTESIAN_POINT('Ctrl Pts',(0.442802799136157,2.16260269917149,8.22888130401443)) ;
#76288=CARTESIAN_POINT('Ctrl Pts',(0.45590301674854,2.11078568946555,8.21832875661974)) ;
#76289=CARTESIAN_POINT('Ctrl Pts',(0.456741824116314,2.11321321015441,8.22792080639223)) ;
#76290=CARTESIAN_POINT('Ctrl Pts',(0.457563066882852,2.11646373803811,8.23730217497138)) ;
#76291=CARTESIAN_POINT('Ctrl Pts',(0.458353937819032,2.12049577671073,8.2463429126454)) ;
#76292=CARTESIAN_POINT('Ctrl Pts',(0.456330681975408,2.09161206695506,8.22321699253091)) ;
#76293=CARTESIAN_POINT('Ctrl Pts',(0.457262636912815,2.09434861239326,8.23386928620929)) ;
#76294=CARTESIAN_POINT('Ctrl Pts',(0.458174489582082,2.09798645436109,8.24429180991143)) ;
#76295=CARTESIAN_POINT('Ctrl Pts',(0.459053285493816,2.10247651427315,8.254336493146)) ;
#76296=CARTESIAN_POINT('',(0.459053285493816,2.10247651427315,8.254336493146)) ;
#76297=CARTESIAN_POINT('Origin',(0.359433815684642,2.10247651427315,8.26305206742076)) ;
#76298=CARTESIAN_POINT('Origin',(0.45342712900337,2.23537208534447,8.19002923019672)) ;
#76299=CARTESIAN_POINT('Ctrl Pts',(0.374769931517269,2.19218377594761,8.22161041260296)) ;
#76300=CARTESIAN_POINT('Ctrl Pts',(0.380213170858573,2.21661176558288,8.27650315801665)) ;
#76301=CARTESIAN_POINT('Ctrl Pts',(0.482714730480227,2.26627787676058,8.29148068544431)) ;
#76302=CARTESIAN_POINT('Ctrl Pts',(0.562407667443435,2.29019609074898,8.27033080754371)) ;
#76303=CARTESIAN_POINT('Ctrl Pts',(0.562908327135226,2.29034966355222,8.27020605330626)) ;
#76304=CARTESIAN_POINT('Ctrl Pts',(0.563402527094042,2.29049913469776,8.27007790985519)) ;
#76305=CARTESIAN_POINT('Ctrl Pts',(0.400674467091864,2.18764541195814,8.2213727471946)) ;
#76306=CARTESIAN_POINT('Ctrl Pts',(0.404799111721846,2.20656371493878,8.26428096645554)) ;
#76307=CARTESIAN_POINT('Ctrl Pts',(0.488360100380293,2.25706718975662,8.29516164781817)) ;
#76308=CARTESIAN_POINT('Ctrl Pts',(0.562496982246372,2.29010647934773,8.27036199639192)) ;
#76309=CARTESIAN_POINT('Ctrl Pts',(0.562950183191371,2.29030216829986,8.27022364133211)) ;
#76310=CARTESIAN_POINT('Ctrl Pts',(0.563402527094042,2.29049913469776,8.27007790985519)) ;
#76311=CARTESIAN_POINT('Ctrl Pts',(0.442802313774349,2.16260237888702,8.22888148964801)) ;
#76312=CARTESIAN_POINT('Ctrl Pts',(0.445542573616263,2.17718689461836,8.26171487424146)) ;
#76313=CARTESIAN_POINT('Ctrl Pts',(0.498696522073216,2.24300782603398,8.30074701463518)) ;
#76314=CARTESIAN_POINT('Ctrl Pts',(0.562651405526709,2.28994112157589,8.27042096922394)) ;
#76315=CARTESIAN_POINT('Ctrl Pts',(0.563023431289625,2.29021905160823,8.27025442037735)) ;
#76316=CARTESIAN_POINT('Ctrl Pts',(0.563402527094042,2.29049913469776,8.27007790985519)) ;
#76317=CARTESIAN_POINT('Ctrl Pts',(0.458353937819032,2.12049577671073,8.2463429126454)) ;
#76318=CARTESIAN_POINT('Ctrl Pts',(0.462239142307061,2.14141849757278,8.29212651289291)) ;
#76319=CARTESIAN_POINT('Ctrl Pts',(0.512038168879329,2.23076778087308,8.30482405987301)) ;
#76320=CARTESIAN_POINT('Ctrl Pts',(0.56279297575247,2.28976846570632,8.27048768137762)) ;
#76321=CARTESIAN_POINT('Ctrl Pts',(0.56309667938788,2.2901359349166,8.27028519942259)) ;
#76322=CARTESIAN_POINT('Ctrl Pts',(0.563402527094042,2.29049913469776,8.27007790985519)) ;
#76323=CARTESIAN_POINT('Ctrl Pts',(0.459053285493816,2.10247651427315,8.254336493146)) ;
#76324=CARTESIAN_POINT('Ctrl Pts',(0.463835018009939,2.12756357252473,8.3089919459031)) ;
#76325=CARTESIAN_POINT('Ctrl Pts',(0.518436488456744,2.22555128597153,8.30657023214747)) ;
#76326=CARTESIAN_POINT('Ctrl Pts',(0.562850741503104,2.28969445195835,8.27051650449314)) ;
#76327=CARTESIAN_POINT('Ctrl Pts',(0.563128071429989,2.29010031347733,8.27029839044198)) ;
#76328=CARTESIAN_POINT('Ctrl Pts',(0.563402527094042,2.29049913469776,8.27007790985519)) ;
#76329=CARTESIAN_POINT('Ctrl Pts',(0.459053285493816,2.10247651427315,8.254336493146)) ;
#76330=CARTESIAN_POINT('Ctrl Pts',(0.463835018009939,2.12756357252473,8.3089919459031)) ;
#76331=CARTESIAN_POINT('Ctrl Pts',(0.518436488456744,2.22555128597153,8.30657023214747)) ;
#76332=CARTESIAN_POINT('Ctrl Pts',(0.562850741503104,2.28969445195835,8.27051650449314)) ;
#76333=CARTESIAN_POINT('Ctrl Pts',(0.563128071429989,2.29010031347733,8.27029839044198)) ;
#76334=CARTESIAN_POINT('Ctrl Pts',(0.563402527094042,2.29049913469776,8.27007790985519)) ;
#76335=CARTESIAN_POINT('Origin',(0.135929041739328,3.89259393415546E-17,
3.41363816217501)) ;
#76336=CARTESIAN_POINT('',(0.48491286401861,1.20584822770277,8.54991282821175)) ;
#76337=CARTESIAN_POINT('Origin',(0.0363095719301537,1.03979559951686E-17,
3.42235373644978)) ;
#76338=CARTESIAN_POINT('',(0.595585710062521,1.22865054909962,8.63793337445424)) ;
#76339=CARTESIAN_POINT('Origin',(0.584532333827785,1.20584822770277,8.54119725393698)) ;
#76340=CARTESIAN_POINT('Origin',(0.138499429641967,3.9662020184192E-17,
3.41341328237267)) ;
#76341=CARTESIAN_POINT('Origin',(0.508,1.45475734489699E-16,8.8138)) ;
#76342=CARTESIAN_POINT('',(0.332764968591536,1.17558412963154,6.81085442572523)) ;
#76343=CARTESIAN_POINT('',(0.332764968591536,9.52937563352271E-17,6.81085442572523)) ;
#76344=CARTESIAN_POINT('',(0.507754795155589,1.21039177030075,8.81099729580349)) ;
#76345=CARTESIAN_POINT('Origin',(0.233145498782362,6.67657729888411E-17,
6.81957)) ;
#76346=CARTESIAN_POINT('',(0.233145498782361,1.13595304047785,6.71957)) ;
#76347=CARTESIAN_POINT('',(0.233145498782362,6.67657729888411E-17,6.71957)) ;
#76348=CARTESIAN_POINT('Origin',(0.233145498782361,1.13595304047784,6.81957)) ;
#76349=CARTESIAN_POINT('Ctrl Pts',(0.233145498782362,1.13595304047784,6.71957)) ;
#76350=CARTESIAN_POINT('Ctrl Pts',(0.286360727148734,1.136701792954,6.71957)) ;
#76351=CARTESIAN_POINT('Ctrl Pts',(0.33571003645063,1.13739615091638,6.7615916062195)) ;
#76352=CARTESIAN_POINT('Ctrl Pts',(0.340348049204388,1.13746140899458,6.81085442572523)) ;
#76353=CARTESIAN_POINT('Ctrl Pts',(0.233145498782362,1.13595304047784,6.71957)) ;
#76354=CARTESIAN_POINT('Ctrl Pts',(0.285105982851001,1.14300981851451,6.71957)) ;
#76355=CARTESIAN_POINT('Ctrl Pts',(0.331172502747836,1.14898571310985,6.76307285057327)) ;
#76356=CARTESIAN_POINT('Ctrl Pts',(0.335376993538154,1.14951407564648,6.81107958928014)) ;
#76357=CARTESIAN_POINT('Ctrl Pts',(0.233145498782362,1.13595304047784,6.71957)) ;
#76358=CARTESIAN_POINT('Ctrl Pts',(0.283851238553268,1.14931784407503,6.71957)) ;
#76359=CARTESIAN_POINT('Ctrl Pts',(0.328698029275171,1.16142573132119,6.76307285057327)) ;
#76360=CARTESIAN_POINT('Ctrl Pts',(0.33278466785003,1.16254657695484,6.81107958928014)) ;
#76361=CARTESIAN_POINT('Ctrl Pts',(0.233145498782362,1.13595304047784,6.71957)) ;
#76362=CARTESIAN_POINT('Ctrl Pts',(0.282596494255534,1.15562586963554,6.71957)) ;
#76363=CARTESIAN_POINT('Ctrl Pts',(0.328455030351461,1.17386952959435,6.7615916062195)) ;
#76364=CARTESIAN_POINT('Ctrl Pts',(0.332764968591536,1.17558412963154,6.81085442572523)) ;
#76365=CARTESIAN_POINT('',(0.340348049204388,1.13746140899458,6.81085442572523)) ;
#76366=CARTESIAN_POINT('Origin',(0.432384438400711,1.17558412963154,6.80213885145047)) ;
#76367=CARTESIAN_POINT('Origin',(0.233145498782362,1.13595304047784,6.81957)) ;
#76368=CARTESIAN_POINT('Origin',(0.607374264964764,1.21039177030075,8.80228172152873)) ;
#76369=CARTESIAN_POINT('',(0.492495944631461,1.16772550706581,8.54991282821175)) ;
#76370=CARTESIAN_POINT('',(0.515337875768441,1.17226904966379,8.81099729580349)) ;
#76371=CARTESIAN_POINT('Origin',(0.584532333827784,1.20584822770277,8.54119725393698)) ;
#76372=CARTESIAN_POINT('Origin',(0.584532333827785,1.20584822770277,8.54119725393698)) ;
#76373=CARTESIAN_POINT('Origin',(0.584532333827785,1.20584822770277,8.54119725393698)) ;
#76374=CARTESIAN_POINT('Origin',(0.854554628096495,0.353968116746256,8.8138)) ;
#76375=CARTESIAN_POINT('',(0.558026198990147,0.611939867549503,6.81085442572523)) ;
#76376=CARTESIAN_POINT('',(0.692658569199242,0.286908573456262,6.81085442572523)) ;
#76377=CARTESIAN_POINT('',(0.570056476111073,0.623970147580653,6.99051559579716)) ;
#76378=CARTESIAN_POINT('',(0.691124600663687,0.745038269223043,8.7985570068643)) ;
#76379=CARTESIAN_POINT('',(0.506191638276493,0.823877279363036,7.19051557427477)) ;
#76380=CARTESIAN_POINT('Origin',(0.58903435075111,0.623877279363035,7.19051557427477)) ;
#76381=CARTESIAN_POINT('',(0.639686894805704,0.823877279363036,8.60022433223443)) ;
#76382=CARTESIAN_POINT('',(0.611189919984901,0.823877279363036,8.29929652382612)) ;
#76383=CARTESIAN_POINT('Origin',(0.415843288169372,0.172247929781573,3.38615128096072)) ;
#76384=CARTESIAN_POINT('Origin',(0.600622180002919,0.248785852819297,6.81957)) ;
#76385=CARTESIAN_POINT('',(0.497571705638608,0.497571705638606,6.71957)) ;
#76386=CARTESIAN_POINT('',(0.600622180002919,0.248785852819297,6.71957)) ;
#76387=CARTESIAN_POINT('Origin',(0.497571705638608,0.497571705638606,6.81957)) ;
#76388=CARTESIAN_POINT('Ctrl Pts',(-0.233145498782343,1.13595304047785,
6.71957)) ;
#76389=CARTESIAN_POINT('Ctrl Pts',(-0.282596494255515,1.15562586963555,
6.71957)) ;
#76390=CARTESIAN_POINT('Ctrl Pts',(-0.328455030351442,1.17386952959436,
6.7615916062195)) ;
#76391=CARTESIAN_POINT('Ctrl Pts',(-0.332764968591517,1.17558412963155,
6.81085442572523)) ;
#76392=CARTESIAN_POINT('Ctrl Pts',(-0.233145498782343,1.13595304047785,
6.71957)) ;
#76393=CARTESIAN_POINT('Ctrl Pts',(-0.283851238553249,1.14931784407504,
6.71957)) ;
#76394=CARTESIAN_POINT('Ctrl Pts',(-0.328698029275152,1.1614257313212,6.76307285057327)) ;
#76395=CARTESIAN_POINT('Ctrl Pts',(-0.332784667850011,1.16254657695485,
6.81107958928014)) ;
#76396=CARTESIAN_POINT('Ctrl Pts',(-0.233145498782343,1.13595304047785,
6.71957)) ;
#76397=CARTESIAN_POINT('Ctrl Pts',(-0.285105982850982,1.14300981851452,
6.71957)) ;
#76398=CARTESIAN_POINT('Ctrl Pts',(-0.331172502747817,1.14898571310986,
6.76307285057327)) ;
#76399=CARTESIAN_POINT('Ctrl Pts',(-0.335376993538135,1.14951407564649,
6.81107958928014)) ;
#76400=CARTESIAN_POINT('Ctrl Pts',(-0.233145498782343,1.13595304047785,
6.71957)) ;
#76401=CARTESIAN_POINT('Ctrl Pts',(-0.286360727148716,1.13670179295401,
6.71957)) ;
#76402=CARTESIAN_POINT('Ctrl Pts',(-0.335710036450612,1.13739615091639,
6.7615916062195)) ;
#76403=CARTESIAN_POINT('Ctrl Pts',(-0.340348049204369,1.13746140899459,
6.81085442572523)) ;
#76404=CARTESIAN_POINT('',(-0.340348049204369,1.13746140899459,6.81085442572523)) ;
#76405=CARTESIAN_POINT('Origin',(-0.432384438400691,1.17558412963155,6.80213885145047)) ;
#76406=CARTESIAN_POINT('Origin',(-0.233145498782343,1.13595304047785,6.81957)) ;
#76407=CARTESIAN_POINT('Origin',(-0.607374264964743,1.21039177030077,8.80228172152873)) ;
#76408=CARTESIAN_POINT('',(-0.48491286401859,1.20584822770278,8.54991282821175)) ;
#76409=CARTESIAN_POINT('',(-0.507754795155569,1.21039177030076,8.81099729580349)) ;
#76410=CARTESIAN_POINT('',(-0.492495944631442,1.16772550706582,8.54991282821175)) ;
#76411=CARTESIAN_POINT('Origin',(-0.584532333827764,1.20584822770279,8.54119725393698)) ;
#76412=CARTESIAN_POINT('',(-0.515337875768421,1.1722690496638,8.81099729580349)) ;
#76413=CARTESIAN_POINT('Origin',(-0.584532333827764,1.20584822770279,8.54119725393698)) ;
#76414=CARTESIAN_POINT('',(-0.5955857100625,1.22865054909963,8.63793337445423)) ;
#76415=CARTESIAN_POINT('Origin',(-0.584532333827764,1.20584822770279,8.54119725393698)) ;
#76416=CARTESIAN_POINT('Origin',(-0.584532333827764,1.20584822770279,8.54119725393698)) ;
#76417=CARTESIAN_POINT('Origin',(-0.507999999999992,9.54610490470689E-15,
8.8138)) ;
#76418=CARTESIAN_POINT('Origin',(-0.0363095719301483,3.78799769529521E-16,
3.42235373644978)) ;
#76419=CARTESIAN_POINT('Origin',(-0.600622180002913,0.248785852819307,6.81957)) ;
#76420=CARTESIAN_POINT('',(-0.558026198990135,0.611939867549514,6.81085442572523)) ;
#76421=CARTESIAN_POINT('',(-0.692658569199236,0.286908573456273,6.81085442572523)) ;
#76422=CARTESIAN_POINT('',(-0.497571705638597,0.497571705638616,6.71957)) ;
#76423=CARTESIAN_POINT('Origin',(-0.497571705638597,0.497571705638616,6.81957)) ;
#76424=CARTESIAN_POINT('',(-0.600622180002913,0.248785852819307,6.71957)) ;
#76425=CARTESIAN_POINT('Ctrl Pts',(-1.19897656428781,-0.496373153556905,
6.33534590600784)) ;
#76426=CARTESIAN_POINT('Ctrl Pts',(-1.29413398678263,-0.345965287843427,
6.33536184533624)) ;
#76427=CARTESIAN_POINT('Ctrl Pts',(-1.35715515810585,-0.175923801053208,
6.33539451712114)) ;
#76428=CARTESIAN_POINT('Ctrl Pts',(-1.44171628055285,0.383734652831137,
6.33548203852068)) ;
#76429=CARTESIAN_POINT('Ctrl Pts',(-1.33636524997174,0.791226364481497,
6.33543138977132)) ;
#76430=CARTESIAN_POINT('Ctrl Pts',(-0.836647006099026,1.44451988146956,
6.33553163726836)) ;
#76431=CARTESIAN_POINT('Ctrl Pts',(-0.429590154010006,1.67667510461985,
6.3354782063715)) ;
#76432=CARTESIAN_POINT('Ctrl Pts',(0.198582828796795,1.75115739905097,6.33553659953948)) ;
#76433=CARTESIAN_POINT('Ctrl Pts',(0.401406734790799,1.74183016014963,6.33550804006764)) ;
#76434=CARTESIAN_POINT('Ctrl Pts',(0.596911211671376,1.69935525494279,6.33551075406924)) ;
#76435=CARTESIAN_POINT('Ctrl Pts',(-1.21215577023931,-0.504706728862282,
6.34487726987667)) ;
#76436=CARTESIAN_POINT('Ctrl Pts',(-1.30846683220268,-0.352463959114778,
6.34488305795696)) ;
#76437=CARTESIAN_POINT('Ctrl Pts',(-1.37224255462146,-0.180350962994336,
6.34489495668493)) ;
#76438=CARTESIAN_POINT('Ctrl Pts',(-1.45778550015873,0.385929272949004,
6.34492679187801)) ;
#76439=CARTESIAN_POINT('Ctrl Pts',(-1.3512559606378,0.797418860642494,6.34490852424714)) ;
#76440=CARTESIAN_POINT('Ctrl Pts',(-0.846299872573819,1.45757218278905,
6.34494501369235)) ;
#76441=CARTESIAN_POINT('Ctrl Pts',(-0.435532263532225,1.69162660148109,
6.34492573960143)) ;
#76442=CARTESIAN_POINT('Ctrl Pts',(0.198561637302729,1.76680713847606,6.34494698214462)) ;
#76443=CARTESIAN_POINT('Ctrl Pts',(0.403018497435118,1.75737616029807,6.34493664202809)) ;
#76444=CARTESIAN_POINT('Ctrl Pts',(0.600209236713373,1.71453384471607,6.34493762678056)) ;
#76445=CARTESIAN_POINT('Ctrl Pts',(-1.22757973634767,-0.514459810923294,
6.35000000399322)) ;
#76446=CARTESIAN_POINT('Ctrl Pts',(-1.3252389028925,-0.360066440752681,
6.34999995101887)) ;
#76447=CARTESIAN_POINT('Ctrl Pts',(-1.38989146862233,-0.185526310309135,
6.34999987913905)) ;
#76448=CARTESIAN_POINT('Ctrl Pts',(-1.47656546565633,0.388502446092232,
6.34999966194095)) ;
#76449=CARTESIAN_POINT('Ctrl Pts',(-1.36866779698095,0.804666226495404,
6.34999994431863)) ;
#76450=CARTESIAN_POINT('Ctrl Pts',(-0.857572260759232,1.47282532997322,
6.34999973263467)) ;
#76451=CARTESIAN_POINT('Ctrl Pts',(-0.442476950791247,1.70910146559139,
6.35000002494746)) ;
#76452=CARTESIAN_POINT('Ctrl Pts',(0.198536630827523,1.78508389827109,6.34999989493859)) ;
#76453=CARTESIAN_POINT('Ctrl Pts',(0.404900148830056,1.7755363105867,6.35000001032902)) ;
#76454=CARTESIAN_POINT('Ctrl Pts',(0.604061670832201,1.73226400636545,6.35000000159026)) ;
#76455=CARTESIAN_POINT('Ctrl Pts',(-1.24302441939919,-0.524226019081257,
6.35)) ;
#76456=CARTESIAN_POINT('Ctrl Pts',(-1.34203370677612,-0.367678700862383,
6.35000000000002)) ;
#76457=CARTESIAN_POINT('Ctrl Pts',(-1.40756443263931,-0.190707970016344,
6.35000000000006)) ;
#76458=CARTESIAN_POINT('Ctrl Pts',(-1.49537112857496,0.391080480273729,
6.35000000000016)) ;
#76459=CARTESIAN_POINT('Ctrl Pts',(-1.38610400991126,0.81192437938103,6.35000000000003)) ;
#76460=CARTESIAN_POINT('Ctrl Pts',(-0.868860233572473,1.48809999932316,
6.35000000000013)) ;
#76461=CARTESIAN_POINT('Ctrl Pts',(-0.449431916290035,1.72660012548333,
6.34999999999999)) ;
#76462=CARTESIAN_POINT('Ctrl Pts',(0.198511164967717,1.80338490120432,6.35000000000006)) ;
#76463=CARTESIAN_POINT('Ctrl Pts',(0.406783902157189,1.7937204004824,6.35)) ;
#76464=CARTESIAN_POINT('Ctrl Pts',(0.607919164074007,1.75001745175322,6.35)) ;
#76465=CARTESIAN_POINT('',(-1.25119325853947,-0.511138653598631,6.35000000000021)) ;
#76466=CARTESIAN_POINT('',(-1.20400491191847,-0.491561463064185,6.33635925836751)) ;
#76467=CARTESIAN_POINT('Ctrl Pts',(-1.25036088004395,-0.512489623160576,
6.35000000000042)) ;
#76468=CARTESIAN_POINT('Ctrl Pts',(-1.24997941519213,-0.512351401822971,
6.35000000000042)) ;
#76469=CARTESIAN_POINT('Ctrl Pts',(-1.2495980855261,-0.512212821605165,
6.34999757998896)) ;
#76470=CARTESIAN_POINT('Ctrl Pts',(-1.24126534039648,-0.509175370306275,
6.34989186587608)) ;
#76471=CARTESIAN_POINT('Ctrl Pts',(-1.23339061866593,-0.506113476122858,
6.34874097096721)) ;
#76472=CARTESIAN_POINT('Ctrl Pts',(-1.2169454739642,-0.499124478633754,
6.34401101135452)) ;
#76473=CARTESIAN_POINT('Ctrl Pts',(-1.20962851798745,-0.495529127664985,
6.34035540742519)) ;
#76474=CARTESIAN_POINT('Ctrl Pts',(-1.20344341232604,-0.492722585888641,
6.33644055435381)) ;
#76475=CARTESIAN_POINT('',(0.607919162256355,1.75001744338779,6.35)) ;
#76476=CARTESIAN_POINT('Ctrl Pts',(-1.25202563703499,-0.509787684036685,
6.35)) ;
#76477=CARTESIAN_POINT('Ctrl Pts',(-1.3460115207624,-0.356834498649399,
6.35)) ;
#76478=CARTESIAN_POINT('Ctrl Pts',(-1.4084112566866,-0.185097036772204,
6.35)) ;
#76479=CARTESIAN_POINT('Ctrl Pts',(-1.49537111971372,0.391080479058958,
6.35)) ;
#76480=CARTESIAN_POINT('Ctrl Pts',(-1.38610400169531,0.811924375960986,
6.35)) ;
#76481=CARTESIAN_POINT('Ctrl Pts',(-0.868860228253576,1.48809999212573,
6.35)) ;
#76482=CARTESIAN_POINT('Ctrl Pts',(-0.449431913012853,1.72660011723795,
6.35)) ;
#76483=CARTESIAN_POINT('Ctrl Pts',(0.198511164979717,1.80338489258088,6.35000000000001)) ;
#76484=CARTESIAN_POINT('Ctrl Pts',(0.406783901269564,1.79372039191405,6.35)) ;
#76485=CARTESIAN_POINT('Ctrl Pts',(0.607919162256355,1.75001744338779,6.35)) ;
#76486=CARTESIAN_POINT('',(0.594304716461005,1.70160433312498,6.33648831456159)) ;
#76487=CARTESIAN_POINT('Ctrl Pts',(0.60791916225634,1.75001744338779,6.35)) ;
#76488=CARTESIAN_POINT('Ctrl Pts',(0.604753665677747,1.74176297877533,6.35)) ;
#76489=CARTESIAN_POINT('Ctrl Pts',(0.602355935083414,1.7333216626848,6.34883057893477)) ;
#76490=CARTESIAN_POINT('Ctrl Pts',(0.60025191269834,1.72507625378891,6.34654040403937)) ;
#76491=CARTESIAN_POINT('Ctrl Pts',(0.598158805400061,1.71687361979617,6.34426210993854)) ;
#76492=CARTESIAN_POINT('Ctrl Pts',(0.596356014106384,1.70891213133337,6.34088508516807)) ;
#76493=CARTESIAN_POINT('Ctrl Pts',(0.594304466751201,1.70160440748,6.3364883075039)) ;
#76494=CARTESIAN_POINT('',(0.19398202776272,1.74176856709214,6.33644353759349)) ;
#76495=CARTESIAN_POINT('Origin',(0.16425687912765,-0.0151938657249959,6.33858452768918)) ;
#76496=CARTESIAN_POINT('',(-4.4909026429235E-6,1.72916360454791,6.3364693018353)) ;
#76497=CARTESIAN_POINT('Origin',(0.213889544320394,-0.0749718660965196,
6.33467644420639)) ;
#76498=CARTESIAN_POINT('',(-1.10119630440643,1.10117706072883,6.33647087602767)) ;
#76499=CARTESIAN_POINT('Ctrl Pts',(-4.4909026429235E-6,1.72916360454791,
6.3364693018353)) ;
#76500=CARTESIAN_POINT('Ctrl Pts',(-0.0665061084793492,1.72124714308604,
6.33650496012767)) ;
#76501=CARTESIAN_POINT('Ctrl Pts',(-0.132510009690253,1.70920342784116,
6.33651427418665)) ;
#76502=CARTESIAN_POINT('Ctrl Pts',(-0.263070109646108,1.67694172545347,
6.33650910196814)) ;
#76503=CARTESIAN_POINT('Ctrl Pts',(-0.327610814596463,1.6566587125351,6.33649450722964)) ;
#76504=CARTESIAN_POINT('Ctrl Pts',(-0.452410105447889,1.60873680599921,
6.33646432848932)) ;
#76505=CARTESIAN_POINT('Ctrl Pts',(-0.512730304175064,1.58126016034659,
6.33644883463083)) ;
#76506=CARTESIAN_POINT('Ctrl Pts',(-0.626197844265137,1.52099206858123,
6.33642982252685)) ;
#76507=CARTESIAN_POINT('Ctrl Pts',(-0.679558438269731,1.48860977014624,
6.33642565469618)) ;
#76508=CARTESIAN_POINT('Ctrl Pts',(-0.780540073139769,1.41911622837787,
6.33642910803844)) ;
#76509=CARTESIAN_POINT('Ctrl Pts',(-0.828293287848511,1.38219980328802,
6.33643632858415)) ;
#76510=CARTESIAN_POINT('Ctrl Pts',(-0.917251046616824,1.30518172810159,
6.33645463390669)) ;
#76511=CARTESIAN_POINT('Ctrl Pts',(-0.958658491361404,1.26531484067809,
6.33646547200062)) ;
#76512=CARTESIAN_POINT('Ctrl Pts',(-1.03416386990157,1.18449355631453,6.33647786812632)) ;
#76513=CARTESIAN_POINT('Ctrl Pts',(-1.06857292586319,1.14382378089233,6.33647997034051)) ;
#76514=CARTESIAN_POINT('Ctrl Pts',(-1.10097095202783,1.10147182646993,6.33647094593189)) ;
#76515=CARTESIAN_POINT('Ctrl Pts',(-1.10108364246668,1.10132445464862,6.33647091226235)) ;
#76516=CARTESIAN_POINT('Ctrl Pts',(-1.1011963026744,1.10117706299481,6.33647087602822)) ;
#76517=CARTESIAN_POINT('',(-1.3852993521282,-4.08688681438726E-6,6.33637672541782)) ;
#76518=CARTESIAN_POINT('Ctrl Pts',(-1.10119630613845,1.10117705846285,6.33647087602712)) ;
#76519=CARTESIAN_POINT('Ctrl Pts',(-1.13938277645153,1.051218319285,6.33645864387353)) ;
#76520=CARTESIAN_POINT('Ctrl Pts',(-1.17431132247377,0.998818901911678,
6.33643471829354)) ;
#76521=CARTESIAN_POINT('Ctrl Pts',(-1.23721697009887,0.889841017732942,
6.33638704294256)) ;
#76522=CARTESIAN_POINT('Ctrl Pts',(-1.26517422524756,0.833250534509621,
6.33636340531505)) ;
#76523=CARTESIAN_POINT('Ctrl Pts',(-1.31279727825361,0.718791029418644,
6.3363325975561)) ;
#76524=CARTESIAN_POINT('Ctrl Pts',(-1.33269939463148,0.661020067748072,
6.33632499965946)) ;
#76525=CARTESIAN_POINT('Ctrl Pts',(-1.36402855946461,0.54744755398184,6.33632837595744)) ;
#76526=CARTESIAN_POINT('Ctrl Pts',(-1.3759424927561,0.491781944166528,6.3363381112914)) ;
#76527=CARTESIAN_POINT('Ctrl Pts',(-1.39287767449329,0.381480997714738,
6.33636606701108)) ;
#76528=CARTESIAN_POINT('Ctrl Pts',(-1.39813367468696,0.326882051026805,
6.33638395114502)) ;
#76529=CARTESIAN_POINT('Ctrl Pts',(-1.40234100536283,0.220109276797855,
6.33641137980185)) ;
#76530=CARTESIAN_POINT('Ctrl Pts',(-1.40158254582667,0.167945264364892,
6.3364212275538)) ;
#76531=CARTESIAN_POINT('Ctrl Pts',(-1.39534727997868,0.0772083222647631,
6.33641343495368)) ;
#76532=CARTESIAN_POINT('Ctrl Pts',(-1.39110922614765,0.0385255715080943,
6.33640201154189)) ;
#76533=CARTESIAN_POINT('Ctrl Pts',(-1.38531426391836,9.48044437915691E-5,
6.33637679031753)) ;
#76534=CARTESIAN_POINT('Ctrl Pts',(-1.38530680871705,4.53633786673787E-5,
6.3363767578705)) ;
#76535=CARTESIAN_POINT('Ctrl Pts',(-1.38529935351574,-4.07768645681171E-6,
6.33637672542347)) ;
#76536=CARTESIAN_POINT('Ctrl Pts',(-1.38529935074065,-4.09608717196282E-6,
6.33637672541216)) ;
#76537=CARTESIAN_POINT('Ctrl Pts',(-1.37604524760285,-0.0613380044097079,
6.33633667262024)) ;
#76538=CARTESIAN_POINT('Ctrl Pts',(-1.36241347430925,-0.12191631163429,
6.33631060447636)) ;
#76539=CARTESIAN_POINT('Ctrl Pts',(-1.32811348145613,-0.23561790872716,
6.33628334303435)) ;
#76540=CARTESIAN_POINT('Ctrl Pts',(-1.30810808812469,-0.288947817502873,
6.33628041020224)) ;
#76541=CARTESIAN_POINT('Ctrl Pts',(-1.26130677709146,-0.392319081970156,
6.33628196319371)) ;
#76542=CARTESIAN_POINT('Ctrl Pts',(-1.23453616146347,-0.442372792708542,
6.33628658201929)) ;
#76543=CARTESIAN_POINT('Ctrl Pts',(-1.20454071887332,-0.490453469945117,
6.33628168225624)) ;
#76544=CARTESIAN_POINT('Origin',(0.,0.,6.25)) ;
#76545=CARTESIAN_POINT('Ctrl Pts',(1.24732203681758,1.23117606233602,6.24999999746782)) ;
#76546=CARTESIAN_POINT('Ctrl Pts',(1.18413913631208,1.29518756019404,6.25616282366101)) ;
#76547=CARTESIAN_POINT('Ctrl Pts',(1.11684156410954,1.35433254331176,6.26273026309037)) ;
#76548=CARTESIAN_POINT('Ctrl Pts',(0.99465531308325,1.44818563488623,6.27524755812259)) ;
#76549=CARTESIAN_POINT('Ctrl Pts',(0.942382820096697,1.48454101942919,6.28074455832599)) ;
#76550=CARTESIAN_POINT('Ctrl Pts',(0.830300417999892,1.5558341017124,6.29330561895835)) ;
#76551=CARTESIAN_POINT('Ctrl Pts',(0.771237474584706,1.58951246918406,6.30027618346742)) ;
#76552=CARTESIAN_POINT('Ctrl Pts',(0.679530090341938,1.64018276569364,6.31325056551678)) ;
#76553=CARTESIAN_POINT('Ctrl Pts',(0.648785354293156,1.65688362190668,6.31827793155166)) ;
#76554=CARTESIAN_POINT('Ctrl Pts',(0.617263445317367,1.67664530547039,6.32521291659261)) ;
#76555=CARTESIAN_POINT('Ctrl Pts',(0.606958715238955,1.68359083166877,6.32782718462676)) ;
#76556=CARTESIAN_POINT('Ctrl Pts',(0.598340879348292,1.69193026794475,6.33148558224764)) ;
#76557=CARTESIAN_POINT('Ctrl Pts',(0.596313784588478,1.69425091096469,6.33255389399815)) ;
#76558=CARTESIAN_POINT('Ctrl Pts',(0.594687442078795,1.69738144367564,6.33413367934689)) ;
#76559=CARTESIAN_POINT('Ctrl Pts',(0.594327845458634,1.69831237814393,6.33461894425858)) ;
#76560=CARTESIAN_POINT('Ctrl Pts',(0.594048306100336,1.70005354271567,6.33557488964638)) ;
#76561=CARTESIAN_POINT('Ctrl Pts',(0.594073405242955,1.70083850204704,6.33602442146924)) ;
#76562=CARTESIAN_POINT('Ctrl Pts',(0.594304965275971,1.70160425498376,6.33648831934986)) ;
#76563=CARTESIAN_POINT('',(1.65743956651353,-0.827659859698077,6.35)) ;
#76564=CARTESIAN_POINT('Origin',(0.,0.,6.35)) ;
#76565=CARTESIAN_POINT('Ctrl Pts',(1.65743956651353,-0.827659859698078,
6.35)) ;
#76566=CARTESIAN_POINT('Ctrl Pts',(1.65708852425179,-0.827457333128657,
6.35)) ;
#76567=CARTESIAN_POINT('Ctrl Pts',(1.65673746283553,-0.827254793665606,
6.34999757623592)) ;
#76568=CARTESIAN_POINT('Ctrl Pts',(1.65638640318299,-0.827052253325088,
6.34999273010545)) ;
#76569=CARTESIAN_POINT('Ctrl Pts',(1.64951073718717,-0.823085406887498,
6.3498978163941)) ;
#76570=CARTESIAN_POINT('Ctrl Pts',(1.64267636638568,-0.819141560396678,
6.34887859204913)) ;
#76571=CARTESIAN_POINT('Ctrl Pts',(1.63603787271552,-0.815310093330816,
6.34695079806314)) ;
#76572=CARTESIAN_POINT('Ctrl Pts',(1.63254991824201,-0.813296988648264,
6.34593790899651)) ;
#76573=CARTESIAN_POINT('Ctrl Pts',(1.62911592055215,-0.811314902311204,
6.34467332331189)) ;
#76574=CARTESIAN_POINT('Ctrl Pts',(1.62575902753902,-0.809378263250201,
6.34315366875848)) ;
#76575=CARTESIAN_POINT('Ctrl Pts',(1.62494337864994,-0.808907703869104,
6.34278442715815)) ;
#76576=CARTESIAN_POINT('Ctrl Pts',(1.62413229353693,-0.808439840243547,
6.34240011167817)) ;
#76577=CARTESIAN_POINT('Ctrl Pts',(1.62332600671688,-0.807974803235035,
6.34200093725414)) ;
#76578=CARTESIAN_POINT('Ctrl Pts',(1.61699826737659,-0.804325192575065,
6.33886821618793)) ;
#76579=CARTESIAN_POINT('Ctrl Pts',(1.61103685589427,-0.800890447046913,
6.33486039023559)) ;
#76580=CARTESIAN_POINT('Ctrl Pts',(1.60554240364908,-0.797722810935053,
6.33011214573865)) ;
#76581=CARTESIAN_POINT('Ctrl Pts',(1.6020280918537,-0.795696756206643,6.32707511658664)) ;
#76582=CARTESIAN_POINT('Ctrl Pts',(1.59870513294145,-0.79378006756951,6.32373401573313)) ;
#76583=CARTESIAN_POINT('Ctrl Pts',(1.5956055098213,-0.791990624580966,6.32011539552532)) ;
#76584=CARTESIAN_POINT('Ctrl Pts',(1.59077222390879,-0.789200320969043,
6.31447283015682)) ;
#76585=CARTESIAN_POINT('Ctrl Pts',(1.5865365972947,-0.786749991588918,6.30822233253495)) ;
#76586=CARTESIAN_POINT('Ctrl Pts',(1.5830020225687,-0.784706540691024,6.3014789531298)) ;
#76587=CARTESIAN_POINT('Ctrl Pts',(1.58165450135156,-0.78392749550042,6.29890810726343)) ;
#76588=CARTESIAN_POINT('Ctrl Pts',(1.58040913941073,-0.783207875063578,
6.29626524041211)) ;
#76589=CARTESIAN_POINT('Ctrl Pts',(1.57927293875872,-0.782552610644341,
6.29355567099931)) ;
#76590=CARTESIAN_POINT('Ctrl Pts',(1.57850015058202,-0.782106931797997,
6.29171275425527)) ;
#76591=CARTESIAN_POINT('Ctrl Pts',(1.57777789040688,-0.781691051893247,
6.28983899945262)) ;
#76592=CARTESIAN_POINT('Ctrl Pts',(1.57710659769393,-0.781304970163598,
6.28793731545109)) ;
#76593=CARTESIAN_POINT('Ctrl Pts',(1.57451220409407,-0.779812852121637,
6.28058773946527)) ;
#76594=CARTESIAN_POINT('Ctrl Pts',(1.57270609928185,-0.778780519248468,
6.2729080946375)) ;
#76595=CARTESIAN_POINT('Ctrl Pts',(1.57168491163117,-0.778195616556964,
6.26507674204093)) ;
#76596=CARTESIAN_POINT('Ctrl Pts',(1.57103619973019,-0.777824055721258,
6.26010185654672)) ;
#76597=CARTESIAN_POINT('Ctrl Pts',(1.57070507101749,-0.77763367306192,6.25506517605237)) ;
#76598=CARTESIAN_POINT('Ctrl Pts',(1.57069890812158,-0.777628441215486,
6.25001120443579)) ;
#76599=CARTESIAN_POINT('Ctrl Pts',(1.61549606864524,-0.799973712389905,
6.16354642763013)) ;
#76600=CARTESIAN_POINT('Ctrl Pts',(1.50866006753038,-0.961820010632383,
6.16354845333704)) ;
#76601=CARTESIAN_POINT('Ctrl Pts',(1.37608293211674,-1.10532255898405,6.16354532462513)) ;
#76602=CARTESIAN_POINT('Ctrl Pts',(0.883476931069763,-1.4943581457905,6.163531510563)) ;
#76603=CARTESIAN_POINT('Ctrl Pts',(0.43189736308726,-1.61774218765324,6.16360457949385)) ;
#76604=CARTESIAN_POINT('Ctrl Pts',(-0.387735196455891,-1.50955658539216,
6.16357104016601)) ;
#76605=CARTESIAN_POINT('Ctrl Pts',(-0.749793159276284,-1.2953985605636,
6.16366106980508)) ;
#76606=CARTESIAN_POINT('Ctrl Pts',(-1.1629753731845,-0.736642926916648,
6.16361636307964)) ;
#76607=CARTESIAN_POINT('Ctrl Pts',(-1.25283238131601,-0.42534079606347,
6.16372466795802)) ;
#76608=CARTESIAN_POINT('Ctrl Pts',(-1.23093886224037,-0.123053381526151,
6.16370469001445)) ;
#76609=CARTESIAN_POINT('Ctrl Pts',(1.59752029062636,-0.788108225162961,
6.1760668526113)) ;
#76610=CARTESIAN_POINT('Ctrl Pts',(1.49196189973369,-0.948020502054166,
6.17606956401923)) ;
#76611=CARTESIAN_POINT('Ctrl Pts',(1.3609705278398,-1.08981355145533,6.17606534815012)) ;
#76612=CARTESIAN_POINT('Ctrl Pts',(0.87434993641677,-1.47414249680429,6.17604676793019)) ;
#76613=CARTESIAN_POINT('Ctrl Pts',(0.429056350360505,-1.59568033539221,
6.17614438922054)) ;
#76614=CARTESIAN_POINT('Ctrl Pts',(-0.379620525679053,-1.48898582643579,
6.17609935232033)) ;
#76615=CARTESIAN_POINT('Ctrl Pts',(-0.735908001637101,-1.27801942757034,
6.17621960211951)) ;
#76616=CARTESIAN_POINT('Ctrl Pts',(-1.14294046129122,-0.727613085333748,
6.17615971202283)) ;
#76617=CARTESIAN_POINT('Ctrl Pts',(-1.23105598826309,-0.421830171326285,
6.17630424830084)) ;
#76618=CARTESIAN_POINT('Ctrl Pts',(-1.20952162058803,-0.124606974019317,
6.1762775805103)) ;
#76619=CARTESIAN_POINT('Ctrl Pts',(1.5698483850616,-0.769842498823944,6.21788308551004)) ;
#76620=CARTESIAN_POINT('Ctrl Pts',(1.46625562510329,-0.926780606179969,
6.21788619683742)) ;
#76621=CARTESIAN_POINT('Ctrl Pts',(1.33770404860818,-1.06594373674671,6.21788139808894)) ;
#76622=CARTESIAN_POINT('Ctrl Pts',(0.860292194298888,-1.44302923241305,
6.21786016739722)) ;
#76623=CARTESIAN_POINT('Ctrl Pts',(0.424681867511836,-1.56175458111409,
6.21797238130401)) ;
#76624=CARTESIAN_POINT('Ctrl Pts',(-0.367140476130573,-1.45734375378515,
6.21792091065796)) ;
#76625=CARTESIAN_POINT('Ctrl Pts',(-0.714565467179568,-1.25131365505249,
6.21805897503878)) ;
#76626=CARTESIAN_POINT('Ctrl Pts',(-1.11212916749052,-0.713731553118314,
6.21799049458104)) ;
#76627=CARTESIAN_POINT('Ctrl Pts',(-1.19759938063696,-0.416441940029509,
6.21815621890648)) ;
#76628=CARTESIAN_POINT('Ctrl Pts',(-1.17660907946778,-0.126994427905559,
6.21812569329284)) ;
#76629=CARTESIAN_POINT('Ctrl Pts',(1.57493624982465,-0.773200906693405,
6.29781698992439)) ;
#76630=CARTESIAN_POINT('Ctrl Pts',(1.47098173367402,-0.930690200837764,
6.29781856153337)) ;
#76631=CARTESIAN_POINT('Ctrl Pts',(1.34197704834607,-1.07033809638994,6.29781612216889)) ;
#76632=CARTESIAN_POINT('Ctrl Pts',(0.862860470622287,-1.44875060656876,
6.29780535264256)) ;
#76633=CARTESIAN_POINT('Ctrl Pts',(0.425481538277075,-1.56806968519663,
6.29786194185147)) ;
#76634=CARTESIAN_POINT('Ctrl Pts',(-0.369463134207585,-1.46320470671826,
6.2978358625339)) ;
#76635=CARTESIAN_POINT('Ctrl Pts',(-0.718577475421128,-1.25633176165636,
6.29790549425836)) ;
#76636=CARTESIAN_POINT('Ctrl Pts',(-1.11787505857057,-0.716322512675761,
6.29787085558639)) ;
#76637=CARTESIAN_POINT('Ctrl Pts',(-1.20393830023574,-0.417466203903967,
6.29795441514621)) ;
#76638=CARTESIAN_POINT('Ctrl Pts',(-1.18282403856848,-0.126543598897747,
6.29793901542275)) ;
#76639=CARTESIAN_POINT('Ctrl Pts',(1.61581214044334,-0.800182345689632,
6.34311290859866)) ;
#76640=CARTESIAN_POINT('Ctrl Pts',(1.50895784490124,-0.962064092159509,
6.34311311389927)) ;
#76641=CARTESIAN_POINT('Ctrl Pts',(1.37634244782511,-1.10559303782759,6.34311280868517)) ;
#76642=CARTESIAN_POINT('Ctrl Pts',(0.883613373539448,-1.49468359196346,
6.34311143808909)) ;
#76643=CARTESIAN_POINT('Ctrl Pts',(0.431936536099549,-1.61824483101601,
6.34311890585529)) ;
#76644=CARTESIAN_POINT('Ctrl Pts',(-0.387923824817847,-1.50996073963872,
6.34311556995257)) ;
#76645=CARTESIAN_POINT('Ctrl Pts',(-0.750207415867593,-1.29587835204616,
6.34312473370235)) ;
#76646=CARTESIAN_POINT('Ctrl Pts',(-1.16347886666241,-0.736854773631983,
6.34312026707438)) ;
#76647=CARTESIAN_POINT('Ctrl Pts',(-1.25359438063852,-0.425451420865333,
6.34313124490448)) ;
#76648=CARTESIAN_POINT('Ctrl Pts',(-1.23164727574712,-0.123001993680601,
6.3431292332343)) ;
#76649=CARTESIAN_POINT('Ctrl Pts',(1.64705017975234,-0.820802012667411,
6.35000039278962)) ;
#76650=CARTESIAN_POINT('Ctrl Pts',(1.53797666056991,-0.986044738024822,
6.35000039841076)) ;
#76651=CARTESIAN_POINT('Ctrl Pts',(1.40260339195363,-1.13254350570539,6.35000037441355)) ;
#76652=CARTESIAN_POINT('Ctrl Pts',(0.899469482201931,-1.52980706906964,
6.35000029469085)) ;
#76653=CARTESIAN_POINT('Ctrl Pts',(0.436871148542969,-1.6566054637442,6.3500004112916)) ;
#76654=CARTESIAN_POINT('Ctrl Pts',(-0.402034709739736,-1.54571554501082,
6.3500002375136)) ;
#76655=CARTESIAN_POINT('Ctrl Pts',(-0.774371464292586,-1.32611335453818,
6.35000040938403)) ;
#76656=CARTESIAN_POINT('Ctrl Pts',(-1.19832606513914,-0.752556628717804,
6.35000021947629)) ;
#76657=CARTESIAN_POINT('Ctrl Pts',(-1.29151446365418,-0.431561348191218,
6.3500004467796)) ;
#76658=CARTESIAN_POINT('Ctrl Pts',(-1.2689337108479,-0.120297260428306,
6.35000039185858)) ;
#76659=CARTESIAN_POINT('Ctrl Pts',(1.65744223319009,-0.82766161992323,6.3499999999496)) ;
#76660=CARTESIAN_POINT('Ctrl Pts',(1.54763268784084,-0.994019054114616,
6.34999999994815)) ;
#76661=CARTESIAN_POINT('Ctrl Pts',(1.41134138578638,-1.14150297307001,6.34999999995431)) ;
#76662=CARTESIAN_POINT('Ctrl Pts',(0.904748656557809,-1.5414771327564,6.34999999997478)) ;
#76663=CARTESIAN_POINT('Ctrl Pts',(0.438512116572987,-1.66934757026883,
6.34999999994481)) ;
#76664=CARTESIAN_POINT('Ctrl Pts',(-0.406724020702625,-1.55758946118512,
6.34999999998944)) ;
#76665=CARTESIAN_POINT('Ctrl Pts',(-0.782406486305098,-1.33615118986062,
6.34999999994525)) ;
#76666=CARTESIAN_POINT('Ctrl Pts',(-1.20991300026391,-0.757768547394265,
6.34999999999403)) ;
#76667=CARTESIAN_POINT('Ctrl Pts',(-1.30412899404698,-0.433585113928121,
6.34999999993561)) ;
#76668=CARTESIAN_POINT('Ctrl Pts',(-1.28133803060964,-0.119397459306505,
6.34999999994972)) ;
#76669=CARTESIAN_POINT('Ctrl Pts',(-1.1832560635873,-0.36080960203242,6.28787103703615)) ;
#76670=CARTESIAN_POINT('Ctrl Pts',(-1.18290594752794,-0.38604397996115,
6.29445533087948)) ;
#76671=CARTESIAN_POINT('Ctrl Pts',(-1.18269642318132,-0.415843789426796,
6.30282243761288)) ;
#76672=CARTESIAN_POINT('Ctrl Pts',(-1.18596333720351,-0.454630048457181,
6.31600036209296)) ;
#76673=CARTESIAN_POINT('Ctrl Pts',(-1.18798952321357,-0.467363137142688,
6.32090935151571)) ;
#76674=CARTESIAN_POINT('Ctrl Pts',(-1.19281338362405,-0.480676013117452,
6.32741836869324)) ;
#76675=CARTESIAN_POINT('Ctrl Pts',(-1.19465667987756,-0.484582846773843,
6.32954668642152)) ;
#76676=CARTESIAN_POINT('Ctrl Pts',(-1.19814970936632,-0.488952031482846,
6.33263966472036)) ;
#76677=CARTESIAN_POINT('Ctrl Pts',(-1.19930907268144,-0.490123758409715,
6.33357989117064)) ;
#76678=CARTESIAN_POINT('Ctrl Pts',(-1.20150568184695,-0.491744394553401,
6.3351747366642)) ;
#76679=CARTESIAN_POINT('Ctrl Pts',(-1.20245370818922,-0.492297942372149,
6.33581763637434)) ;
#76680=CARTESIAN_POINT('Ctrl Pts',(-1.20346579048344,-0.492729032924015,
6.33645424047249)) ;
#76681=CARTESIAN_POINT('',(-0.981372199195172,-0.981394101666046,6.16407961983129)) ;
#76682=CARTESIAN_POINT('Ctrl Pts',(-1.23064526020309,-0.123127494296425,
6.16388000977423)) ;
#76683=CARTESIAN_POINT('Ctrl Pts',(-1.25250788324639,-0.425166570526641,
6.16390005359003)) ;
#76684=CARTESIAN_POINT('Ctrl Pts',(-1.16278265791006,-0.736199040603134,
6.1637913874525)) ;
#76685=CARTESIAN_POINT('Ctrl Pts',(-0.981532123342657,-0.981510743966889,
6.16381096867958)) ;
#76686=CARTESIAN_POINT('',(-6.49131666398584E-5,-1.5604080583864,6.16377232746739)) ;
#76687=CARTESIAN_POINT('Ctrl Pts',(-0.981288525738987,-0.981332430047466,
6.16398951297446)) ;
#76688=CARTESIAN_POINT('Ctrl Pts',(-0.981191603913097,-0.981463607802477,
6.16398952349692)) ;
#76689=CARTESIAN_POINT('Ctrl Pts',(-0.98109465590878,-0.981594766764438,
6.16398953405623)) ;
#76690=CARTESIAN_POINT('Ctrl Pts',(-0.74957909382456,-1.29467797482235,
6.16401483138177)) ;
#76691=CARTESIAN_POINT('Ctrl Pts',(-0.388051709564117,-1.50866049563573,
6.16392411658099)) ;
#76692=CARTESIAN_POINT('Ctrl Pts',(-2.7475723418453E-5,-1.56012574561803,
6.16393999325065)) ;
#76693=CARTESIAN_POINT('',(1.22475281344944,-1.22479663701074,6.16355881950494)) ;
#76694=CARTESIAN_POINT('Origin',(0.31156214245914,-0.314022316645595,6.16355474486492)) ;
#76695=CARTESIAN_POINT('Origin',(0.0911459276996181,0.210924778456014,6.16345720164817)) ;
#76696=CARTESIAN_POINT('Ctrl Pts',(1.65743956651353,-0.827659859698077,
6.35)) ;
#76697=CARTESIAN_POINT('Ctrl Pts',(1.54763021003401,-0.994017007846987,
6.35)) ;
#76698=CARTESIAN_POINT('Ctrl Pts',(1.41133914355359,-1.14150067400533,6.35)) ;
#76699=CARTESIAN_POINT('Ctrl Pts',(0.904747301883336,-1.54147413813279,
6.35)) ;
#76700=CARTESIAN_POINT('Ctrl Pts',(0.438511695488632,-1.66934430055112,
6.35)) ;
#76701=CARTESIAN_POINT('Ctrl Pts',(-0.406722817391188,-1.55758641425134,
6.35000000000001)) ;
#76702=CARTESIAN_POINT('Ctrl Pts',(-0.782404424459881,-1.33614861407856,
6.35)) ;
#76703=CARTESIAN_POINT('Ctrl Pts',(-1.13178243085231,-0.863467693146003,
6.35000000000001)) ;
#76704=CARTESIAN_POINT('Ctrl Pts',(-1.20953277971566,-0.691197369173528,
6.35)) ;
#76705=CARTESIAN_POINT('Ctrl Pts',(-1.25070895267785,-0.510968789729886,
6.35)) ;
#76706=CARTESIAN_POINT('Ctrl Pts',(0.,4.49979483821861,1.58609367936188)) ;
#76707=CARTESIAN_POINT('Ctrl Pts',(-1.8638760498866,4.49979483821861,1.63570305436188)) ;
#76708=CARTESIAN_POINT('Ctrl Pts',(-3.1818354440526,3.1818354440526,1.68531242936188)) ;
#76709=CARTESIAN_POINT('Ctrl Pts',(-4.49979483821861,1.8638760498866,1.73492180436188)) ;
#76710=CARTESIAN_POINT('Ctrl Pts',(-4.49979483821861,2.7553296727221E-16,
1.78453117936188)) ;
#76711=CARTESIAN_POINT('Ctrl Pts',(-4.49979483821861,-1.8638760498866,1.83414055436188)) ;
#76712=CARTESIAN_POINT('Ctrl Pts',(-3.1818354440526,-3.1818354440526,1.88374992936188)) ;
#76713=CARTESIAN_POINT('Ctrl Pts',(-1.8638760498866,-4.49979483821861,1.93335930436188)) ;
#76714=CARTESIAN_POINT('Ctrl Pts',(-5.5106593454442E-16,-4.49979483821861,
1.98296867936188)) ;
#76715=CARTESIAN_POINT('Ctrl Pts',(1.86387604988659,-4.49979483821861,2.03257805436188)) ;
#76716=CARTESIAN_POINT('Ctrl Pts',(3.1818354440526,-3.18183544405261,2.08218742936188)) ;
#76717=CARTESIAN_POINT('Ctrl Pts',(4.49979483821861,-1.8638760498866,2.13179680436188)) ;
#76718=CARTESIAN_POINT('Ctrl Pts',(4.49979483821861,-8.2659890181663E-16,
2.18140617936188)) ;
#76719=CARTESIAN_POINT('Ctrl Pts',(4.49979483821861,1.8638760498866,2.23101555436188)) ;
#76720=CARTESIAN_POINT('Ctrl Pts',(3.18183544405261,3.1818354440526,2.28062492936188)) ;
#76721=CARTESIAN_POINT('Ctrl Pts',(1.8638760498866,4.49979483821861,2.33023430436188)) ;
#76722=CARTESIAN_POINT('Ctrl Pts',(0.,4.49979483821861,2.37984367936188)) ;
#76723=CARTESIAN_POINT('Ctrl Pts',(-1.8638760498866,4.49979483821861,2.42945305436188)) ;
#76724=CARTESIAN_POINT('Ctrl Pts',(-3.1818354440526,3.1818354440526,2.47906242936188)) ;
#76725=CARTESIAN_POINT('Ctrl Pts',(-4.49979483821861,1.8638760498866,2.52867180436188)) ;
#76726=CARTESIAN_POINT('Ctrl Pts',(-4.49979483821861,2.7553296727221E-16,
2.57828117936188)) ;
#76727=CARTESIAN_POINT('Ctrl Pts',(-4.49979483821861,-1.8638760498866,2.62789055436188)) ;
#76728=CARTESIAN_POINT('Ctrl Pts',(-3.1818354440526,-3.1818354440526,2.67749992936188)) ;
#76729=CARTESIAN_POINT('Ctrl Pts',(-1.8638760498866,-4.49979483821861,2.72710930436188)) ;
#76730=CARTESIAN_POINT('Ctrl Pts',(-5.5106593454442E-16,-4.49979483821861,
2.77671867936188)) ;
#76731=CARTESIAN_POINT('Ctrl Pts',(1.86387604988659,-4.49979483821861,2.82632805436188)) ;
#76732=CARTESIAN_POINT('Ctrl Pts',(3.1818354440526,-3.18183544405261,2.87593742936188)) ;
#76733=CARTESIAN_POINT('Ctrl Pts',(4.49979483821861,-1.8638760498866,2.92554680436188)) ;
#76734=CARTESIAN_POINT('Ctrl Pts',(4.49979483821861,-8.2659890181663E-16,
2.97515617936187)) ;
#76735=CARTESIAN_POINT('Ctrl Pts',(4.49979483821861,1.8638760498866,3.02476555436188)) ;
#76736=CARTESIAN_POINT('Ctrl Pts',(3.18183544405261,3.1818354440526,3.07437492936188)) ;
#76737=CARTESIAN_POINT('Ctrl Pts',(1.8638760498866,4.49979483821861,3.12398430436187)) ;
#76738=CARTESIAN_POINT('Ctrl Pts',(0.,4.49979483821861,3.17359367936188)) ;
#76739=CARTESIAN_POINT('Ctrl Pts',(-1.8638760498866,4.49979483821861,3.22320305436188)) ;
#76740=CARTESIAN_POINT('Ctrl Pts',(-3.1818354440526,3.1818354440526,3.27281242936188)) ;
#76741=CARTESIAN_POINT('Ctrl Pts',(-4.49979483821861,1.8638760498866,3.32242180436188)) ;
#76742=CARTESIAN_POINT('Ctrl Pts',(-4.49979483821861,2.7553296727221E-16,
3.37203117936187)) ;
#76743=CARTESIAN_POINT('Ctrl Pts',(-4.49979483821861,-1.8638760498866,3.42164055436188)) ;
#76744=CARTESIAN_POINT('Ctrl Pts',(-3.1818354440526,-3.1818354440526,3.47124992936188)) ;
#76745=CARTESIAN_POINT('Ctrl Pts',(-1.8638760498866,-4.49979483821861,3.52085930436187)) ;
#76746=CARTESIAN_POINT('Ctrl Pts',(-5.5106593454442E-16,-4.49979483821861,
3.57046867936188)) ;
#76747=CARTESIAN_POINT('Ctrl Pts',(1.86387604988659,-4.49979483821861,3.62007805436187)) ;
#76748=CARTESIAN_POINT('Ctrl Pts',(3.1818354440526,-3.18183544405261,3.66968742936188)) ;
#76749=CARTESIAN_POINT('Ctrl Pts',(4.49979483821861,-1.8638760498866,3.71929680436188)) ;
#76750=CARTESIAN_POINT('Ctrl Pts',(4.49979483821861,-8.2659890181663E-16,
3.76890617936188)) ;
#76751=CARTESIAN_POINT('Ctrl Pts',(4.49979483821861,1.8638760498866,3.81851555436188)) ;
#76752=CARTESIAN_POINT('Ctrl Pts',(3.18183544405261,3.1818354440526,3.86812492936188)) ;
#76753=CARTESIAN_POINT('Ctrl Pts',(1.8638760498866,4.49979483821861,3.91773430436188)) ;
#76754=CARTESIAN_POINT('Ctrl Pts',(0.,4.49979483821861,3.96734367936188)) ;
#76755=CARTESIAN_POINT('Ctrl Pts',(-1.8638760498866,4.49979483821861,4.01695305436187)) ;
#76756=CARTESIAN_POINT('Ctrl Pts',(-3.1818354440526,3.1818354440526,4.06656242936188)) ;
#76757=CARTESIAN_POINT('Ctrl Pts',(-4.49979483821861,1.8638760498866,4.11617180436188)) ;
#76758=CARTESIAN_POINT('Ctrl Pts',(-4.49979483821861,2.7553296727221E-16,
4.16578117936188)) ;
#76759=CARTESIAN_POINT('Ctrl Pts',(-4.49979483821861,-1.8638760498866,4.21539055436187)) ;
#76760=CARTESIAN_POINT('Ctrl Pts',(-3.1818354440526,-3.1818354440526,4.26499992936188)) ;
#76761=CARTESIAN_POINT('Ctrl Pts',(-1.8638760498866,-4.49979483821861,4.31460930436188)) ;
#76762=CARTESIAN_POINT('Ctrl Pts',(-5.5106593454442E-16,-4.49979483821861,
4.36421867936188)) ;
#76763=CARTESIAN_POINT('Ctrl Pts',(1.86387604988659,-4.49979483821861,4.41382805436188)) ;
#76764=CARTESIAN_POINT('Ctrl Pts',(3.1818354440526,-3.18183544405261,4.46343742936188)) ;
#76765=CARTESIAN_POINT('Ctrl Pts',(4.49979483821861,-1.8638760498866,4.51304680436187)) ;
#76766=CARTESIAN_POINT('Ctrl Pts',(4.49979483821861,-8.2659890181663E-16,
4.56265617936188)) ;
#76767=CARTESIAN_POINT('Ctrl Pts',(4.49979483821861,1.8638760498866,4.61226555436188)) ;
#76768=CARTESIAN_POINT('Ctrl Pts',(3.18183544405261,3.1818354440526,4.66187492936188)) ;
#76769=CARTESIAN_POINT('Ctrl Pts',(1.8638760498866,4.49979483821861,4.71148430436188)) ;
#76770=CARTESIAN_POINT('Ctrl Pts',(0.,4.49979483821861,4.76109367936188)) ;
#76771=CARTESIAN_POINT('Ctrl Pts',(-1.8638760498866,4.49979483821861,4.81070305436188)) ;
#76772=CARTESIAN_POINT('Ctrl Pts',(-3.1818354440526,3.1818354440526,4.86031242936188)) ;
#76773=CARTESIAN_POINT('Ctrl Pts',(-4.49979483821861,1.8638760498866,4.90992180436188)) ;
#76774=CARTESIAN_POINT('Ctrl Pts',(-4.49979483821861,2.7553296727221E-16,
4.95953117936188)) ;
#76775=CARTESIAN_POINT('Ctrl Pts',(-4.49979483821861,-1.8638760498866,5.00914055436187)) ;
#76776=CARTESIAN_POINT('Ctrl Pts',(-3.1818354440526,-3.1818354440526,5.05874992936188)) ;
#76777=CARTESIAN_POINT('Ctrl Pts',(-1.8638760498866,-4.49979483821861,5.10835930436188)) ;
#76778=CARTESIAN_POINT('Ctrl Pts',(-5.5106593454442E-16,-4.49979483821861,
5.15796867936188)) ;
#76779=CARTESIAN_POINT('Ctrl Pts',(1.86387604988659,-4.49979483821861,5.20757805436187)) ;
#76780=CARTESIAN_POINT('Ctrl Pts',(3.1818354440526,-3.18183544405261,5.25718742936188)) ;
#76781=CARTESIAN_POINT('Ctrl Pts',(4.49979483821861,-1.8638760498866,5.30679680436188)) ;
#76782=CARTESIAN_POINT('Ctrl Pts',(4.49979483821861,-8.2659890181663E-16,
5.35640617936188)) ;
#76783=CARTESIAN_POINT('Ctrl Pts',(4.49979483821861,1.8638760498866,5.40601555436188)) ;
#76784=CARTESIAN_POINT('Ctrl Pts',(3.18183544405261,3.1818354440526,5.45562492936187)) ;
#76785=CARTESIAN_POINT('Ctrl Pts',(1.8638760498866,4.49979483821861,5.50523430436188)) ;
#76786=CARTESIAN_POINT('Ctrl Pts',(0.,4.49979483821861,5.55484367936188)) ;
#76787=CARTESIAN_POINT('Ctrl Pts',(-1.8638760498866,4.49979483821861,5.60445305436188)) ;
#76788=CARTESIAN_POINT('Ctrl Pts',(-3.1818354440526,3.1818354440526,5.65406242936188)) ;
#76789=CARTESIAN_POINT('Ctrl Pts',(-4.49979483821861,1.8638760498866,5.70367180436188)) ;
#76790=CARTESIAN_POINT('Ctrl Pts',(-4.49979483821861,2.7553296727221E-16,
5.75328117936188)) ;
#76791=CARTESIAN_POINT('Ctrl Pts',(-4.49979483821861,-1.8638760498866,5.80289055436188)) ;
#76792=CARTESIAN_POINT('Ctrl Pts',(-3.1818354440526,-3.1818354440526,5.85249992936188)) ;
#76793=CARTESIAN_POINT('Ctrl Pts',(-1.8638760498866,-4.49979483821861,5.90210930436188)) ;
#76794=CARTESIAN_POINT('Ctrl Pts',(-5.5106593454442E-16,-4.49979483821861,
5.95171867936188)) ;
#76795=CARTESIAN_POINT('Ctrl Pts',(1.86387604988659,-4.49979483821861,6.00132805436188)) ;
#76796=CARTESIAN_POINT('Ctrl Pts',(3.1818354440526,-3.18183544405261,6.05093742936188)) ;
#76797=CARTESIAN_POINT('Ctrl Pts',(4.49979483821861,-1.8638760498866,6.10054680436188)) ;
#76798=CARTESIAN_POINT('Ctrl Pts',(4.49979483821861,-8.2659890181663E-16,
6.15015617936188)) ;
#76799=CARTESIAN_POINT('Ctrl Pts',(4.49979483821861,1.8638760498866,6.19976555436188)) ;
#76800=CARTESIAN_POINT('Ctrl Pts',(3.18183544405261,3.1818354440526,6.24937492936188)) ;
#76801=CARTESIAN_POINT('Ctrl Pts',(1.8638760498866,4.49979483821861,6.29898430436187)) ;
#76802=CARTESIAN_POINT('Ctrl Pts',(0.,4.49979483821861,6.34859367936188)) ;
#76803=CARTESIAN_POINT('Ctrl Pts',(-1.8638760498866,4.49979483821861,6.39820305436188)) ;
#76804=CARTESIAN_POINT('Ctrl Pts',(-3.1818354440526,3.1818354440526,6.44781242936188)) ;
#76805=CARTESIAN_POINT('Ctrl Pts',(-4.49979483821861,1.8638760498866,6.49742180436188)) ;
#76806=CARTESIAN_POINT('Ctrl Pts',(-4.49979483821861,2.7553296727221E-16,
6.54703117936188)) ;
#76807=CARTESIAN_POINT('Ctrl Pts',(-4.49979483821861,-1.8638760498866,6.59664055436189)) ;
#76808=CARTESIAN_POINT('Ctrl Pts',(-3.1818354440526,-3.1818354440526,6.64624992936188)) ;
#76809=CARTESIAN_POINT('Ctrl Pts',(-1.8638760498866,-4.49979483821861,6.69585930436188)) ;
#76810=CARTESIAN_POINT('Ctrl Pts',(-5.5106593454442E-16,-4.49979483821861,
6.74546867936188)) ;
#76811=CARTESIAN_POINT('Ctrl Pts',(1.86387604988659,-4.49979483821861,6.79507805436187)) ;
#76812=CARTESIAN_POINT('Ctrl Pts',(3.1818354440526,-3.18183544405261,6.84468742936188)) ;
#76813=CARTESIAN_POINT('Ctrl Pts',(4.49979483821861,-1.8638760498866,6.89429680436188)) ;
#76814=CARTESIAN_POINT('Ctrl Pts',(4.49979483821861,-8.2659890181663E-16,
6.94390617936188)) ;
#76815=CARTESIAN_POINT('Ctrl Pts',(4.49979483821861,1.8638760498866,6.99351555436188)) ;
#76816=CARTESIAN_POINT('Ctrl Pts',(3.18183544405261,3.1818354440526,7.04312492936188)) ;
#76817=CARTESIAN_POINT('Ctrl Pts',(1.8638760498866,4.49979483821861,7.09273430436188)) ;
#76818=CARTESIAN_POINT('Ctrl Pts',(0.,4.49979483821861,7.14234367936188)) ;
#76819=CARTESIAN_POINT('Ctrl Pts',(-1.8638760498866,4.49979483821861,7.19195305436187)) ;
#76820=CARTESIAN_POINT('Ctrl Pts',(-3.1818354440526,3.1818354440526,7.24156242936188)) ;
#76821=CARTESIAN_POINT('Ctrl Pts',(-4.49979483821861,1.8638760498866,7.29117180436188)) ;
#76822=CARTESIAN_POINT('Ctrl Pts',(-4.49979483821861,2.7553296727221E-16,
7.34078117936187)) ;
#76823=CARTESIAN_POINT('Ctrl Pts',(-4.49979483821861,-1.8638760498866,7.39039055436188)) ;
#76824=CARTESIAN_POINT('Ctrl Pts',(-3.1818354440526,-3.1818354440526,7.43999992936188)) ;
#76825=CARTESIAN_POINT('Ctrl Pts',(-1.8638760498866,-4.49979483821861,7.48960930436188)) ;
#76826=CARTESIAN_POINT('Ctrl Pts',(-5.5106593454442E-16,-4.49979483821861,
7.53921867936188)) ;
#76827=CARTESIAN_POINT('Ctrl Pts',(1.86387604988659,-4.49979483821861,7.58882805436189)) ;
#76828=CARTESIAN_POINT('Ctrl Pts',(3.1818354440526,-3.18183544405261,7.63843742936188)) ;
#76829=CARTESIAN_POINT('Ctrl Pts',(4.49979483821861,-1.8638760498866,7.68804680436188)) ;
#76830=CARTESIAN_POINT('Ctrl Pts',(4.49979483821861,-8.2659890181663E-16,
7.73765617936188)) ;
#76831=CARTESIAN_POINT('Ctrl Pts',(4.49979483821861,1.8638760498866,7.78726555436187)) ;
#76832=CARTESIAN_POINT('Ctrl Pts',(3.18183544405261,3.1818354440526,7.83687492936187)) ;
#76833=CARTESIAN_POINT('Ctrl Pts',(1.8638760498866,4.49979483821861,7.88648430436188)) ;
#76834=CARTESIAN_POINT('Ctrl Pts',(0.,4.49979483821861,7.93609367936188)) ;
#76835=CARTESIAN_POINT('Ctrl Pts',(-1.8638760498866,4.49979483821861,7.98570305436189)) ;
#76836=CARTESIAN_POINT('Ctrl Pts',(-3.1818354440526,3.1818354440526,8.03531242936188)) ;
#76837=CARTESIAN_POINT('Ctrl Pts',(-4.49979483821861,1.8638760498866,8.08492180436188)) ;
#76838=CARTESIAN_POINT('Ctrl Pts',(-4.49979483821861,2.7553296727221E-16,
8.13453117936188)) ;
#76839=CARTESIAN_POINT('Ctrl Pts',(-4.49979483821861,-1.8638760498866,8.18414055436188)) ;
#76840=CARTESIAN_POINT('Ctrl Pts',(-3.1818354440526,-3.1818354440526,8.23374992936188)) ;
#76841=CARTESIAN_POINT('Ctrl Pts',(-1.8638760498866,-4.49979483821861,8.28335930436188)) ;
#76842=CARTESIAN_POINT('Ctrl Pts',(-5.5106593454442E-16,-4.49979483821861,
8.33296867936188)) ;
#76843=CARTESIAN_POINT('Ctrl Pts',(1.86387604988659,-4.49979483821861,8.38257805436188)) ;
#76844=CARTESIAN_POINT('Ctrl Pts',(3.1818354440526,-3.18183544405261,8.43218742936187)) ;
#76845=CARTESIAN_POINT('Ctrl Pts',(4.49979483821861,-1.8638760498866,8.48179680436188)) ;
#76846=CARTESIAN_POINT('Ctrl Pts',(4.49979483821861,-8.2659890181663E-16,
8.53140617936188)) ;
#76847=CARTESIAN_POINT('Ctrl Pts',(4.49979483821861,1.8638760498866,8.58101555436188)) ;
#76848=CARTESIAN_POINT('Ctrl Pts',(3.18183544405261,3.1818354440526,8.63062492936188)) ;
#76849=CARTESIAN_POINT('Ctrl Pts',(1.8638760498866,4.49979483821861,8.68023430436188)) ;
#76850=CARTESIAN_POINT('Ctrl Pts',(0.,4.49979483821861,8.72984367936187)) ;
#76851=CARTESIAN_POINT('Ctrl Pts',(0.,1.7526,-1.0842021724855E-16)) ;
#76852=CARTESIAN_POINT('Ctrl Pts',(-0.725950689415087,1.7526,0.0496093749999999)) ;
#76853=CARTESIAN_POINT('Ctrl Pts',(-1.23927534470754,1.23927534470754,0.0992187499999999)) ;
#76854=CARTESIAN_POINT('Ctrl Pts',(-1.7526,0.725950689415087,0.148828125)) ;
#76855=CARTESIAN_POINT('Ctrl Pts',(-1.7526,1.07315799009283E-16,0.1984375)) ;
#76856=CARTESIAN_POINT('Ctrl Pts',(-1.7526,-0.725950689415086,0.248046875)) ;
#76857=CARTESIAN_POINT('Ctrl Pts',(-1.23927534470754,-1.23927534470754,
0.29765625)) ;
#76858=CARTESIAN_POINT('Ctrl Pts',(-0.725950689415087,-1.7526,0.347265625)) ;
#76859=CARTESIAN_POINT('Ctrl Pts',(-2.14631598018565E-16,-1.7526,0.396875)) ;
#76860=CARTESIAN_POINT('Ctrl Pts',(0.725950689415086,-1.7526,0.446484375)) ;
#76861=CARTESIAN_POINT('Ctrl Pts',(1.23927534470754,-1.23927534470754,0.49609375)) ;
#76862=CARTESIAN_POINT('Ctrl Pts',(1.7526,-0.725950689415087,0.545703125)) ;
#76863=CARTESIAN_POINT('Ctrl Pts',(1.7526,-3.21947397027848E-16,0.5953125)) ;
#76864=CARTESIAN_POINT('Ctrl Pts',(1.7526,0.725950689415087,0.644921875)) ;
#76865=CARTESIAN_POINT('Ctrl Pts',(1.23927534470754,1.23927534470754,0.69453125)) ;
#76866=CARTESIAN_POINT('Ctrl Pts',(0.725950689415088,1.7526,0.744140625)) ;
#76867=CARTESIAN_POINT('Ctrl Pts',(0.,1.7526,0.79375)) ;
#76868=CARTESIAN_POINT('Ctrl Pts',(-0.725950689415087,1.7526,0.843359375)) ;
#76869=CARTESIAN_POINT('Ctrl Pts',(-1.23927534470754,1.23927534470754,0.89296875)) ;
#76870=CARTESIAN_POINT('Ctrl Pts',(-1.7526,0.725950689415087,0.942578125)) ;
#76871=CARTESIAN_POINT('Ctrl Pts',(-1.7526,1.07315799009283E-16,0.9921875)) ;
#76872=CARTESIAN_POINT('Ctrl Pts',(-1.7526,-0.725950689415086,1.041796875)) ;
#76873=CARTESIAN_POINT('Ctrl Pts',(-1.23927534470754,-1.23927534470754,
1.09140625)) ;
#76874=CARTESIAN_POINT('Ctrl Pts',(-0.725950689415087,-1.7526,1.141015625)) ;
#76875=CARTESIAN_POINT('Ctrl Pts',(-2.14631598018565E-16,-1.7526,1.190625)) ;
#76876=CARTESIAN_POINT('Ctrl Pts',(0.725950689415086,-1.7526,1.240234375)) ;
#76877=CARTESIAN_POINT('Ctrl Pts',(1.23927534470754,-1.23927534470754,1.28984375)) ;
#76878=CARTESIAN_POINT('Ctrl Pts',(1.7526,-0.725950689415087,1.339453125)) ;
#76879=CARTESIAN_POINT('Ctrl Pts',(1.7526,-3.21947397027848E-16,1.3890625)) ;
#76880=CARTESIAN_POINT('Ctrl Pts',(1.7526,0.725950689415087,1.438671875)) ;
#76881=CARTESIAN_POINT('Ctrl Pts',(1.23927534470754,1.23927534470754,1.48828125)) ;
#76882=CARTESIAN_POINT('Ctrl Pts',(0.725950689415088,1.7526,1.537890625)) ;
#76883=CARTESIAN_POINT('Ctrl Pts',(0.,1.7526,1.5875)) ;
#76884=CARTESIAN_POINT('Ctrl Pts',(-0.725950689415087,1.7526,1.637109375)) ;
#76885=CARTESIAN_POINT('Ctrl Pts',(-1.23927534470754,1.23927534470754,1.68671875)) ;
#76886=CARTESIAN_POINT('Ctrl Pts',(-1.7526,0.725950689415087,1.736328125)) ;
#76887=CARTESIAN_POINT('Ctrl Pts',(-1.7526,1.07315799009283E-16,1.7859375)) ;
#76888=CARTESIAN_POINT('Ctrl Pts',(-1.7526,-0.725950689415086,1.835546875)) ;
#76889=CARTESIAN_POINT('Ctrl Pts',(-1.23927534470754,-1.23927534470754,
1.88515625)) ;
#76890=CARTESIAN_POINT('Ctrl Pts',(-0.725950689415087,-1.7526,1.934765625)) ;
#76891=CARTESIAN_POINT('Ctrl Pts',(-2.14631598018565E-16,-1.7526,1.984375)) ;
#76892=CARTESIAN_POINT('Ctrl Pts',(0.725950689415086,-1.7526,2.033984375)) ;
#76893=CARTESIAN_POINT('Ctrl Pts',(1.23927534470754,-1.23927534470754,2.08359375)) ;
#76894=CARTESIAN_POINT('Ctrl Pts',(1.7526,-0.725950689415087,2.133203125)) ;
#76895=CARTESIAN_POINT('Ctrl Pts',(1.7526,-3.21947397027848E-16,2.1828125)) ;
#76896=CARTESIAN_POINT('Ctrl Pts',(1.7526,0.725950689415087,2.232421875)) ;
#76897=CARTESIAN_POINT('Ctrl Pts',(1.23927534470754,1.23927534470754,2.28203125)) ;
#76898=CARTESIAN_POINT('Ctrl Pts',(0.725950689415088,1.7526,2.331640625)) ;
#76899=CARTESIAN_POINT('Ctrl Pts',(0.,1.7526,2.38125)) ;
#76900=CARTESIAN_POINT('Ctrl Pts',(-0.725950689415087,1.7526,2.430859375)) ;
#76901=CARTESIAN_POINT('Ctrl Pts',(-1.23927534470754,1.23927534470754,2.48046875)) ;
#76902=CARTESIAN_POINT('Ctrl Pts',(-1.7526,0.725950689415087,2.530078125)) ;
#76903=CARTESIAN_POINT('Ctrl Pts',(-1.7526,1.07315799009283E-16,2.5796875)) ;
#76904=CARTESIAN_POINT('Ctrl Pts',(-1.7526,-0.725950689415086,2.629296875)) ;
#76905=CARTESIAN_POINT('Ctrl Pts',(-1.23927534470754,-1.23927534470754,
2.67890625)) ;
#76906=CARTESIAN_POINT('Ctrl Pts',(-0.725950689415087,-1.7526,2.728515625)) ;
#76907=CARTESIAN_POINT('Ctrl Pts',(-2.14631598018565E-16,-1.7526,2.778125)) ;
#76908=CARTESIAN_POINT('Ctrl Pts',(0.725950689415086,-1.7526,2.827734375)) ;
#76909=CARTESIAN_POINT('Ctrl Pts',(1.23927534470754,-1.23927534470754,2.87734375)) ;
#76910=CARTESIAN_POINT('Ctrl Pts',(1.7526,-0.725950689415087,2.926953125)) ;
#76911=CARTESIAN_POINT('Ctrl Pts',(1.7526,-3.21947397027848E-16,2.9765625)) ;
#76912=CARTESIAN_POINT('Ctrl Pts',(1.7526,0.725950689415087,3.026171875)) ;
#76913=CARTESIAN_POINT('Ctrl Pts',(1.23927534470754,1.23927534470754,3.07578125)) ;
#76914=CARTESIAN_POINT('Ctrl Pts',(0.725950689415088,1.7526,3.125390625)) ;
#76915=CARTESIAN_POINT('Ctrl Pts',(0.,1.7526,3.175)) ;
#76916=CARTESIAN_POINT('Ctrl Pts',(-0.725950689415087,1.7526,3.224609375)) ;
#76917=CARTESIAN_POINT('Ctrl Pts',(-1.23927534470754,1.23927534470754,3.27421875)) ;
#76918=CARTESIAN_POINT('Ctrl Pts',(-1.7526,0.725950689415087,3.323828125)) ;
#76919=CARTESIAN_POINT('Ctrl Pts',(-1.7526,1.07315799009283E-16,3.3734375)) ;
#76920=CARTESIAN_POINT('Ctrl Pts',(-1.7526,-0.725950689415086,3.423046875)) ;
#76921=CARTESIAN_POINT('Ctrl Pts',(-1.23927534470754,-1.23927534470754,
3.47265625)) ;
#76922=CARTESIAN_POINT('Ctrl Pts',(-0.725950689415087,-1.7526,3.522265625)) ;
#76923=CARTESIAN_POINT('Ctrl Pts',(-2.14631598018565E-16,-1.7526,3.571875)) ;
#76924=CARTESIAN_POINT('Ctrl Pts',(0.725950689415086,-1.7526,3.621484375)) ;
#76925=CARTESIAN_POINT('Ctrl Pts',(1.23927534470754,-1.23927534470754,3.67109375)) ;
#76926=CARTESIAN_POINT('Ctrl Pts',(1.7526,-0.725950689415087,3.720703125)) ;
#76927=CARTESIAN_POINT('Ctrl Pts',(1.7526,-3.21947397027848E-16,3.7703125)) ;
#76928=CARTESIAN_POINT('Ctrl Pts',(1.7526,0.725950689415087,3.819921875)) ;
#76929=CARTESIAN_POINT('Ctrl Pts',(1.23927534470754,1.23927534470754,3.86953125)) ;
#76930=CARTESIAN_POINT('Ctrl Pts',(0.725950689415088,1.7526,3.919140625)) ;
#76931=CARTESIAN_POINT('Ctrl Pts',(0.,1.7526,3.96875)) ;
#76932=CARTESIAN_POINT('Ctrl Pts',(-0.725950689415087,1.7526,4.018359375)) ;
#76933=CARTESIAN_POINT('Ctrl Pts',(-1.23927534470754,1.23927534470754,4.06796875)) ;
#76934=CARTESIAN_POINT('Ctrl Pts',(-1.7526,0.725950689415087,4.117578125)) ;
#76935=CARTESIAN_POINT('Ctrl Pts',(-1.7526,1.07315799009283E-16,4.1671875)) ;
#76936=CARTESIAN_POINT('Ctrl Pts',(-1.7526,-0.725950689415086,4.216796875)) ;
#76937=CARTESIAN_POINT('Ctrl Pts',(-1.23927534470754,-1.23927534470754,
4.26640625)) ;
#76938=CARTESIAN_POINT('Ctrl Pts',(-0.725950689415087,-1.7526,4.316015625)) ;
#76939=CARTESIAN_POINT('Ctrl Pts',(-2.14631598018565E-16,-1.7526,4.365625)) ;
#76940=CARTESIAN_POINT('Ctrl Pts',(0.725950689415086,-1.7526,4.415234375)) ;
#76941=CARTESIAN_POINT('Ctrl Pts',(1.23927534470754,-1.23927534470754,4.46484375)) ;
#76942=CARTESIAN_POINT('Ctrl Pts',(1.7526,-0.725950689415087,4.514453125)) ;
#76943=CARTESIAN_POINT('Ctrl Pts',(1.7526,-3.21947397027848E-16,4.5640625)) ;
#76944=CARTESIAN_POINT('Ctrl Pts',(1.7526,0.725950689415087,4.613671875)) ;
#76945=CARTESIAN_POINT('Ctrl Pts',(1.23927534470754,1.23927534470754,4.66328125)) ;
#76946=CARTESIAN_POINT('Ctrl Pts',(0.725950689415088,1.7526,4.712890625)) ;
#76947=CARTESIAN_POINT('Ctrl Pts',(0.,1.7526,4.7625)) ;
#76948=CARTESIAN_POINT('Ctrl Pts',(-0.725950689415087,1.7526,4.812109375)) ;
#76949=CARTESIAN_POINT('Ctrl Pts',(-1.23927534470754,1.23927534470754,4.86171875)) ;
#76950=CARTESIAN_POINT('Ctrl Pts',(-1.7526,0.725950689415087,4.911328125)) ;
#76951=CARTESIAN_POINT('Ctrl Pts',(-1.7526,1.07315799009283E-16,4.9609375)) ;
#76952=CARTESIAN_POINT('Ctrl Pts',(-1.7526,-0.725950689415086,5.010546875)) ;
#76953=CARTESIAN_POINT('Ctrl Pts',(-1.23927534470754,-1.23927534470754,
5.06015625)) ;
#76954=CARTESIAN_POINT('Ctrl Pts',(-0.725950689415087,-1.7526,5.109765625)) ;
#76955=CARTESIAN_POINT('Ctrl Pts',(-2.14631598018565E-16,-1.7526,5.159375)) ;
#76956=CARTESIAN_POINT('Ctrl Pts',(0.725950689415086,-1.7526,5.208984375)) ;
#76957=CARTESIAN_POINT('Ctrl Pts',(1.23927534470754,-1.23927534470754,5.25859375)) ;
#76958=CARTESIAN_POINT('Ctrl Pts',(1.7526,-0.725950689415087,5.308203125)) ;
#76959=CARTESIAN_POINT('Ctrl Pts',(1.7526,-3.21947397027848E-16,5.3578125)) ;
#76960=CARTESIAN_POINT('Ctrl Pts',(1.7526,0.725950689415087,5.407421875)) ;
#76961=CARTESIAN_POINT('Ctrl Pts',(1.23927534470754,1.23927534470754,5.45703125)) ;
#76962=CARTESIAN_POINT('Ctrl Pts',(0.725950689415088,1.7526,5.506640625)) ;
#76963=CARTESIAN_POINT('Ctrl Pts',(0.,1.7526,5.55625)) ;
#76964=CARTESIAN_POINT('Ctrl Pts',(-0.725950689415087,1.7526,5.605859375)) ;
#76965=CARTESIAN_POINT('Ctrl Pts',(-1.23927534470754,1.23927534470754,5.65546875)) ;
#76966=CARTESIAN_POINT('Ctrl Pts',(-1.7526,0.725950689415087,5.705078125)) ;
#76967=CARTESIAN_POINT('Ctrl Pts',(-1.7526,1.07315799009283E-16,5.7546875)) ;
#76968=CARTESIAN_POINT('Ctrl Pts',(-1.7526,-0.725950689415086,5.804296875)) ;
#76969=CARTESIAN_POINT('Ctrl Pts',(-1.23927534470754,-1.23927534470754,
5.85390625)) ;
#76970=CARTESIAN_POINT('Ctrl Pts',(-0.725950689415087,-1.7526,5.903515625)) ;
#76971=CARTESIAN_POINT('Ctrl Pts',(-2.14631598018565E-16,-1.7526,5.953125)) ;
#76972=CARTESIAN_POINT('Ctrl Pts',(0.725950689415086,-1.7526,6.002734375)) ;
#76973=CARTESIAN_POINT('Ctrl Pts',(1.23927534470754,-1.23927534470754,6.05234375)) ;
#76974=CARTESIAN_POINT('Ctrl Pts',(1.7526,-0.725950689415087,6.101953125)) ;
#76975=CARTESIAN_POINT('Ctrl Pts',(1.7526,-3.21947397027848E-16,6.1515625)) ;
#76976=CARTESIAN_POINT('Ctrl Pts',(1.7526,0.725950689415087,6.201171875)) ;
#76977=CARTESIAN_POINT('Ctrl Pts',(1.23927534470754,1.23927534470754,6.25078125)) ;
#76978=CARTESIAN_POINT('Ctrl Pts',(0.725950689415088,1.7526,6.300390625)) ;
#76979=CARTESIAN_POINT('Ctrl Pts',(0.,1.7526,6.35)) ;
#76980=CARTESIAN_POINT('Ctrl Pts',(-0.725950689415087,1.7526,6.399609375)) ;
#76981=CARTESIAN_POINT('Ctrl Pts',(-1.23927534470754,1.23927534470754,6.44921875)) ;
#76982=CARTESIAN_POINT('Ctrl Pts',(-1.7526,0.725950689415087,6.498828125)) ;
#76983=CARTESIAN_POINT('Ctrl Pts',(-1.7526,1.07315799009283E-16,6.5484375)) ;
#76984=CARTESIAN_POINT('Ctrl Pts',(-1.7526,-0.725950689415086,6.598046875)) ;
#76985=CARTESIAN_POINT('Ctrl Pts',(-1.23927534470754,-1.23927534470754,
6.64765625)) ;
#76986=CARTESIAN_POINT('Ctrl Pts',(-0.725950689415087,-1.7526,6.697265625)) ;
#76987=CARTESIAN_POINT('Ctrl Pts',(-2.14631598018565E-16,-1.7526,6.746875)) ;
#76988=CARTESIAN_POINT('Ctrl Pts',(0.725950689415086,-1.7526,6.796484375)) ;
#76989=CARTESIAN_POINT('Ctrl Pts',(1.23927534470754,-1.23927534470754,6.84609375)) ;
#76990=CARTESIAN_POINT('Ctrl Pts',(1.7526,-0.725950689415087,6.895703125)) ;
#76991=CARTESIAN_POINT('Ctrl Pts',(1.7526,-3.21947397027848E-16,6.9453125)) ;
#76992=CARTESIAN_POINT('Ctrl Pts',(1.7526,0.725950689415087,6.994921875)) ;
#76993=CARTESIAN_POINT('Ctrl Pts',(1.23927534470754,1.23927534470754,7.04453125)) ;
#76994=CARTESIAN_POINT('Ctrl Pts',(0.725950689415088,1.7526,7.094140625)) ;
#76995=CARTESIAN_POINT('Ctrl Pts',(0.,1.7526,7.14375)) ;
#76996=CARTESIAN_POINT('Ctrl Pts',(0.,1.23704425180958,-0.297656250000002)) ;
#76997=CARTESIAN_POINT('Ctrl Pts',(-0.512400506355205,1.23704425180958,
-0.248046875000002)) ;
#76998=CARTESIAN_POINT('Ctrl Pts',(-0.874722379082391,0.874722379082391,
-0.198437500000002)) ;
#76999=CARTESIAN_POINT('Ctrl Pts',(-1.23704425180958,0.512400506355205,
-0.148828125000002)) ;
#77000=CARTESIAN_POINT('Ctrl Pts',(-1.23704425180958,7.57471141691116E-17,
-0.0992187500000015)) ;
#77001=CARTESIAN_POINT('Ctrl Pts',(-1.23704425180958,-0.512400506355205,
-0.0496093750000015)) ;
#77002=CARTESIAN_POINT('Ctrl Pts',(-0.874722379082391,-0.874722379082391,
-1.57209315010398E-15)) ;
#77003=CARTESIAN_POINT('Ctrl Pts',(-0.512400506355205,-1.23704425180958,
0.0496093749999984)) ;
#77004=CARTESIAN_POINT('Ctrl Pts',(-1.51494228338223E-16,-1.23704425180958,
0.0992187499999985)) ;
#77005=CARTESIAN_POINT('Ctrl Pts',(0.512400506355205,-1.23704425180958,
0.148828124999998)) ;
#77006=CARTESIAN_POINT('Ctrl Pts',(0.874722379082391,-0.874722379082391,
0.198437499999998)) ;
#77007=CARTESIAN_POINT('Ctrl Pts',(1.23704425180958,-0.512400506355206,
0.248046874999998)) ;
#77008=CARTESIAN_POINT('Ctrl Pts',(1.23704425180958,-2.27241342507335E-16,
0.297656249999998)) ;
#77009=CARTESIAN_POINT('Ctrl Pts',(1.23704425180958,0.512400506355206,0.347265624999998)) ;
#77010=CARTESIAN_POINT('Ctrl Pts',(0.874722379082391,0.874722379082391,
0.396874999999998)) ;
#77011=CARTESIAN_POINT('Ctrl Pts',(0.512400506355206,1.23704425180958,0.446484374999998)) ;
#77012=CARTESIAN_POINT('Ctrl Pts',(0.,1.23704425180958,0.496093749999999)) ;
#77013=CARTESIAN_POINT('Ctrl Pts',(-0.512400506355205,1.23704425180958,
0.545703124999998)) ;
#77014=CARTESIAN_POINT('Ctrl Pts',(-0.874722379082391,0.874722379082391,
0.595312499999998)) ;
#77015=CARTESIAN_POINT('Ctrl Pts',(-1.23704425180958,0.512400506355205,
0.644921874999998)) ;
#77016=CARTESIAN_POINT('Ctrl Pts',(-1.23704425180958,7.57471141691116E-17,
0.694531249999999)) ;
#77017=CARTESIAN_POINT('Ctrl Pts',(-1.23704425180958,-0.512400506355205,
0.744140624999998)) ;
#77018=CARTESIAN_POINT('Ctrl Pts',(-0.874722379082391,-0.874722379082391,
0.793749999999999)) ;
#77019=CARTESIAN_POINT('Ctrl Pts',(-0.512400506355205,-1.23704425180958,
0.843359374999998)) ;
#77020=CARTESIAN_POINT('Ctrl Pts',(-1.51494228338223E-16,-1.23704425180958,
0.892968749999998)) ;
#77021=CARTESIAN_POINT('Ctrl Pts',(0.512400506355205,-1.23704425180958,
0.942578124999999)) ;
#77022=CARTESIAN_POINT('Ctrl Pts',(0.874722379082391,-0.874722379082391,
0.992187499999999)) ;
#77023=CARTESIAN_POINT('Ctrl Pts',(1.23704425180958,-0.512400506355206,
1.041796875)) ;
#77024=CARTESIAN_POINT('Ctrl Pts',(1.23704425180958,-2.27241342507335E-16,
1.09140625)) ;
#77025=CARTESIAN_POINT('Ctrl Pts',(1.23704425180958,0.512400506355206,1.141015625)) ;
#77026=CARTESIAN_POINT('Ctrl Pts',(0.874722379082391,0.874722379082391,
1.190625)) ;
#77027=CARTESIAN_POINT('Ctrl Pts',(0.512400506355206,1.23704425180958,1.240234375)) ;
#77028=CARTESIAN_POINT('Ctrl Pts',(0.,1.23704425180958,1.28984375)) ;
#77029=CARTESIAN_POINT('Ctrl Pts',(-0.512400506355205,1.23704425180958,
1.339453125)) ;
#77030=CARTESIAN_POINT('Ctrl Pts',(-0.874722379082391,0.874722379082391,
1.3890625)) ;
#77031=CARTESIAN_POINT('Ctrl Pts',(-1.23704425180958,0.512400506355205,
1.438671875)) ;
#77032=CARTESIAN_POINT('Ctrl Pts',(-1.23704425180958,7.57471141691116E-17,
1.48828125)) ;
#77033=CARTESIAN_POINT('Ctrl Pts',(-1.23704425180958,-0.512400506355205,
1.537890625)) ;
#77034=CARTESIAN_POINT('Ctrl Pts',(-0.874722379082391,-0.874722379082391,
1.5875)) ;
#77035=CARTESIAN_POINT('Ctrl Pts',(-0.512400506355205,-1.23704425180958,
1.637109375)) ;
#77036=CARTESIAN_POINT('Ctrl Pts',(-1.51494228338223E-16,-1.23704425180958,
1.68671875)) ;
#77037=CARTESIAN_POINT('Ctrl Pts',(0.512400506355205,-1.23704425180958,
1.736328125)) ;
#77038=CARTESIAN_POINT('Ctrl Pts',(0.874722379082391,-0.874722379082391,
1.7859375)) ;
#77039=CARTESIAN_POINT('Ctrl Pts',(1.23704425180958,-0.512400506355206,
1.835546875)) ;
#77040=CARTESIAN_POINT('Ctrl Pts',(1.23704425180958,-2.27241342507335E-16,
1.88515625)) ;
#77041=CARTESIAN_POINT('Ctrl Pts',(1.23704425180958,0.512400506355206,1.934765625)) ;
#77042=CARTESIAN_POINT('Ctrl Pts',(0.874722379082391,0.874722379082391,
1.984375)) ;
#77043=CARTESIAN_POINT('Ctrl Pts',(0.512400506355206,1.23704425180958,2.033984375)) ;
#77044=CARTESIAN_POINT('Ctrl Pts',(0.,1.23704425180958,2.08359375)) ;
#77045=CARTESIAN_POINT('Ctrl Pts',(-0.512400506355205,1.23704425180958,
2.133203125)) ;
#77046=CARTESIAN_POINT('Ctrl Pts',(-0.874722379082391,0.874722379082391,
2.1828125)) ;
#77047=CARTESIAN_POINT('Ctrl Pts',(-1.23704425180958,0.512400506355205,
2.232421875)) ;
#77048=CARTESIAN_POINT('Ctrl Pts',(-1.23704425180958,7.57471141691116E-17,
2.28203125)) ;
#77049=CARTESIAN_POINT('Ctrl Pts',(-1.23704425180958,-0.512400506355205,
2.331640625)) ;
#77050=CARTESIAN_POINT('Ctrl Pts',(-0.874722379082391,-0.874722379082391,
2.38125)) ;
#77051=CARTESIAN_POINT('Ctrl Pts',(-0.512400506355205,-1.23704425180958,
2.430859375)) ;
#77052=CARTESIAN_POINT('Ctrl Pts',(-1.51494228338223E-16,-1.23704425180958,
2.48046875)) ;
#77053=CARTESIAN_POINT('Ctrl Pts',(0.512400506355205,-1.23704425180958,
2.530078125)) ;
#77054=CARTESIAN_POINT('Ctrl Pts',(0.874722379082391,-0.874722379082391,
2.5796875)) ;
#77055=CARTESIAN_POINT('Ctrl Pts',(1.23704425180958,-0.512400506355206,
2.629296875)) ;
#77056=CARTESIAN_POINT('Ctrl Pts',(1.23704425180958,-2.27241342507335E-16,
2.67890625)) ;
#77057=CARTESIAN_POINT('Ctrl Pts',(1.23704425180958,0.512400506355206,2.728515625)) ;
#77058=CARTESIAN_POINT('Ctrl Pts',(0.874722379082391,0.874722379082391,
2.778125)) ;
#77059=CARTESIAN_POINT('Ctrl Pts',(0.512400506355206,1.23704425180958,2.827734375)) ;
#77060=CARTESIAN_POINT('Ctrl Pts',(0.,1.23704425180958,2.87734375)) ;
#77061=CARTESIAN_POINT('Ctrl Pts',(-0.512400506355205,1.23704425180958,
2.926953125)) ;
#77062=CARTESIAN_POINT('Ctrl Pts',(-0.874722379082391,0.874722379082391,
2.9765625)) ;
#77063=CARTESIAN_POINT('Ctrl Pts',(-1.23704425180958,0.512400506355205,
3.026171875)) ;
#77064=CARTESIAN_POINT('Ctrl Pts',(-1.23704425180958,7.57471141691116E-17,
3.07578125)) ;
#77065=CARTESIAN_POINT('Ctrl Pts',(-1.23704425180958,-0.512400506355205,
3.125390625)) ;
#77066=CARTESIAN_POINT('Ctrl Pts',(-0.874722379082391,-0.874722379082391,
3.175)) ;
#77067=CARTESIAN_POINT('Ctrl Pts',(-0.512400506355205,-1.23704425180958,
3.224609375)) ;
#77068=CARTESIAN_POINT('Ctrl Pts',(-1.51494228338223E-16,-1.23704425180958,
3.27421875)) ;
#77069=CARTESIAN_POINT('Ctrl Pts',(0.512400506355205,-1.23704425180958,
3.323828125)) ;
#77070=CARTESIAN_POINT('Ctrl Pts',(0.874722379082391,-0.874722379082391,
3.3734375)) ;
#77071=CARTESIAN_POINT('Ctrl Pts',(1.23704425180958,-0.512400506355206,
3.423046875)) ;
#77072=CARTESIAN_POINT('Ctrl Pts',(1.23704425180958,-2.27241342507335E-16,
3.47265625)) ;
#77073=CARTESIAN_POINT('Ctrl Pts',(1.23704425180958,0.512400506355206,3.522265625)) ;
#77074=CARTESIAN_POINT('Ctrl Pts',(0.874722379082391,0.874722379082391,
3.571875)) ;
#77075=CARTESIAN_POINT('Ctrl Pts',(0.512400506355206,1.23704425180958,3.621484375)) ;
#77076=CARTESIAN_POINT('Ctrl Pts',(0.,1.23704425180958,3.67109375)) ;
#77077=CARTESIAN_POINT('Ctrl Pts',(-0.512400506355205,1.23704425180958,
3.720703125)) ;
#77078=CARTESIAN_POINT('Ctrl Pts',(-0.874722379082391,0.874722379082391,
3.7703125)) ;
#77079=CARTESIAN_POINT('Ctrl Pts',(-1.23704425180958,0.512400506355205,
3.819921875)) ;
#77080=CARTESIAN_POINT('Ctrl Pts',(-1.23704425180958,7.57471141691116E-17,
3.86953125)) ;
#77081=CARTESIAN_POINT('Ctrl Pts',(-1.23704425180958,-0.512400506355205,
3.919140625)) ;
#77082=CARTESIAN_POINT('Ctrl Pts',(-0.874722379082391,-0.874722379082391,
3.96875)) ;
#77083=CARTESIAN_POINT('Ctrl Pts',(-0.512400506355205,-1.23704425180958,
4.018359375)) ;
#77084=CARTESIAN_POINT('Ctrl Pts',(-1.51494228338223E-16,-1.23704425180958,
4.06796875)) ;
#77085=CARTESIAN_POINT('Ctrl Pts',(0.512400506355205,-1.23704425180958,
4.117578125)) ;
#77086=CARTESIAN_POINT('Ctrl Pts',(0.874722379082391,-0.874722379082391,
4.1671875)) ;
#77087=CARTESIAN_POINT('Ctrl Pts',(1.23704425180958,-0.512400506355206,
4.216796875)) ;
#77088=CARTESIAN_POINT('Ctrl Pts',(1.23704425180958,-2.27241342507335E-16,
4.26640625)) ;
#77089=CARTESIAN_POINT('Ctrl Pts',(1.23704425180958,0.512400506355206,4.316015625)) ;
#77090=CARTESIAN_POINT('Ctrl Pts',(0.874722379082391,0.874722379082391,
4.365625)) ;
#77091=CARTESIAN_POINT('Ctrl Pts',(0.512400506355206,1.23704425180958,4.415234375)) ;
#77092=CARTESIAN_POINT('Ctrl Pts',(0.,1.23704425180958,4.46484375)) ;
#77093=CARTESIAN_POINT('Ctrl Pts',(-0.512400506355205,1.23704425180958,
4.514453125)) ;
#77094=CARTESIAN_POINT('Ctrl Pts',(-0.874722379082391,0.874722379082391,
4.5640625)) ;
#77095=CARTESIAN_POINT('Ctrl Pts',(-1.23704425180958,0.512400506355205,
4.613671875)) ;
#77096=CARTESIAN_POINT('Ctrl Pts',(-1.23704425180958,7.57471141691116E-17,
4.66328125)) ;
#77097=CARTESIAN_POINT('Ctrl Pts',(-1.23704425180958,-0.512400506355205,
4.712890625)) ;
#77098=CARTESIAN_POINT('Ctrl Pts',(-0.874722379082391,-0.874722379082391,
4.7625)) ;
#77099=CARTESIAN_POINT('Ctrl Pts',(-0.512400506355205,-1.23704425180958,
4.812109375)) ;
#77100=CARTESIAN_POINT('Ctrl Pts',(-1.51494228338223E-16,-1.23704425180958,
4.86171875)) ;
#77101=CARTESIAN_POINT('Ctrl Pts',(0.512400506355205,-1.23704425180958,
4.911328125)) ;
#77102=CARTESIAN_POINT('Ctrl Pts',(0.874722379082391,-0.874722379082391,
4.9609375)) ;
#77103=CARTESIAN_POINT('Ctrl Pts',(1.23704425180958,-0.512400506355206,
5.010546875)) ;
#77104=CARTESIAN_POINT('Ctrl Pts',(1.23704425180958,-2.27241342507335E-16,
5.06015625)) ;
#77105=CARTESIAN_POINT('Ctrl Pts',(1.23704425180958,0.512400506355206,5.109765625)) ;
#77106=CARTESIAN_POINT('Ctrl Pts',(0.874722379082391,0.874722379082391,
5.159375)) ;
#77107=CARTESIAN_POINT('Ctrl Pts',(0.512400506355206,1.23704425180958,5.208984375)) ;
#77108=CARTESIAN_POINT('Ctrl Pts',(0.,1.23704425180958,5.25859375)) ;
#77109=CARTESIAN_POINT('Ctrl Pts',(-0.512400506355205,1.23704425180958,
5.308203125)) ;
#77110=CARTESIAN_POINT('Ctrl Pts',(-0.874722379082391,0.874722379082391,
5.3578125)) ;
#77111=CARTESIAN_POINT('Ctrl Pts',(-1.23704425180958,0.512400506355205,
5.407421875)) ;
#77112=CARTESIAN_POINT('Ctrl Pts',(-1.23704425180958,7.57471141691116E-17,
5.45703125)) ;
#77113=CARTESIAN_POINT('Ctrl Pts',(-1.23704425180958,-0.512400506355205,
5.506640625)) ;
#77114=CARTESIAN_POINT('Ctrl Pts',(-0.874722379082391,-0.874722379082391,
5.55625)) ;
#77115=CARTESIAN_POINT('Ctrl Pts',(-0.512400506355205,-1.23704425180958,
5.605859375)) ;
#77116=CARTESIAN_POINT('Ctrl Pts',(-1.51494228338223E-16,-1.23704425180958,
5.65546875)) ;
#77117=CARTESIAN_POINT('Ctrl Pts',(0.512400506355205,-1.23704425180958,
5.705078125)) ;
#77118=CARTESIAN_POINT('Ctrl Pts',(0.874722379082391,-0.874722379082391,
5.7546875)) ;
#77119=CARTESIAN_POINT('Ctrl Pts',(1.23704425180958,-0.512400506355206,
5.804296875)) ;
#77120=CARTESIAN_POINT('Ctrl Pts',(1.23704425180958,-2.27241342507335E-16,
5.85390625)) ;
#77121=CARTESIAN_POINT('Ctrl Pts',(1.23704425180958,0.512400506355206,5.903515625)) ;
#77122=CARTESIAN_POINT('Ctrl Pts',(0.874722379082391,0.874722379082391,
5.953125)) ;
#77123=CARTESIAN_POINT('Ctrl Pts',(0.512400506355206,1.23704425180958,6.002734375)) ;
#77124=CARTESIAN_POINT('Ctrl Pts',(0.,1.23704425180958,6.05234375)) ;
#77125=CARTESIAN_POINT('Ctrl Pts',(-0.512400506355205,1.23704425180958,
6.101953125)) ;
#77126=CARTESIAN_POINT('Ctrl Pts',(-0.874722379082391,0.874722379082391,
6.1515625)) ;
#77127=CARTESIAN_POINT('Ctrl Pts',(-1.23704425180958,0.512400506355205,
6.201171875)) ;
#77128=CARTESIAN_POINT('Ctrl Pts',(-1.23704425180958,7.57471141691116E-17,
6.25078125)) ;
#77129=CARTESIAN_POINT('Ctrl Pts',(-1.23704425180958,-0.512400506355205,
6.300390625)) ;
#77130=CARTESIAN_POINT('Ctrl Pts',(-0.874722379082391,-0.874722379082391,
6.35)) ;
#77131=CARTESIAN_POINT('Ctrl Pts',(-0.512400506355205,-1.23704425180958,
6.399609375)) ;
#77132=CARTESIAN_POINT('Ctrl Pts',(-1.51494228338223E-16,-1.23704425180958,
6.44921875)) ;
#77133=CARTESIAN_POINT('Ctrl Pts',(0.512400506355205,-1.23704425180958,
6.498828125)) ;
#77134=CARTESIAN_POINT('Ctrl Pts',(0.874722379082391,-0.874722379082391,
6.5484375)) ;
#77135=CARTESIAN_POINT('Ctrl Pts',(1.23704425180958,-0.512400506355206,
6.598046875)) ;
#77136=CARTESIAN_POINT('Ctrl Pts',(1.23704425180958,-2.27241342507335E-16,
6.64765625)) ;
#77137=CARTESIAN_POINT('Ctrl Pts',(1.23704425180958,0.512400506355206,6.697265625)) ;
#77138=CARTESIAN_POINT('Ctrl Pts',(0.874722379082391,0.874722379082391,
6.746875)) ;
#77139=CARTESIAN_POINT('Ctrl Pts',(0.512400506355206,1.23704425180958,6.796484375)) ;
#77140=CARTESIAN_POINT('Ctrl Pts',(0.,1.23704425180958,6.84609375)) ;
#77141=CARTESIAN_POINT('Ctrl Pts',(0.,0.417702301404716,-0.770703545624604)) ;
#77142=CARTESIAN_POINT('Ctrl Pts',(-0.173017958276288,0.417702301404717,
-0.721094170624604)) ;
#77143=CARTESIAN_POINT('Ctrl Pts',(-0.295360129840502,0.295360129840502,
-0.671484795624604)) ;
#77144=CARTESIAN_POINT('Ctrl Pts',(-0.417702301404717,0.173017958276288,
-0.621875420624604)) ;
#77145=CARTESIAN_POINT('Ctrl Pts',(-0.417702301404716,2.55768893205885E-17,
-0.572266045624604)) ;
#77146=CARTESIAN_POINT('Ctrl Pts',(-0.417702301404717,-0.173017958276288,
-0.522656670624604)) ;
#77147=CARTESIAN_POINT('Ctrl Pts',(-0.295360129840502,-0.295360129840502,
-0.473047295624604)) ;
#77148=CARTESIAN_POINT('Ctrl Pts',(-0.173017958276288,-0.417702301404717,
-0.423437920624604)) ;
#77149=CARTESIAN_POINT('Ctrl Pts',(-5.1153778641177E-17,-0.417702301404716,
-0.373828545624604)) ;
#77150=CARTESIAN_POINT('Ctrl Pts',(0.173017958276288,-0.417702301404716,
-0.324219170624604)) ;
#77151=CARTESIAN_POINT('Ctrl Pts',(0.295360129840502,-0.295360129840502,
-0.274609795624604)) ;
#77152=CARTESIAN_POINT('Ctrl Pts',(0.417702301404717,-0.173017958276288,
-0.225000420624604)) ;
#77153=CARTESIAN_POINT('Ctrl Pts',(0.417702301404716,-7.67306679617654E-17,
-0.175391045624604)) ;
#77154=CARTESIAN_POINT('Ctrl Pts',(0.417702301404717,0.173017958276288,
-0.125781670624604)) ;
#77155=CARTESIAN_POINT('Ctrl Pts',(0.295360129840502,0.295360129840503,
-0.0761722956246044)) ;
#77156=CARTESIAN_POINT('Ctrl Pts',(0.173017958276288,0.417702301404717,
-0.0265629206246046)) ;
#77157=CARTESIAN_POINT('Ctrl Pts',(0.,0.417702301404716,0.0230464543753958)) ;
#77158=CARTESIAN_POINT('Ctrl Pts',(-0.173017958276288,0.417702301404717,
0.0726558293753954)) ;
#77159=CARTESIAN_POINT('Ctrl Pts',(-0.295360129840502,0.295360129840502,
0.122265204375396)) ;
#77160=CARTESIAN_POINT('Ctrl Pts',(-0.417702301404717,0.173017958276288,
0.171874579375395)) ;
#77161=CARTESIAN_POINT('Ctrl Pts',(-0.417702301404716,2.55768893205885E-17,
0.221483954375396)) ;
#77162=CARTESIAN_POINT('Ctrl Pts',(-0.417702301404717,-0.173017958276288,
0.271093329375396)) ;
#77163=CARTESIAN_POINT('Ctrl Pts',(-0.295360129840502,-0.295360129840502,
0.320702704375395)) ;
#77164=CARTESIAN_POINT('Ctrl Pts',(-0.173017958276288,-0.417702301404717,
0.370312079375396)) ;
#77165=CARTESIAN_POINT('Ctrl Pts',(-5.1153778641177E-17,-0.417702301404716,
0.419921454375396)) ;
#77166=CARTESIAN_POINT('Ctrl Pts',(0.173017958276288,-0.417702301404716,
0.469530829375396)) ;
#77167=CARTESIAN_POINT('Ctrl Pts',(0.295360129840502,-0.295360129840502,
0.519140204375396)) ;
#77168=CARTESIAN_POINT('Ctrl Pts',(0.417702301404717,-0.173017958276288,
0.568749579375395)) ;
#77169=CARTESIAN_POINT('Ctrl Pts',(0.417702301404716,-7.67306679617654E-17,
0.618358954375396)) ;
#77170=CARTESIAN_POINT('Ctrl Pts',(0.417702301404717,0.173017958276288,
0.667968329375395)) ;
#77171=CARTESIAN_POINT('Ctrl Pts',(0.295360129840502,0.295360129840503,
0.717577704375396)) ;
#77172=CARTESIAN_POINT('Ctrl Pts',(0.173017958276288,0.417702301404717,
0.767187079375397)) ;
#77173=CARTESIAN_POINT('Ctrl Pts',(0.,0.417702301404716,0.816796454375395)) ;
#77174=CARTESIAN_POINT('Ctrl Pts',(-0.173017958276288,0.417702301404717,
0.866405829375395)) ;
#77175=CARTESIAN_POINT('Ctrl Pts',(-0.295360129840502,0.295360129840502,
0.916015204375395)) ;
#77176=CARTESIAN_POINT('Ctrl Pts',(-0.417702301404717,0.173017958276288,
0.965624579375395)) ;
#77177=CARTESIAN_POINT('Ctrl Pts',(-0.417702301404716,2.55768893205885E-17,
1.0152339543754)) ;
#77178=CARTESIAN_POINT('Ctrl Pts',(-0.417702301404717,-0.173017958276288,
1.0648433293754)) ;
#77179=CARTESIAN_POINT('Ctrl Pts',(-0.295360129840502,-0.295360129840502,
1.1144527043754)) ;
#77180=CARTESIAN_POINT('Ctrl Pts',(-0.173017958276288,-0.417702301404717,
1.1640620793754)) ;
#77181=CARTESIAN_POINT('Ctrl Pts',(-5.1153778641177E-17,-0.417702301404716,
1.2136714543754)) ;
#77182=CARTESIAN_POINT('Ctrl Pts',(0.173017958276288,-0.417702301404716,
1.2632808293754)) ;
#77183=CARTESIAN_POINT('Ctrl Pts',(0.295360129840502,-0.295360129840502,
1.3128902043754)) ;
#77184=CARTESIAN_POINT('Ctrl Pts',(0.417702301404717,-0.173017958276288,
1.3624995793754)) ;
#77185=CARTESIAN_POINT('Ctrl Pts',(0.417702301404716,-7.67306679617654E-17,
1.4121089543754)) ;
#77186=CARTESIAN_POINT('Ctrl Pts',(0.417702301404717,0.173017958276288,
1.4617183293754)) ;
#77187=CARTESIAN_POINT('Ctrl Pts',(0.295360129840502,0.295360129840503,
1.51132770437539)) ;
#77188=CARTESIAN_POINT('Ctrl Pts',(0.173017958276288,0.417702301404717,
1.5609370793754)) ;
#77189=CARTESIAN_POINT('Ctrl Pts',(0.,0.417702301404716,1.61054645437539)) ;
#77190=CARTESIAN_POINT('Ctrl Pts',(-0.173017958276288,0.417702301404717,
1.6601558293754)) ;
#77191=CARTESIAN_POINT('Ctrl Pts',(-0.295360129840502,0.295360129840502,
1.7097652043754)) ;
#77192=CARTESIAN_POINT('Ctrl Pts',(-0.417702301404717,0.173017958276288,
1.75937457937539)) ;
#77193=CARTESIAN_POINT('Ctrl Pts',(-0.417702301404716,2.55768893205885E-17,
1.8089839543754)) ;
#77194=CARTESIAN_POINT('Ctrl Pts',(-0.417702301404717,-0.173017958276288,
1.8585933293754)) ;
#77195=CARTESIAN_POINT('Ctrl Pts',(-0.295360129840502,-0.295360129840502,
1.9082027043754)) ;
#77196=CARTESIAN_POINT('Ctrl Pts',(-0.173017958276288,-0.417702301404717,
1.9578120793754)) ;
#77197=CARTESIAN_POINT('Ctrl Pts',(-5.1153778641177E-17,-0.417702301404716,
2.00742145437539)) ;
#77198=CARTESIAN_POINT('Ctrl Pts',(0.173017958276288,-0.417702301404716,
2.0570308293754)) ;
#77199=CARTESIAN_POINT('Ctrl Pts',(0.295360129840502,-0.295360129840502,
2.10664020437539)) ;
#77200=CARTESIAN_POINT('Ctrl Pts',(0.417702301404717,-0.173017958276288,
2.1562495793754)) ;
#77201=CARTESIAN_POINT('Ctrl Pts',(0.417702301404716,-7.67306679617654E-17,
2.2058589543754)) ;
#77202=CARTESIAN_POINT('Ctrl Pts',(0.417702301404717,0.173017958276288,
2.2554683293754)) ;
#77203=CARTESIAN_POINT('Ctrl Pts',(0.295360129840502,0.295360129840503,
2.3050777043754)) ;
#77204=CARTESIAN_POINT('Ctrl Pts',(0.173017958276288,0.417702301404717,
2.3546870793754)) ;
#77205=CARTESIAN_POINT('Ctrl Pts',(0.,0.417702301404716,2.4042964543754)) ;
#77206=CARTESIAN_POINT('Ctrl Pts',(-0.173017958276288,0.417702301404717,
2.4539058293754)) ;
#77207=CARTESIAN_POINT('Ctrl Pts',(-0.295360129840502,0.295360129840502,
2.50351520437539)) ;
#77208=CARTESIAN_POINT('Ctrl Pts',(-0.417702301404717,0.173017958276288,
2.55312457937539)) ;
#77209=CARTESIAN_POINT('Ctrl Pts',(-0.417702301404716,2.55768893205885E-17,
2.60273395437539)) ;
#77210=CARTESIAN_POINT('Ctrl Pts',(-0.417702301404717,-0.173017958276288,
2.6523433293754)) ;
#77211=CARTESIAN_POINT('Ctrl Pts',(-0.295360129840502,-0.295360129840502,
2.70195270437539)) ;
#77212=CARTESIAN_POINT('Ctrl Pts',(-0.173017958276288,-0.417702301404717,
2.7515620793754)) ;
#77213=CARTESIAN_POINT('Ctrl Pts',(-5.1153778641177E-17,-0.417702301404716,
2.8011714543754)) ;
#77214=CARTESIAN_POINT('Ctrl Pts',(0.173017958276288,-0.417702301404716,
2.8507808293754)) ;
#77215=CARTESIAN_POINT('Ctrl Pts',(0.295360129840502,-0.295360129840502,
2.9003902043754)) ;
#77216=CARTESIAN_POINT('Ctrl Pts',(0.417702301404717,-0.173017958276288,
2.9499995793754)) ;
#77217=CARTESIAN_POINT('Ctrl Pts',(0.417702301404716,-7.67306679617654E-17,
2.9996089543754)) ;
#77218=CARTESIAN_POINT('Ctrl Pts',(0.417702301404717,0.173017958276288,
3.04921832937539)) ;
#77219=CARTESIAN_POINT('Ctrl Pts',(0.295360129840502,0.295360129840503,
3.0988277043754)) ;
#77220=CARTESIAN_POINT('Ctrl Pts',(0.173017958276288,0.417702301404717,
3.1484370793754)) ;
#77221=CARTESIAN_POINT('Ctrl Pts',(0.,0.417702301404716,3.1980464543754)) ;
#77222=CARTESIAN_POINT('Ctrl Pts',(-0.173017958276288,0.417702301404717,
3.2476558293754)) ;
#77223=CARTESIAN_POINT('Ctrl Pts',(-0.295360129840502,0.295360129840502,
3.29726520437539)) ;
#77224=CARTESIAN_POINT('Ctrl Pts',(-0.417702301404717,0.173017958276288,
3.3468745793754)) ;
#77225=CARTESIAN_POINT('Ctrl Pts',(-0.417702301404716,2.55768893205885E-17,
3.3964839543754)) ;
#77226=CARTESIAN_POINT('Ctrl Pts',(-0.417702301404717,-0.173017958276288,
3.44609332937539)) ;
#77227=CARTESIAN_POINT('Ctrl Pts',(-0.295360129840502,-0.295360129840502,
3.49570270437539)) ;
#77228=CARTESIAN_POINT('Ctrl Pts',(-0.173017958276288,-0.417702301404717,
3.5453120793754)) ;
#77229=CARTESIAN_POINT('Ctrl Pts',(-5.1153778641177E-17,-0.417702301404716,
3.59492145437539)) ;
#77230=CARTESIAN_POINT('Ctrl Pts',(0.173017958276288,-0.417702301404716,
3.64453082937539)) ;
#77231=CARTESIAN_POINT('Ctrl Pts',(0.295360129840502,-0.295360129840502,
3.6941402043754)) ;
#77232=CARTESIAN_POINT('Ctrl Pts',(0.417702301404717,-0.173017958276288,
3.74374957937539)) ;
#77233=CARTESIAN_POINT('Ctrl Pts',(0.417702301404716,-7.67306679617654E-17,
3.79335895437539)) ;
#77234=CARTESIAN_POINT('Ctrl Pts',(0.417702301404717,0.173017958276288,
3.84296832937539)) ;
#77235=CARTESIAN_POINT('Ctrl Pts',(0.295360129840502,0.295360129840503,
3.89257770437539)) ;
#77236=CARTESIAN_POINT('Ctrl Pts',(0.173017958276288,0.417702301404717,
3.9421870793754)) ;
#77237=CARTESIAN_POINT('Ctrl Pts',(0.,0.417702301404716,3.9917964543754)) ;
#77238=CARTESIAN_POINT('Ctrl Pts',(-0.173017958276288,0.417702301404717,
4.04140582937539)) ;
#77239=CARTESIAN_POINT('Ctrl Pts',(-0.295360129840502,0.295360129840502,
4.09101520437539)) ;
#77240=CARTESIAN_POINT('Ctrl Pts',(-0.417702301404717,0.173017958276288,
4.14062457937539)) ;
#77241=CARTESIAN_POINT('Ctrl Pts',(-0.417702301404716,2.55768893205885E-17,
4.1902339543754)) ;
#77242=CARTESIAN_POINT('Ctrl Pts',(-0.417702301404717,-0.173017958276288,
4.23984332937539)) ;
#77243=CARTESIAN_POINT('Ctrl Pts',(-0.295360129840502,-0.295360129840502,
4.28945270437539)) ;
#77244=CARTESIAN_POINT('Ctrl Pts',(-0.173017958276288,-0.417702301404717,
4.3390620793754)) ;
#77245=CARTESIAN_POINT('Ctrl Pts',(-5.1153778641177E-17,-0.417702301404716,
4.38867145437539)) ;
#77246=CARTESIAN_POINT('Ctrl Pts',(0.173017958276288,-0.417702301404716,
4.4382808293754)) ;
#77247=CARTESIAN_POINT('Ctrl Pts',(0.295360129840502,-0.295360129840502,
4.48789020437539)) ;
#77248=CARTESIAN_POINT('Ctrl Pts',(0.417702301404717,-0.173017958276288,
4.53749957937539)) ;
#77249=CARTESIAN_POINT('Ctrl Pts',(0.417702301404716,-7.67306679617654E-17,
4.58710895437539)) ;
#77250=CARTESIAN_POINT('Ctrl Pts',(0.417702301404717,0.173017958276288,
4.63671832937539)) ;
#77251=CARTESIAN_POINT('Ctrl Pts',(0.295360129840502,0.295360129840503,
4.6863277043754)) ;
#77252=CARTESIAN_POINT('Ctrl Pts',(0.173017958276288,0.417702301404717,
4.73593707937539)) ;
#77253=CARTESIAN_POINT('Ctrl Pts',(0.,0.417702301404716,4.78554645437539)) ;
#77254=CARTESIAN_POINT('Ctrl Pts',(-0.173017958276288,0.417702301404717,
4.8351558293754)) ;
#77255=CARTESIAN_POINT('Ctrl Pts',(-0.295360129840502,0.295360129840502,
4.88476520437539)) ;
#77256=CARTESIAN_POINT('Ctrl Pts',(-0.417702301404717,0.173017958276288,
4.9343745793754)) ;
#77257=CARTESIAN_POINT('Ctrl Pts',(-0.417702301404716,2.55768893205885E-17,
4.9839839543754)) ;
#77258=CARTESIAN_POINT('Ctrl Pts',(-0.417702301404717,-0.173017958276288,
5.03359332937539)) ;
#77259=CARTESIAN_POINT('Ctrl Pts',(-0.295360129840502,-0.295360129840502,
5.08320270437539)) ;
#77260=CARTESIAN_POINT('Ctrl Pts',(-0.173017958276288,-0.417702301404717,
5.13281207937539)) ;
#77261=CARTESIAN_POINT('Ctrl Pts',(-5.1153778641177E-17,-0.417702301404716,
5.1824214543754)) ;
#77262=CARTESIAN_POINT('Ctrl Pts',(0.173017958276288,-0.417702301404716,
5.23203082937539)) ;
#77263=CARTESIAN_POINT('Ctrl Pts',(0.295360129840502,-0.295360129840502,
5.28164020437539)) ;
#77264=CARTESIAN_POINT('Ctrl Pts',(0.417702301404717,-0.173017958276288,
5.33124957937539)) ;
#77265=CARTESIAN_POINT('Ctrl Pts',(0.417702301404716,-7.67306679617654E-17,
5.3808589543754)) ;
#77266=CARTESIAN_POINT('Ctrl Pts',(0.417702301404717,0.173017958276288,
5.4304683293754)) ;
#77267=CARTESIAN_POINT('Ctrl Pts',(0.295360129840502,0.295360129840503,
5.4800777043754)) ;
#77268=CARTESIAN_POINT('Ctrl Pts',(0.173017958276288,0.417702301404717,
5.5296870793754)) ;
#77269=CARTESIAN_POINT('Ctrl Pts',(0.,0.417702301404716,5.57929645437539)) ;
#77270=CARTESIAN_POINT('Ctrl Pts',(-0.173017958276288,0.417702301404717,
5.62890582937539)) ;
#77271=CARTESIAN_POINT('Ctrl Pts',(-0.295360129840502,0.295360129840502,
5.6785152043754)) ;
#77272=CARTESIAN_POINT('Ctrl Pts',(-0.417702301404717,0.173017958276288,
5.72812457937539)) ;
#77273=CARTESIAN_POINT('Ctrl Pts',(-0.417702301404716,2.55768893205885E-17,
5.77773395437539)) ;
#77274=CARTESIAN_POINT('Ctrl Pts',(-0.417702301404717,-0.173017958276288,
5.82734332937539)) ;
#77275=CARTESIAN_POINT('Ctrl Pts',(-0.295360129840502,-0.295360129840502,
5.87695270437539)) ;
#77276=CARTESIAN_POINT('Ctrl Pts',(-0.173017958276288,-0.417702301404717,
5.9265620793754)) ;
#77277=CARTESIAN_POINT('Ctrl Pts',(-5.1153778641177E-17,-0.417702301404716,
5.97617145437539)) ;
#77278=CARTESIAN_POINT('Ctrl Pts',(0.173017958276288,-0.417702301404716,
6.0257808293754)) ;
#77279=CARTESIAN_POINT('Ctrl Pts',(0.295360129840502,-0.295360129840502,
6.0753902043754)) ;
#77280=CARTESIAN_POINT('Ctrl Pts',(0.417702301404717,-0.173017958276288,
6.12499957937539)) ;
#77281=CARTESIAN_POINT('Ctrl Pts',(0.417702301404716,-7.67306679617654E-17,
6.1746089543754)) ;
#77282=CARTESIAN_POINT('Ctrl Pts',(0.417702301404717,0.173017958276288,
6.22421832937539)) ;
#77283=CARTESIAN_POINT('Ctrl Pts',(0.295360129840502,0.295360129840503,
6.27382770437539)) ;
#77284=CARTESIAN_POINT('Ctrl Pts',(0.173017958276288,0.417702301404717,
6.3234370793754)) ;
#77285=CARTESIAN_POINT('Ctrl Pts',(0.,0.417702301404716,6.3730464543754)) ;
#77286=CARTESIAN_POINT('Ctrl Pts',(-0.194635088947967,-1.22163646928409,
0.0797567518094009)) ;
#77287=CARTESIAN_POINT('Ctrl Pts',(-0.0043082693312935,-1.30090248401962,
0.128089684784921)) ;
#77288=CARTESIAN_POINT('Ctrl Pts',(0.17965409482365,-1.316658036297,0.165447546864525)) ;
#77289=CARTESIAN_POINT('Ctrl Pts',(0.484008391354344,-1.31323795873721,
0.23199194234403)) ;
#77290=CARTESIAN_POINT('Ctrl Pts',(0.655998289214855,-1.27815569745546,
0.269189612454462)) ;
#77291=CARTESIAN_POINT('Ctrl Pts',(1.01370529834126,-1.13088907272712,0.347108578180816)) ;
#77292=CARTESIAN_POINT('Ctrl Pts',(1.17648098544676,-1.01084917584401,0.382416490912591)) ;
#77293=CARTESIAN_POINT('Ctrl Pts',(1.42251858408678,-0.760738367422026,
0.448222681167146)) ;
#77294=CARTESIAN_POINT('Ctrl Pts',(1.51694609891737,-0.630767018075734,
0.478024324337763)) ;
#77295=CARTESIAN_POINT('Ctrl Pts',(1.7004605039317,-0.277947938509247,0.549796632634112)) ;
#77296=CARTESIAN_POINT('Ctrl Pts',(1.73763017634033,-0.0925850035561787,
0.580342676340329)) ;
#77297=CARTESIAN_POINT('Ctrl Pts',(1.7526,-3.21947397027848E-16,0.5953125)) ;
#77298=CARTESIAN_POINT('Origin',(0.,-2.985516,6.35)) ;
#77299=CARTESIAN_POINT('Ctrl Pts',(-1.94288959754296,-0.448102752174796,
7.0818)) ;
#77300=CARTESIAN_POINT('Ctrl Pts',(-1.94270197516804,-0.44756275002075,
7.0818)) ;
#77301=CARTESIAN_POINT('Ctrl Pts',(-1.94251230527771,-0.447017983233947,
7.08179766992681)) ;
#77302=CARTESIAN_POINT('Ctrl Pts',(-1.91803916780255,-0.376442475898735,
7.08160456336027)) ;
#77303=CARTESIAN_POINT('Ctrl Pts',(-1.88761451839117,-0.293719590124047,
7.05576035709451)) ;
#77304=CARTESIAN_POINT('Ctrl Pts',(-1.87819429271644,-0.268591723493095,
7.00768190451026)) ;
#77305=CARTESIAN_POINT('Ctrl Pts',(-1.94288959754296,-0.448102752174796,
7.0818)) ;
#77306=CARTESIAN_POINT('Ctrl Pts',(-1.94252901127664,-0.44757378511647,
7.0818)) ;
#77307=CARTESIAN_POINT('Ctrl Pts',(-1.94238760924975,-0.447241733483015,
7.08171624908906)) ;
#77308=CARTESIAN_POINT('Ctrl Pts',(-1.90274378880994,-0.385137079174368,
7.0842962048653)) ;
#77309=CARTESIAN_POINT('Ctrl Pts',(-1.86635603372515,-0.320809755584884,
7.03323707646529)) ;
#77310=CARTESIAN_POINT('Ctrl Pts',(-1.86932161172289,-0.312347136547012,
6.9980193066578)) ;
#77311=CARTESIAN_POINT('Ctrl Pts',(-1.94288959754296,-0.448102752174796,
7.0818)) ;
#77312=CARTESIAN_POINT('Ctrl Pts',(-1.94245161464451,-0.447640464231361,
7.0818)) ;
#77313=CARTESIAN_POINT('Ctrl Pts',(-1.94216670833245,-0.447413283195794,
7.08171624908906)) ;
#77314=CARTESIAN_POINT('Ctrl Pts',(-1.89052514974837,-0.394910453248505,
7.08429620486504)) ;
#77315=CARTESIAN_POINT('Ctrl Pts',(-1.8347389543407,-0.347957809715575,
7.0332370764653)) ;
#77316=CARTESIAN_POINT('Ctrl Pts',(-1.82714531063845,-0.348921084254559,
6.9980193066578)) ;
#77317=CARTESIAN_POINT('Ctrl Pts',(-1.94288959754296,-0.448102752174796,
7.0818)) ;
#77318=CARTESIAN_POINT('Ctrl Pts',(-1.94240557475944,-0.447798570605971,
7.0818)) ;
#77319=CARTESIAN_POINT('Ctrl Pts',(-1.94191738994489,-0.447492388347843,
7.08179766992681)) ;
#77320=CARTESIAN_POINT('Ctrl Pts',(-1.87864342769047,-0.407664231468328,
7.08160456336)) ;
#77321=CARTESIAN_POINT('Ctrl Pts',(-1.80491723090524,-0.364392752089199,
7.05576035709452)) ;
#77322=CARTESIAN_POINT('Ctrl Pts',(-1.78257449869962,-0.351510169545915,
7.00768190451026)) ;
#77323=CARTESIAN_POINT('',(-1.78257449869962,-0.35151016954591,7.00768190451024)) ;
#77324=CARTESIAN_POINT('',(-1.87819429271644,-0.268591723493095,7.00768190451026)) ;
#77325=CARTESIAN_POINT('Origin',(-1.78257449869962,-0.254917586917006,7.03356380902051)) ;
#77326=CARTESIAN_POINT('',(-1.89249580907583,-0.307272596057229,7.04638255392192)) ;
#77327=CARTESIAN_POINT('Origin',(-1.98523598945348,-0.564759059977123,6.9430176984354)) ;
#77328=CARTESIAN_POINT('',(-1.91807183825027,-0.377810206882459,7.07388013398117)) ;
#77329=CARTESIAN_POINT('Origin',(-1.9365430293827,-0.434616459037521,6.99727618798715)) ;
#77330=CARTESIAN_POINT('',(-1.94182783334028,-0.445044808441315,7.08178867415542)) ;
#77331=CARTESIAN_POINT('Origin',(-1.92795162512393,-0.413874762423167,7.02228347025522)) ;
#77332=CARTESIAN_POINT('',(-1.94288959754296,-0.448102752174818,7.0818)) ;
#77333=CARTESIAN_POINT('',(-1.94182783307279,-0.445044807670936,7.08178867415257)) ;
#77334=CARTESIAN_POINT('',(-1.94014976372661,-0.4463802141404,7.08178692473713)) ;
#77335=CARTESIAN_POINT('',(-1.94288959754295,-0.448102752174801,7.0818)) ;
#77336=CARTESIAN_POINT('',(-1.87964216948038,-0.409078843661158,7.07382903170985)) ;
#77337=CARTESIAN_POINT('Origin',(-1.92743649770787,-0.446270284367414,6.99208610043499)) ;
#77338=CARTESIAN_POINT('',(-1.81813539254511,-0.372312156582617,7.04714690179984)) ;
#77339=CARTESIAN_POINT('Origin',(-1.9325040879477,-0.44453393011351,6.99487389856661)) ;
#77340=CARTESIAN_POINT('Origin',(-2.04686400773891,-0.509803748797932,6.94140176115792)) ;
#77341=CARTESIAN_POINT('Ctrl Pts',(-1.87819429271643,-0.268591723493085,
7.00768190451022)) ;
#77342=CARTESIAN_POINT('Ctrl Pts',(-1.87559269584778,-0.265429455820014,
6.99639968079939)) ;
#77343=CARTESIAN_POINT('Ctrl Pts',(-1.87277553216538,-0.263323474391198,
6.98489826419215)) ;
#77344=CARTESIAN_POINT('Ctrl Pts',(-1.86979680842784,-0.262281765411183,
6.97334924403636)) ;
#77345=CARTESIAN_POINT('Ctrl Pts',(-1.87312418929155,-0.293594816666754,
7.00216042002311)) ;
#77346=CARTESIAN_POINT('Ctrl Pts',(-1.87084473493899,-0.291084530404652,
6.99224479183829)) ;
#77347=CARTESIAN_POINT('Ctrl Pts',(-1.86834496343776,-0.289501530632308,
6.98216124843708)) ;
#77348=CARTESIAN_POINT('Ctrl Pts',(-1.86572206147513,-0.288873179727176,
6.97207530474358)) ;
#77349=CARTESIAN_POINT('Ctrl Pts',(-1.84631328088201,-0.334524427261344,
6.9974230667741)) ;
#77350=CARTESIAN_POINT('Ctrl Pts',(-1.84417962418044,-0.333091612281746,
6.98998909901151)) ;
#77351=CARTESIAN_POINT('Ctrl Pts',(-1.84187319629001,-0.332400676673093,
6.98249471608034)) ;
#77352=CARTESIAN_POINT('Ctrl Pts',(-1.83942120369611,-0.332407181519401,
6.97506009028094)) ;
#77353=CARTESIAN_POINT('Ctrl Pts',(-1.80167627524482,-0.350400561563901,
7.0035407911449)) ;
#77354=CARTESIAN_POINT('Ctrl Pts',(-1.79920012229604,-0.349063108054369,
6.9975751162926)) ;
#77355=CARTESIAN_POINT('Ctrl Pts',(-1.79652736146151,-0.348276516130449,
6.99152359092133)) ;
#77356=CARTESIAN_POINT('Ctrl Pts',(-1.79370245617676,-0.348044577753767,
6.98550115761471)) ;
#77357=CARTESIAN_POINT('Ctrl Pts',(-1.78257449869961,-0.35151016954591,
7.00768190451025)) ;
#77358=CARTESIAN_POINT('Ctrl Pts',(-1.77995299478772,-0.34999863817984,
7.00204079265483)) ;
#77359=CARTESIAN_POINT('Ctrl Pts',(-1.77712384321892,-0.348988486534664,
6.99629008435121)) ;
#77360=CARTESIAN_POINT('Ctrl Pts',(-1.77414072885052,-0.348483282365518,
6.99051557427332)) ;
#77361=CARTESIAN_POINT('',(-1.77414072885053,-0.348483282365581,6.99051557427404)) ;
#77362=CARTESIAN_POINT('',(-1.86979680842784,-0.262281765411183,6.97334924403636)) ;
#77363=CARTESIAN_POINT('Origin',(-1.77414072885052,-0.248863812556215,6.99923114854662)) ;
#77364=CARTESIAN_POINT('Origin',(-1.84377759622581,-0.424925231995625,6.96360853180443)) ;
#77365=CARTESIAN_POINT('Origin',(-1.74961486668251,-0.42410100616838,6.98537442847036)) ;
#77366=CARTESIAN_POINT('Ctrl Pts',(-1.72771014821048,-0.332764968591514,
6.81085442572523)) ;
#77367=CARTESIAN_POINT('Ctrl Pts',(-1.74319473414623,-0.338004233132819,
6.87073949346036)) ;
#77368=CARTESIAN_POINT('Ctrl Pts',(-1.75867139282682,-0.343243675639426,
6.93062659534819)) ;
#77369=CARTESIAN_POINT('Ctrl Pts',(-1.77414072885052,-0.348483282365389,
6.99051557427185)) ;
#77370=CARTESIAN_POINT('Ctrl Pts',(-1.75388379891716,-0.332177363448602,
6.80413806820838)) ;
#77371=CARTESIAN_POINT('Ctrl Pts',(-1.76933665987689,-0.337416538558189,
6.86403381882623)) ;
#77372=CARTESIAN_POINT('Ctrl Pts',(-1.78478377705788,-0.342658817603973,
6.92393065445506)) ;
#77373=CARTESIAN_POINT('Ctrl Pts',(-1.80022303195211,-0.347898342882965,
6.98382968539379)) ;
#77374=CARTESIAN_POINT('Ctrl Pts',(-1.79938284222792,-0.310992589547657,
6.79422672914051)) ;
#77375=CARTESIAN_POINT('Ctrl Pts',(-1.81478360858998,-0.316286258253172,
6.85413545484315)) ;
#77376=CARTESIAN_POINT('Ctrl Pts',(-1.8301777875902,-0.321577463411775,
6.91404581861747)) ;
#77377=CARTESIAN_POINT('Ctrl Pts',(-1.84556760072685,-0.326868409115673,
6.97395705441162)) ;
#77378=CARTESIAN_POINT('Ctrl Pts',(-1.82046616955548,-0.266091328799139,
6.79270352788241)) ;
#77379=CARTESIAN_POINT('Ctrl Pts',(-1.83589739021241,-0.271473267897804,
6.85259865161434)) ;
#77380=CARTESIAN_POINT('Ctrl Pts',(-1.85132258737841,-0.276850760615209,
6.91249534127297)) ;
#77381=CARTESIAN_POINT('Ctrl Pts',(-1.86674074821324,-0.282225326148102,
6.9723937895665)) ;
#77382=CARTESIAN_POINT('Ctrl Pts',(-1.82343508275074,-0.246063080838804,
6.79368809548975)) ;
#77383=CARTESIAN_POINT('Ctrl Pts',(-1.83889654046897,-0.251473735590624,
6.85357316322487)) ;
#77384=CARTESIAN_POINT('Ctrl Pts',(-1.85435024060401,-0.256879845047546,
6.9134602651127)) ;
#77385=CARTESIAN_POINT('Ctrl Pts',(-1.86979680842784,-0.262281765411184,
6.97334924403636)) ;
#77386=CARTESIAN_POINT('',(-1.72771014821048,-0.332764968591514,6.81085442572523)) ;
#77387=CARTESIAN_POINT('',(-1.77414072885052,-0.348483282365389,6.99051557427185)) ;
#77388=CARTESIAN_POINT('',(-1.82343508275074,-0.246063080838804,6.79368809548975)) ;
#77389=CARTESIAN_POINT('Origin',(-1.72771014821048,-0.233145498782339,6.81957)) ;
#77390=CARTESIAN_POINT('',(-1.82343508275074,-0.246063080838804,6.79368809548975)) ;
#77391=CARTESIAN_POINT('Origin',(-1.72771014821048,-0.233145498782339,6.81957)) ;
#77392=CARTESIAN_POINT('',(-1.72771014821048,-0.233145498782339,6.71957)) ;
#77393=CARTESIAN_POINT('Origin',(-1.72771014821048,-0.233145498782339,6.81957)) ;
#77394=CARTESIAN_POINT('Origin',(-1.72771014821048,-0.233145498782339,6.81957)) ;
#77395=CARTESIAN_POINT('Origin',(-3.54734504026457E-15,-0.507999999999988,
8.8138)) ;
#77396=CARTESIAN_POINT('',(-1.17871069663557,-0.348483282365649,6.99051557427477)) ;
#77397=CARTESIAN_POINT('',(4.7625,-0.34848328236569,6.99051557427477)) ;
#77398=CARTESIAN_POINT('',(-1.17558412963155,-0.332764968591518,6.81085442572523)) ;
#77399=CARTESIAN_POINT('',(-1.21039177030076,-0.507754795155569,8.81099729580349)) ;
#77400=CARTESIAN_POINT('',(-2.32368535611608E-15,-0.332764968591526,6.81085442572523)) ;
#77401=CARTESIAN_POINT('Origin',(4.7625,-0.448102752174865,6.9818)) ;
#77402=CARTESIAN_POINT('',(-1.17871069663558,-0.448102752174823,7.0818)) ;
#77403=CARTESIAN_POINT('',(4.7625,-0.448102752174865,7.0818)) ;
#77404=CARTESIAN_POINT('Origin',(-1.17871069663558,-0.448102752174823,6.9818)) ;
#77405=CARTESIAN_POINT('Origin',(-4.45650581216736E-16,7.57196551496331E-15,
6.98180000000001)) ;
#77406=CARTESIAN_POINT('',(-1.87819429271644,0.268591723493141,7.00768190451026)) ;
#77407=CARTESIAN_POINT('Origin',(0.,7.3282997741086E-15,7.00768190451026)) ;
#77408=CARTESIAN_POINT('',(-1.93516376196126,0.425958697938772,7.08103018110414)) ;
#77409=CARTESIAN_POINT('Ctrl Pts',(-1.93516376196126,0.425958697938772,
7.08103018110414)) ;
#77410=CARTESIAN_POINT('Ctrl Pts',(-1.91237404551335,0.361043831880854,
7.07642065497011)) ;
#77411=CARTESIAN_POINT('Ctrl Pts',(-1.88670733098046,0.291299724077108,
7.05113030167797)) ;
#77412=CARTESIAN_POINT('Ctrl Pts',(-1.87819429271644,0.268591723493142,
7.00768190451026)) ;
#77413=CARTESIAN_POINT('',(-1.94288959754295,0.448102752174865,7.0818)) ;
#77414=CARTESIAN_POINT('Ctrl Pts',(-1.94288959754295,0.448102752174872,
7.0818)) ;
#77415=CARTESIAN_POINT('Ctrl Pts',(-1.94270198330611,0.44756277344327,7.0818)) ;
#77416=CARTESIAN_POINT('Ctrl Pts',(-1.94251232165803,0.447018030321751,
7.08179767010457)) ;
#77417=CARTESIAN_POINT('Ctrl Pts',(-1.9399882560469,0.43973914278705,7.08177775516638)) ;
#77418=CARTESIAN_POINT('Ctrl Pts',(-1.93759234469623,0.432876340960395,
7.08152139456926)) ;
#77419=CARTESIAN_POINT('Ctrl Pts',(-1.93516376196126,0.425958697938772,
7.08103018110414)) ;
#77420=CARTESIAN_POINT('Origin',(-4.45650581216736E-16,7.57196551496331E-15,
7.0818)) ;
#77421=CARTESIAN_POINT('Origin',(-1.72771014821048,0.233145498782383,6.81957)) ;
#77422=CARTESIAN_POINT('',(-1.72771014821048,0.332764968591557,6.81085442572523)) ;
#77423=CARTESIAN_POINT('',(-1.82343508275074,0.246063080838849,6.79368809548975)) ;
#77424=CARTESIAN_POINT('Origin',(-1.72771014821048,0.233145498782383,6.81957)) ;
#77425=CARTESIAN_POINT('',(-1.72771014821048,0.233145498782383,6.71957)) ;
#77426=CARTESIAN_POINT('Origin',(-1.72771014821048,0.233145498782383,6.81957)) ;
#77427=CARTESIAN_POINT('Origin',(-1.72771014821048,0.233145498782383,6.81957)) ;
#77428=CARTESIAN_POINT('Ctrl Pts',(-1.82343508274976,0.246063080838507,
6.79368809548596)) ;
#77429=CARTESIAN_POINT('Ctrl Pts',(-1.8388965404683,0.251473735590436,6.85357316322228)) ;
#77430=CARTESIAN_POINT('Ctrl Pts',(-1.85435024060365,0.256879845047465,
6.91346026511131)) ;
#77431=CARTESIAN_POINT('Ctrl Pts',(-1.86979680842779,0.262281765411211,
6.97334924403617)) ;
#77432=CARTESIAN_POINT('Ctrl Pts',(-1.81947653182275,0.272767411452289,
6.79237533867617)) ;
#77433=CARTESIAN_POINT('Ctrl Pts',(-1.83489694400734,0.278139250484315,
6.85227406114401)) ;
#77434=CARTESIAN_POINT('Ctrl Pts',(-1.85031405219097,0.283508230262916,
6.91217346932062)) ;
#77435=CARTESIAN_POINT('Ctrl Pts',(-1.86572206147498,0.288873179727103,
6.97207530474301)) ;
#77436=CARTESIAN_POINT('Ctrl Pts',(-1.79322013108717,0.316574402604316,
6.79533188669133)) ;
#77437=CARTESIAN_POINT('Ctrl Pts',(-1.80862659259988,0.321853195169872,
6.85523985899826)) ;
#77438=CARTESIAN_POINT('Ctrl Pts',(-1.82402601364689,0.327130342614484,
6.91514954549618)) ;
#77439=CARTESIAN_POINT('Ctrl Pts',(-1.83942125592947,0.332407254608791,
6.97506007039325)) ;
#77440=CARTESIAN_POINT('Ctrl Pts',(-1.74734038623951,0.332324264734042,
6.8058171575838)) ;
#77441=CARTESIAN_POINT('Ctrl Pts',(-1.76280167491966,0.337563919259398,
6.86571006109106)) ;
#77442=CARTESIAN_POINT('Ctrl Pts',(-1.77825521655385,0.342804601986218,
6.92560480456484)) ;
#77443=CARTESIAN_POINT('Ctrl Pts',(-1.79370245617666,0.348044577753599,
6.98550115761311)) ;
#77444=CARTESIAN_POINT('Ctrl Pts',(-1.7277101482095,0.332764968591226,6.81085442572145)) ;
#77445=CARTESIAN_POINT('Ctrl Pts',(-1.74319473414556,0.338004233132636,
6.87073949345777)) ;
#77446=CARTESIAN_POINT('Ctrl Pts',(-1.75867139282645,0.343243675639348,
6.93062659534679)) ;
#77447=CARTESIAN_POINT('Ctrl Pts',(-1.77414072885046,0.348483282365417,
6.99051557427166)) ;
#77448=CARTESIAN_POINT('',(-1.77414072885046,0.348483282365553,6.99051557427321)) ;
#77449=CARTESIAN_POINT('',(-1.86979680842779,0.262281765411211,6.97334924403617)) ;
#77450=CARTESIAN_POINT('Origin',(-1.77414072885046,0.248863812556242,6.99923114854642)) ;
#77451=CARTESIAN_POINT('',(-1.86979680842779,0.262281765411211,6.97334924403617)) ;
#77452=CARTESIAN_POINT('',(-1.7277101482095,0.332764968591226,6.81085442572145)) ;
#77453=CARTESIAN_POINT('Ctrl Pts',(-1.78257449869961,0.351510169545958,
7.00768190451026)) ;
#77454=CARTESIAN_POINT('Ctrl Pts',(-1.7799529947877,0.349998638179875,7.0020407926548)) ;
#77455=CARTESIAN_POINT('Ctrl Pts',(-1.77712384321888,0.348988486534698,
6.99629008435115)) ;
#77456=CARTESIAN_POINT('Ctrl Pts',(-1.77414072885046,0.348483282365553,
6.99051557427321)) ;
#77457=CARTESIAN_POINT('Ctrl Pts',(-1.80804353409323,0.350030692236613,
7.00216042002313)) ;
#77458=CARTESIAN_POINT('Ctrl Pts',(-1.80562039408462,0.348758544781101,
6.99609033866213)) ;
#77459=CARTESIAN_POINT('Ctrl Pts',(-1.80298985197567,0.348031691489769,
6.98992923493179)) ;
#77460=CARTESIAN_POINT('Ctrl Pts',(-1.80022303195211,0.347898342883226,
6.98382968539506)) ;
#77461=CARTESIAN_POINT('Ctrl Pts',(-1.85235642894571,0.329284001344761,
6.99742306677412)) ;
#77462=CARTESIAN_POINT('Ctrl Pts',(-1.85025698915433,0.327717973988231,
6.98963152733253)) ;
#77463=CARTESIAN_POINT('Ctrl Pts',(-1.84798352930075,0.326928615466665,
6.98177037827478)) ;
#77464=CARTESIAN_POINT('Ctrl Pts',(-1.84556753758067,0.326868345860465,
6.97395707625727)) ;
#77465=CARTESIAN_POINT('Ctrl Pts',(-1.87439171514777,0.287344043373391,
7.00354079114492)) ;
#77466=CARTESIAN_POINT('Ctrl Pts',(-1.87202794762724,0.284665751804286,
6.99328116783748)) ;
#77467=CARTESIAN_POINT('Ctrl Pts',(-1.86945702547209,0.282962222021335,
6.98284900252258)) ;
#77468=CARTESIAN_POINT('Ctrl Pts',(-1.86674074821325,0.282225326148211,
6.9723937895666)) ;
#77469=CARTESIAN_POINT('Ctrl Pts',(-1.87819429271644,0.268591723493141,
7.00768190451026)) ;
#77470=CARTESIAN_POINT('Ctrl Pts',(-1.87559269584777,0.265429455820045,
6.99639968079935)) ;
#77471=CARTESIAN_POINT('Ctrl Pts',(-1.87277553216535,0.263323474391225,
6.98489826419204)) ;
#77472=CARTESIAN_POINT('Ctrl Pts',(-1.86979680842779,0.262281765411211,
6.97334924403617)) ;
#77473=CARTESIAN_POINT('',(-1.78257449869961,0.351510169545958,7.00768190451026)) ;
#77474=CARTESIAN_POINT('Origin',(-1.74961486676053,0.424101005970564,6.98537442850825)) ;
#77475=CARTESIAN_POINT('Origin',(-1.78257449869961,0.254917586917051,7.03356380902051)) ;
#77476=CARTESIAN_POINT('Origin',(-1.8437775962501,0.424925231867001,6.96360853182487)) ;
#77477=CARTESIAN_POINT('Ctrl Pts',(-1.87819429271644,0.268591723493142,
7.00768190451026)) ;
#77478=CARTESIAN_POINT('Ctrl Pts',(-1.88761452163364,0.293719598773215,
7.0557603736433)) ;
#77479=CARTESIAN_POINT('Ctrl Pts',(-1.91803918303173,0.376442517983045,
7.08160457645398)) ;
#77480=CARTESIAN_POINT('Ctrl Pts',(-1.94251232165803,0.447018030321751,
7.08179767010457)) ;
#77481=CARTESIAN_POINT('Ctrl Pts',(-1.94270198330611,0.44756277344327,7.0818)) ;
#77482=CARTESIAN_POINT('Ctrl Pts',(-1.94288959754295,0.448102752174872,
7.0818)) ;
#77483=CARTESIAN_POINT('Ctrl Pts',(-1.87312418929155,0.293594816666808,
7.00216042002314)) ;
#77484=CARTESIAN_POINT('Ctrl Pts',(-1.87796531081865,0.311402705036892,
7.04213224265873)) ;
#77485=CARTESIAN_POINT('Ctrl Pts',(-1.90981006048309,0.381903712030246,
7.08210548357769)) ;
#77486=CARTESIAN_POINT('Ctrl Pts',(-1.9424029083422,0.447111003798291,7.08179401271422)) ;
#77487=CARTESIAN_POINT('Ctrl Pts',(-1.94264552853424,0.447607689701659,
7.0818)) ;
#77488=CARTESIAN_POINT('Ctrl Pts',(-1.94288959754295,0.448102752174872,
7.0818)) ;
#77489=CARTESIAN_POINT('Ctrl Pts',(-1.84631288834535,0.334523890843312,
6.99742330171556)) ;
#77490=CARTESIAN_POINT('Ctrl Pts',(-1.85235243119885,0.341052363542256,
7.03081187673423)) ;
#77491=CARTESIAN_POINT('Ctrl Pts',(-1.89649530788188,0.39165635273821,7.08258953702512)) ;
#77492=CARTESIAN_POINT('Ctrl Pts',(-1.94220561752678,0.447272672620756,
7.08179067948989)) ;
#77493=CARTESIAN_POINT('Ctrl Pts',(-1.94254673268347,0.447686293153841,
7.0818)) ;
#77494=CARTESIAN_POINT('Ctrl Pts',(-1.94288959754295,0.448102752174872,
7.0818)) ;
#77495=CARTESIAN_POINT('Ctrl Pts',(-1.80167627524482,0.350400561563948,
7.00354079114491)) ;
#77496=CARTESIAN_POINT('Ctrl Pts',(-1.81914768429023,0.359424731059564,
7.04558504389613)) ;
#77497=CARTESIAN_POINT('Ctrl Pts',(-1.88400085756141,0.402627171214686,
7.08196334045253)) ;
#77498=CARTESIAN_POINT('Ctrl Pts',(-1.94200387814168,0.4474277521,7.0817950153739)) ;
#77499=CARTESIAN_POINT('Ctrl Pts',(-1.9424479368327,0.447764896606022,7.0818)) ;
#77500=CARTESIAN_POINT('Ctrl Pts',(-1.94288959754295,0.448102752174872,
7.0818)) ;
#77501=CARTESIAN_POINT('Ctrl Pts',(-1.78257449869961,0.351510169545957,
7.00768190451025)) ;
#77502=CARTESIAN_POINT('Ctrl Pts',(-1.80491723859567,0.364392756523483,
7.0557603736433)) ;
#77503=CARTESIAN_POINT('Ctrl Pts',(-1.87864346527326,0.40766425386111,7.08160457645373)) ;
#77504=CARTESIAN_POINT('Ctrl Pts',(-1.94191743214594,0.447492414836652,
7.08179767010457)) ;
#77505=CARTESIAN_POINT('Ctrl Pts',(-1.9424055957538,0.447798583799814,7.0818)) ;
#77506=CARTESIAN_POINT('Ctrl Pts',(-1.94288959754295,0.448102752174872,
7.0818)) ;
#77507=CARTESIAN_POINT('',(-1.92349887676128,0.435977594947785,7.0810654941764)) ;
#77508=CARTESIAN_POINT('Ctrl Pts',(-1.78257449869961,0.351510169545957,
7.00768190451025)) ;
#77509=CARTESIAN_POINT('Ctrl Pts',(-1.80281774439844,0.363182210425264,
7.05124255409984)) ;
#77510=CARTESIAN_POINT('Ctrl Pts',(-1.8652414202704,0.399800345697346,7.07655121308281)) ;
#77511=CARTESIAN_POINT('Ctrl Pts',(-1.92349887676128,0.435977594947785,
7.0810654941764)) ;
#77512=CARTESIAN_POINT('Ctrl Pts',(-1.92349887676128,0.435977594947785,
7.0810654941764)) ;
#77513=CARTESIAN_POINT('Ctrl Pts',(-1.92954095092606,0.439729657537118,
7.08153368525118)) ;
#77514=CARTESIAN_POINT('Ctrl Pts',(-1.93553821134988,0.443476977756891,
7.08177820258746)) ;
#77515=CARTESIAN_POINT('Ctrl Pts',(-1.94191743214594,0.447492414836652,
7.08179767010457)) ;
#77516=CARTESIAN_POINT('Ctrl Pts',(-1.9424055957538,0.447798583799814,7.0818)) ;
#77517=CARTESIAN_POINT('Ctrl Pts',(-1.94288959754295,0.448102752174872,
7.0818)) ;
#77518=CARTESIAN_POINT('Origin',(4.76250000000001,0.448102752174797,6.9818)) ;
#77519=CARTESIAN_POINT('',(-1.17871069663556,0.348483282365683,6.99051557427477)) ;
#77520=CARTESIAN_POINT('',(4.76250000000001,0.348483282365622,6.99051557427477)) ;
#77521=CARTESIAN_POINT('',(-1.17871069663556,0.448102752174857,7.0818)) ;
#77522=CARTESIAN_POINT('Origin',(-1.17871069663556,0.448102752174857,6.9818)) ;
#77523=CARTESIAN_POINT('',(4.76250000000001,0.448102752174797,7.0818)) ;
#77524=CARTESIAN_POINT('Origin',(9.40062917021727E-15,0.508000000000005,
8.8138)) ;
#77525=CARTESIAN_POINT('',(-1.17558412963153,0.332764968591552,6.81085442572523)) ;
#77526=CARTESIAN_POINT('',(5.49947457873019E-15,0.33276496859154,6.81085442572523)) ;
#77527=CARTESIAN_POINT('',(-1.21039177030074,0.507754795155606,8.81099729580349)) ;
#77528=CARTESIAN_POINT('Origin',(4.4887220033037E-15,0.233145498782365,
6.81957)) ;
#77529=CARTESIAN_POINT('',(-1.13595304047784,0.233145498782376,6.71957)) ;
#77530=CARTESIAN_POINT('',(4.4887220033037E-15,0.233145498782365,6.71957)) ;
#77531=CARTESIAN_POINT('Origin',(-1.13595304047784,0.233145498782377,6.81957)) ;
#77532=CARTESIAN_POINT('Origin',(9.525,-0.761999999999999,7.0818)) ;
#77533=CARTESIAN_POINT('',(-0.662097436533287,0.662040915604455,7.08180000837043)) ;
#77534=CARTESIAN_POINT('',(3.59929774852521,2.42721865129353,7.0818)) ;
#77535=CARTESIAN_POINT('',(0.,0.662,7.0818)) ;
#77536=CARTESIAN_POINT('',(-0.662097436318068,-0.66204091586428,7.08180000837054)) ;
#77537=CARTESIAN_POINT('',(0.,-0.662,7.0818)) ;
#77538=CARTESIAN_POINT('',(3.86870543215719,-2.5388109676615,7.0818)) ;
#77539=CARTESIAN_POINT('Ctrl Pts',(-0.611939867549494,0.558026198990156,
6.81085442572523)) ;
#77540=CARTESIAN_POINT('Ctrl Pts',(-0.606991841672513,0.555410694880575,
6.7615916062195)) ;
#77541=CARTESIAN_POINT('Ctrl Pts',(-0.55434393568323,0.527581249784821,
6.71957)) ;
#77542=CARTESIAN_POINT('Ctrl Pts',(-0.497571705638597,0.497571705638616,
6.71957)) ;
#77543=CARTESIAN_POINT('Ctrl Pts',(-0.587896866738722,0.568073880351635,
6.81179156524867)) ;
#77544=CARTESIAN_POINT('Ctrl Pts',(-0.584594051674633,0.565801572147184,
6.76779239028237)) ;
#77545=CARTESIAN_POINT('Ctrl Pts',(-0.545423040383754,0.536502145084297,
6.71957)) ;
#77546=CARTESIAN_POINT('Ctrl Pts',(-0.497571705638597,0.497571705638616,
6.71957)) ;
#77547=CARTESIAN_POINT('Ctrl Pts',(-0.568073880351614,0.587896866738742,
6.81179156524867)) ;
#77548=CARTESIAN_POINT('Ctrl Pts',(-0.565801572147164,0.584594051674654,
6.76779239028237)) ;
#77549=CARTESIAN_POINT('Ctrl Pts',(-0.536502145084278,0.545423040383773,
6.71957)) ;
#77550=CARTESIAN_POINT('Ctrl Pts',(-0.497571705638597,0.497571705638616,
6.71957)) ;
#77551=CARTESIAN_POINT('Ctrl Pts',(-0.558026198990135,0.611939867549514,
6.81085442572523)) ;
#77552=CARTESIAN_POINT('Ctrl Pts',(-0.555410694880554,0.606991841672533,
6.7615916062195)) ;
#77553=CARTESIAN_POINT('Ctrl Pts',(-0.527581249784801,0.55434393568325,
6.71957)) ;
#77554=CARTESIAN_POINT('Ctrl Pts',(-0.497571705638597,0.497571705638616,
6.71957)) ;
#77555=CARTESIAN_POINT('',(-0.611939867549494,0.558026198990157,6.81085442572523)) ;
#77556=CARTESIAN_POINT('Origin',(-0.650062588186457,0.65006258818648,6.80213885145047)) ;
#77557=CARTESIAN_POINT('Origin',(-0.497571705638597,0.497571705638616,6.81957)) ;
#77558=CARTESIAN_POINT('Origin',(-0.783160989859995,0.783160989860022,8.78984143258953)) ;
#77559=CARTESIAN_POINT('',(-0.57005647672015,0.623970146151627,6.99051559580133)) ;
#77560=CARTESIAN_POINT('',(-0.623970146872331,0.57005647538499,6.9905155850314)) ;
#77561=CARTESIAN_POINT('Origin',(-0.662092866158805,0.662092866158827,6.981800021508)) ;
#77562=CARTESIAN_POINT('',(-0.745038269223031,0.691124600663699,8.7985570068643)) ;
#77563=CARTESIAN_POINT('',(-0.691124600663673,0.745038269223056,8.7985570068643)) ;
#77564=CARTESIAN_POINT('Ctrl Pts',(-0.57023634760258,0.62345266657714,6.99014289219157)) ;
#77565=CARTESIAN_POINT('Ctrl Pts',(-0.54533484188452,0.683543323877059,
6.99003852336951)) ;
#77566=CARTESIAN_POINT('Ctrl Pts',(-0.506923472001745,0.787787260371042,
7.04037308986155)) ;
#77567=CARTESIAN_POINT('Ctrl Pts',(-0.501809041727926,0.824264612279483,
7.14592568521385)) ;
#77568=CARTESIAN_POINT('Ctrl Pts',(-0.506127211986293,0.824152009463264,
7.19103163220241)) ;
#77569=CARTESIAN_POINT('Ctrl Pts',(-0.572397806648059,0.624406912457803,
7.01844435877122)) ;
#77570=CARTESIAN_POINT('Ctrl Pts',(-0.550442551132344,0.677132597440327,
7.01611788185536)) ;
#77571=CARTESIAN_POINT('Ctrl Pts',(-0.515355266894961,0.771079003376811,
7.05746161336935)) ;
#77572=CARTESIAN_POINT('Ctrl Pts',(-0.51068146638924,0.803741078261582,
7.15053005046882)) ;
#77573=CARTESIAN_POINT('Ctrl Pts',(-0.514624648025357,0.80325589553316,
7.19016526188573)) ;
#77574=CARTESIAN_POINT('Ctrl Pts',(-0.596834402166937,0.63463042661229,
7.06566080704229)) ;
#77575=CARTESIAN_POINT('Ctrl Pts',(-0.576378560707317,0.673163424606222,
7.06005906508349)) ;
#77576=CARTESIAN_POINT('Ctrl Pts',(-0.543010521615669,0.747243595992697,
7.08604143012023)) ;
#77577=CARTESIAN_POINT('Ctrl Pts',(-0.538457963976829,0.772998673862634,
7.15737445737381)) ;
#77578=CARTESIAN_POINT('Ctrl Pts',(-0.542247535400501,0.772088823972345,
7.18744210330885)) ;
#77579=CARTESIAN_POINT('Ctrl Pts',(-0.642835376848303,0.653727314049703,
7.08186031165656)) ;
#77580=CARTESIAN_POINT('Ctrl Pts',(-0.61927398724742,0.684773072748138,
7.07934238671448)) ;
#77581=CARTESIAN_POINT('Ctrl Pts',(-0.582387971573308,0.742244553421204,
7.10272807520075)) ;
#77582=CARTESIAN_POINT('Ctrl Pts',(-0.57744327389336,0.762394272353267,
7.15957559967768)) ;
#77583=CARTESIAN_POINT('Ctrl Pts',(-0.58160171008854,0.761968609441389,
7.18364859166338)) ;
#77584=CARTESIAN_POINT('Ctrl Pts',(-0.662485200451311,0.661870075855026,
7.08179987236142)) ;
#77585=CARTESIAN_POINT('Ctrl Pts',(-0.637610174556416,0.691856881100706,
7.08175608902504)) ;
#77586=CARTESIAN_POINT('Ctrl Pts',(-0.599228555531057,0.743859867172772,
7.10688022713665)) ;
#77587=CARTESIAN_POINT('Ctrl Pts',(-0.594118370980124,0.762055140291634,
7.15953504564004)) ;
#77588=CARTESIAN_POINT('Ctrl Pts',(-0.598433070233959,0.761999835561836,
7.18203726714093)) ;
#77589=CARTESIAN_POINT('Origin',(-0.662092865474104,0.662092867823976,6.98180002156108)) ;
#77590=CARTESIAN_POINT('',(-0.506191638276483,0.823877279363034,7.19051557427477)) ;
#77591=CARTESIAN_POINT('Origin',(-0.589034350751103,0.623877279363034,7.19051557427477)) ;
#77592=CARTESIAN_POINT('Origin',(-0.598228027472806,0.862,7.1818)) ;
#77593=CARTESIAN_POINT('Origin',(-0.681070739947426,0.662,7.1818)) ;
#77594=CARTESIAN_POINT('Origin',(-0.787882878836553,0.862,9.1845535952074)) ;
#77595=CARTESIAN_POINT('',(-0.639686894805695,0.823877279363034,8.60022433223444)) ;
#77596=CARTESIAN_POINT('Origin',(-0.731723284002018,0.862,8.59150875795967)) ;
#77597=CARTESIAN_POINT('',(-0.69584648964023,0.823877279363034,9.19326916948217)) ;
#77598=CARTESIAN_POINT('Origin',(-0.731723284002017,0.862,8.59150875795967)) ;
#77599=CARTESIAN_POINT('',(-0.745560008319434,0.878300227999278,8.68919625781168)) ;
#77600=CARTESIAN_POINT('Origin',(-0.731723284002017,0.862,8.59150875795967)) ;
#77601=CARTESIAN_POINT('Origin',(-0.731723284002017,0.862,8.59150875795967)) ;
#77602=CARTESIAN_POINT('Origin',(-0.662092866162308,0.66209286616233,6.98180002156031)) ;
#77603=CARTESIAN_POINT('Origin',(-0.662092866162308,0.66209286616233,6.98180002156031)) ;
#77604=CARTESIAN_POINT('Origin',(-0.248785852819289,0.600622180002925,6.81957)) ;
#77605=CARTESIAN_POINT('',(-1.13746140899457,0.340348049204403,6.81085442572523)) ;
#77606=CARTESIAN_POINT('',(-0.286908573456253,0.692658569199248,6.81085442572523)) ;
#77607=CARTESIAN_POINT('Origin',(-1.13595304047784,0.233145498782377,6.81957)) ;
#77608=CARTESIAN_POINT('',(-0.248785852819289,0.600622180002925,6.71957)) ;
#77609=CARTESIAN_POINT('Origin',(-0.353968116746243,0.854554628096503,8.8138)) ;
#77610=CARTESIAN_POINT('',(-1.1405879759986,0.356066362978534,6.99051557427477)) ;
#77611=CARTESIAN_POINT('',(3.63742046916217,2.3351822620972,6.99051557427477)) ;
#77612=CARTESIAN_POINT('',(-1.17226904966378,0.515337875768457,8.81099729580349)) ;
#77613=CARTESIAN_POINT('Origin',(0.,0.662,7.1818)) ;
#77614=CARTESIAN_POINT('Origin',(-1.17871069663556,0.448102752174857,6.9818)) ;
#77615=CARTESIAN_POINT('Origin',(-1.17871069663556,0.448102752174857,6.9818)) ;
#77616=CARTESIAN_POINT('Origin',(-1.17871069663556,0.448102752174857,6.9818)) ;
#77617=CARTESIAN_POINT('Origin',(3.59929774852521,2.42721865129353,6.9818)) ;
#77618=CARTESIAN_POINT('Origin',(-1.21039177030074,0.607374264964781,8.80228172152873)) ;
#77619=CARTESIAN_POINT('Origin',(-1.17558412963153,0.432384438400726,6.80213885145047)) ;
#77620=CARTESIAN_POINT('Ctrl Pts',(-1.17558412963154,0.332764968591552,
6.81085442572523)) ;
#77621=CARTESIAN_POINT('Ctrl Pts',(-1.17386952959435,0.328455030351476,
6.7615916062195)) ;
#77622=CARTESIAN_POINT('Ctrl Pts',(-1.15562586963554,0.282596494255549,
6.71957)) ;
#77623=CARTESIAN_POINT('Ctrl Pts',(-1.13595304047784,0.233145498782377,
6.71957)) ;
#77624=CARTESIAN_POINT('Ctrl Pts',(-1.16254657695483,0.332784667850045,
6.81107958928014)) ;
#77625=CARTESIAN_POINT('Ctrl Pts',(-1.16142573132118,0.328698029275187,
6.76307285057327)) ;
#77626=CARTESIAN_POINT('Ctrl Pts',(-1.14931784407502,0.283851238553283,
6.71957)) ;
#77627=CARTESIAN_POINT('Ctrl Pts',(-1.13595304047784,0.233145498782377,
6.71957)) ;
#77628=CARTESIAN_POINT('Ctrl Pts',(-1.14951407564647,0.335376993538169,
6.81107958928014)) ;
#77629=CARTESIAN_POINT('Ctrl Pts',(-1.14898571310984,0.331172502747851,
6.76307285057327)) ;
#77630=CARTESIAN_POINT('Ctrl Pts',(-1.14300981851451,0.285105982851016,
6.71957)) ;
#77631=CARTESIAN_POINT('Ctrl Pts',(-1.13595304047784,0.233145498782377,
6.71957)) ;
#77632=CARTESIAN_POINT('Ctrl Pts',(-1.13746140899457,0.340348049204403,
6.81085442572523)) ;
#77633=CARTESIAN_POINT('Ctrl Pts',(-1.13739615091638,0.335710036450645,
6.7615916062195)) ;
#77634=CARTESIAN_POINT('Ctrl Pts',(-1.13670179295399,0.286360727148749,
6.71957)) ;
#77635=CARTESIAN_POINT('Ctrl Pts',(-1.13595304047784,0.233145498782377,
6.71957)) ;
#77636=CARTESIAN_POINT('Ctrl Pts',(-0.506127211989078,-0.82415200945132,
7.19103163217991)) ;
#77637=CARTESIAN_POINT('Ctrl Pts',(-0.501809041773239,-0.824264612261493,
7.14592568561392)) ;
#77638=CARTESIAN_POINT('Ctrl Pts',(-0.506923471858881,-0.787787261003788,
7.04037309112128)) ;
#77639=CARTESIAN_POINT('Ctrl Pts',(-0.545334841097472,-0.683543325948823,
6.99003852412021)) ;
#77640=CARTESIAN_POINT('Ctrl Pts',(-0.570236346572291,-0.623452669067161,
6.99014289220396)) ;
#77641=CARTESIAN_POINT('Ctrl Pts',(-0.514624648029491,-0.803255895526575,
7.1901652618658)) ;
#77642=CARTESIAN_POINT('Ctrl Pts',(-0.510681466432051,-0.803741078245772,
7.15053005081949)) ;
#77643=CARTESIAN_POINT('Ctrl Pts',(-0.515355266764847,-0.771079003955546,
7.05746161448053)) ;
#77644=CARTESIAN_POINT('Ctrl Pts',(-0.550442550421403,-0.677132599298618,
7.01611788244042)) ;
#77645=CARTESIAN_POINT('Ctrl Pts',(-0.572397805740086,-0.624406914644257,
7.01844435868783)) ;
#77646=CARTESIAN_POINT('Ctrl Pts',(-0.542247535402147,-0.772088823972612,
7.18744210329385)) ;
#77647=CARTESIAN_POINT('Ctrl Pts',(-0.53845796401558,-0.77299867385038,
7.15737445763862)) ;
#77648=CARTESIAN_POINT('Ctrl Pts',(-0.543010521485572,-0.747243596469415,
7.08604143097494)) ;
#77649=CARTESIAN_POINT('Ctrl Pts',(-0.576378560033109,-0.673163426046929,
7.06005906538994)) ;
#77650=CARTESIAN_POINT('Ctrl Pts',(-0.596834401325316,-0.634630428210077,
7.06566080680978)) ;
#77651=CARTESIAN_POINT('Ctrl Pts',(-0.581601710084174,-0.761968609442201,
7.18364859165186)) ;
#77652=CARTESIAN_POINT('Ctrl Pts',(-0.577443273929769,-0.762394272347131,
7.15957559988957)) ;
#77653=CARTESIAN_POINT('Ctrl Pts',(-0.582387971427533,-0.74224455378735,
7.10272807587653)) ;
#77654=CARTESIAN_POINT('Ctrl Pts',(-0.619273986488663,-0.684773073873152,
7.07934238702148)) ;
#77655=CARTESIAN_POINT('Ctrl Pts',(-0.642835375870018,-0.65372731533593,
7.08186031155258)) ;
#77656=CARTESIAN_POINT('Ctrl Pts',(-0.598433070228347,-0.761999835561857,
7.18203726713029)) ;
#77657=CARTESIAN_POINT('Ctrl Pts',(-0.594118371016825,-0.762055140288618,
7.15953504583831)) ;
#77658=CARTESIAN_POINT('Ctrl Pts',(-0.599228555379944,-0.743859867492794,
7.10688022775928)) ;
#77659=CARTESIAN_POINT('Ctrl Pts',(-0.637610173763258,-0.691856882134678,
7.08175608939188)) ;
#77660=CARTESIAN_POINT('Ctrl Pts',(-0.662485199416716,-0.661870077095623,
7.08179987235985)) ;
#77661=CARTESIAN_POINT('',(-0.598228027472817,-0.762,7.1818)) ;
#77662=CARTESIAN_POINT('Origin',(-0.598228027472817,-0.862,7.1818)) ;
#77663=CARTESIAN_POINT('Origin',(-0.662092864798467,-0.6620928694553,6.98180002156184)) ;
#77664=CARTESIAN_POINT('Origin',(-0.681070739947432,-0.662,7.1818)) ;
#77665=CARTESIAN_POINT('Origin',(-0.78788287883656,-0.862000000000001,9.1845535952074)) ;
#77666=CARTESIAN_POINT('',(-0.731723284002027,-0.762,8.59150875795967)) ;
#77667=CARTESIAN_POINT('Origin',(-0.731723284002027,-0.862000000000001,
8.59150875795967)) ;
#77668=CARTESIAN_POINT('',(-0.78788287883656,-0.762,9.1845535952074)) ;
#77669=CARTESIAN_POINT('Origin',(-0.731723284002027,-0.862,8.59150875795967)) ;
#77670=CARTESIAN_POINT('',(-0.745560008319445,-0.878300227999277,8.68919625781168)) ;
#77671=CARTESIAN_POINT('Origin',(-0.731723284002027,-0.862,8.59150875795967)) ;
#77672=CARTESIAN_POINT('Origin',(-0.731723284002027,-0.862,8.59150875795967)) ;
#77673=CARTESIAN_POINT('Origin',(-0.783160989860015,-0.783160989859993,
8.78984143258953)) ;
#77674=CARTESIAN_POINT('',(-0.623970146870624,-0.570056475383248,6.99051558500572)) ;
#77675=CARTESIAN_POINT('Origin',(-0.662092866155382,-0.662092866155364,
6.98180002145664)) ;
#77676=CARTESIAN_POINT('',(-0.611939867549509,-0.558026198990134,6.81085442572523)) ;
#77677=CARTESIAN_POINT('Origin',(-0.650062588186474,-0.650062588186457,
6.80213885145047)) ;
#77678=CARTESIAN_POINT('',(-0.74503826922305,-0.691124600663671,8.7985570068643)) ;
#77679=CARTESIAN_POINT('Ctrl Pts',(-0.558026198990151,-0.611939867549492,
6.81085442572523)) ;
#77680=CARTESIAN_POINT('Ctrl Pts',(-0.55541069488057,-0.606991841672512,
6.7615916062195)) ;
#77681=CARTESIAN_POINT('Ctrl Pts',(-0.527581249784816,-0.554343935683229,
6.71957)) ;
#77682=CARTESIAN_POINT('Ctrl Pts',(-0.497571705638611,-0.497571705638596,
6.71957)) ;
#77683=CARTESIAN_POINT('Ctrl Pts',(-0.568073880351629,-0.58789686673872,
6.81179156524867)) ;
#77684=CARTESIAN_POINT('Ctrl Pts',(-0.565801572147179,-0.584594051674632,
6.76779239028237)) ;
#77685=CARTESIAN_POINT('Ctrl Pts',(-0.536502145084292,-0.545423040383753,
6.71957)) ;
#77686=CARTESIAN_POINT('Ctrl Pts',(-0.497571705638611,-0.497571705638596,
6.71957)) ;
#77687=CARTESIAN_POINT('Ctrl Pts',(-0.587896866738737,-0.568073880351612,
6.81179156524867)) ;
#77688=CARTESIAN_POINT('Ctrl Pts',(-0.584594051674648,-0.565801572147162,
6.76779239028237)) ;
#77689=CARTESIAN_POINT('Ctrl Pts',(-0.545423040383768,-0.536502145084276,
6.71957)) ;
#77690=CARTESIAN_POINT('Ctrl Pts',(-0.497571705638611,-0.497571705638596,
6.71957)) ;
#77691=CARTESIAN_POINT('Ctrl Pts',(-0.611939867549509,-0.558026198990134,
6.81085442572523)) ;
#77692=CARTESIAN_POINT('Ctrl Pts',(-0.606991841672528,-0.555410694880553,
6.7615916062195)) ;
#77693=CARTESIAN_POINT('Ctrl Pts',(-0.554343935683244,-0.5275812497848,
6.71957)) ;
#77694=CARTESIAN_POINT('Ctrl Pts',(-0.497571705638611,-0.497571705638596,
6.71957)) ;
#77695=CARTESIAN_POINT('Origin',(-0.497571705638611,-0.497571705638596,
6.81957)) ;
#77696=CARTESIAN_POINT('Origin',(-0.662092866162324,-0.662092866162307,
6.98180002156031)) ;
#77697=CARTESIAN_POINT('Origin',(-0.662092866162324,-0.662092866162307,
6.98180002156031)) ;
#77698=CARTESIAN_POINT('Origin',(-0.507879677365695,-0.210370650418533,
3.37743570668596)) ;
#77699=CARTESIAN_POINT('Origin',(-0.517483568940243,-0.214348712560272,
3.376526246514)) ;
#77700=CARTESIAN_POINT('Origin',(0.,-0.862,3.42553041237115)) ;
#77701=CARTESIAN_POINT('',(-3.07434158440252,-0.762,7.64111756647598)) ;
#77702=CARTESIAN_POINT('Origin',(0.,-0.762,3.42553041237115)) ;
#77703=CARTESIAN_POINT('',(-3.13247669898886,-0.878300227999278,7.72083338058588)) ;
#77704=CARTESIAN_POINT('Origin',(-3.07434158440252,-0.862,7.64111756647598)) ;
#77705=CARTESIAN_POINT('Origin',(0.,-0.878300227999278,3.42553041237115)) ;
#77706=CARTESIAN_POINT('Origin',(-9.525,-0.762,8.72161438184689)) ;
#77707=CARTESIAN_POINT('',(-3.21546217517793,-0.762,7.36730649953872)) ;
#77708=CARTESIAN_POINT('',(-3.21546217517793,-0.762,0.)) ;
#77709=CARTESIAN_POINT('Origin',(-2.94522915997985,-0.762,7.40850798245898)) ;
#77710=CARTESIAN_POINT('',(0.,-0.762,7.1818)) ;
#77711=CARTESIAN_POINT('Origin',(0.,-0.662,7.1818)) ;
#77712=CARTESIAN_POINT('Origin',(-0.353968116746264,-0.854554628096483,
8.8138)) ;
#77713=CARTESIAN_POINT('',(-1.13746140899458,-0.34034804920437,6.81085442572523)) ;
#77714=CARTESIAN_POINT('',(-0.286908573456268,-0.692658569199233,6.81085442572523)) ;
#77715=CARTESIAN_POINT('',(-1.14058797599861,-0.356066362978501,6.99051557427476)) ;
#77716=CARTESIAN_POINT('',(-1.17226904966379,-0.515337875768421,8.81099729580349)) ;
#77717=CARTESIAN_POINT('',(3.90682815279416,-2.44677457846517,6.99051557427477)) ;
#77718=CARTESIAN_POINT('Origin',(-1.17871069663558,-0.448102752174823,6.9818)) ;
#77719=CARTESIAN_POINT('Origin',(-1.17871069663558,-0.448102752174823,6.9818)) ;
#77720=CARTESIAN_POINT('Origin',(-1.17871069663558,-0.448102752174823,6.9818)) ;
#77721=CARTESIAN_POINT('Origin',(3.86870543215719,-2.5388109676615,6.9818)) ;
#77722=CARTESIAN_POINT('Origin',(-1.21039177030076,-0.607374264964743,8.80228172152873)) ;
#77723=CARTESIAN_POINT('Origin',(-1.17558412963155,-0.432384438400692,6.80213885145047)) ;
#77724=CARTESIAN_POINT('Ctrl Pts',(-1.13746140899458,-0.34034804920437,
6.81085442572523)) ;
#77725=CARTESIAN_POINT('Ctrl Pts',(-1.13739615091639,-0.335710036450613,
6.7615916062195)) ;
#77726=CARTESIAN_POINT('Ctrl Pts',(-1.136701792954,-0.286360727148716,6.71957)) ;
#77727=CARTESIAN_POINT('Ctrl Pts',(-1.13595304047785,-0.233145498782344,
6.71957)) ;
#77728=CARTESIAN_POINT('Ctrl Pts',(-1.14951407564648,-0.335376993538136,
6.81107958928014)) ;
#77729=CARTESIAN_POINT('Ctrl Pts',(-1.14898571310985,-0.331172502747818,
6.76307285057327)) ;
#77730=CARTESIAN_POINT('Ctrl Pts',(-1.14300981851452,-0.285105982850983,
6.71957)) ;
#77731=CARTESIAN_POINT('Ctrl Pts',(-1.13595304047785,-0.233145498782344,
6.71957)) ;
#77732=CARTESIAN_POINT('Ctrl Pts',(-1.16254657695484,-0.332784667850012,
6.81107958928014)) ;
#77733=CARTESIAN_POINT('Ctrl Pts',(-1.16142573132119,-0.328698029275153,
6.76307285057327)) ;
#77734=CARTESIAN_POINT('Ctrl Pts',(-1.14931784407503,-0.283851238553249,
6.71957)) ;
#77735=CARTESIAN_POINT('Ctrl Pts',(-1.13595304047785,-0.233145498782344,
6.71957)) ;
#77736=CARTESIAN_POINT('Ctrl Pts',(-1.17558412963155,-0.332764968591518,
6.81085442572523)) ;
#77737=CARTESIAN_POINT('Ctrl Pts',(-1.17386952959436,-0.328455030351443,
6.7615916062195)) ;
#77738=CARTESIAN_POINT('Ctrl Pts',(-1.15562586963555,-0.282596494255516,
6.71957)) ;
#77739=CARTESIAN_POINT('Ctrl Pts',(-1.13595304047785,-0.233145498782344,
6.71957)) ;
#77740=CARTESIAN_POINT('',(-1.13595304047785,-0.233145498782344,6.71957)) ;
#77741=CARTESIAN_POINT('Origin',(-1.13595304047785,-0.233145498782344,6.81957)) ;
#77742=CARTESIAN_POINT('Origin',(-1.13595304047785,-0.233145498782344,6.81957)) ;
#77743=CARTESIAN_POINT('Origin',(-1.62804631646772E-15,-0.233145498782352,
6.81957)) ;
#77744=CARTESIAN_POINT('',(-1.62804631646772E-15,-0.233145498782352,6.71957)) ;
#77745=CARTESIAN_POINT('Origin',(-0.248785852819302,-0.60062218000291,6.81957)) ;
#77746=CARTESIAN_POINT('',(-0.248785852819302,-0.60062218000291,6.71957)) ;
#77747=CARTESIAN_POINT('Ctrl Pts',(-3.27942391815487,0.70707706204744,7.03908289042881)) ;
#77748=CARTESIAN_POINT('Ctrl Pts',(-3.28250258905352,0.697893994312427,
7.03746804394249)) ;
#77749=CARTESIAN_POINT('Ctrl Pts',(-3.28505418610036,0.68846516745384,7.03662526114751)) ;
#77750=CARTESIAN_POINT('Ctrl Pts',(-3.2870264093502,0.678916496982226,7.03662526114754)) ;
#77751=CARTESIAN_POINT('Ctrl Pts',(-3.27140856314617,0.702764080010679,
7.05223037429146)) ;
#77752=CARTESIAN_POINT('Ctrl Pts',(-3.27436377099682,0.694432640985322,
7.05063990488633)) ;
#77753=CARTESIAN_POINT('Ctrl Pts',(-3.27680438884804,0.685870405895161,
7.04975105907268)) ;
#77754=CARTESIAN_POINT('Ctrl Pts',(-3.27867914825949,0.677192417965742,
7.04962706151202)) ;
#77755=CARTESIAN_POINT('Ctrl Pts',(-3.2602197508559,0.697769125082712,7.06320246322391)) ;
#77756=CARTESIAN_POINT('Ctrl Pts',(-3.26310028573039,0.690308451268357,
7.0616920887364)) ;
#77757=CARTESIAN_POINT('Ctrl Pts',(-3.26548225911655,0.682632678233894,
7.0608038408065)) ;
#77758=CARTESIAN_POINT('Ctrl Pts',(-3.26731641278819,0.674845509970035,
7.06059580486544)) ;
#77759=CARTESIAN_POINT('Ctrl Pts',(-3.24710198979438,0.692647775796393,
7.07077875440785)) ;
#77760=CARTESIAN_POINT('Ctrl Pts',(-3.24994267520402,0.685970018257057,
7.06941712332046)) ;
#77761=CARTESIAN_POINT('Ctrl Pts',(-3.2523024328244,0.679097740077075,7.06859808355775)) ;
#77762=CARTESIAN_POINT('Ctrl Pts',(-3.25413500684122,0.672122965993735,
7.06837618534763)) ;
#77763=CARTESIAN_POINT('Ctrl Pts',(3.27942391815487,-0.70707706204744,7.03908289042881)) ;
#77764=CARTESIAN_POINT('Ctrl Pts',(3.28250258905352,-0.697893994312428,
7.03746804394249)) ;
#77765=CARTESIAN_POINT('Ctrl Pts',(3.28505418610036,-0.68846516745384,7.03662526114751)) ;
#77766=CARTESIAN_POINT('Ctrl Pts',(3.2870264093502,-0.678916496982227,7.03662526114754)) ;
#77767=CARTESIAN_POINT('Ctrl Pts',(3.27140856314617,-0.70276408001068,7.05223037429146)) ;
#77768=CARTESIAN_POINT('Ctrl Pts',(3.27436377099682,-0.694432640985322,
7.05063990488633)) ;
#77769=CARTESIAN_POINT('Ctrl Pts',(3.27680438884804,-0.685870405895162,
7.04975105907268)) ;
#77770=CARTESIAN_POINT('Ctrl Pts',(3.2786791482595,-0.677192417965742,7.04962706151202)) ;
#77771=CARTESIAN_POINT('Ctrl Pts',(3.2602197508559,-0.697769125082713,7.0632024632239)) ;
#77772=CARTESIAN_POINT('Ctrl Pts',(3.26310028573039,-0.690308451268358,
7.0616920887364)) ;
#77773=CARTESIAN_POINT('Ctrl Pts',(3.26548225911656,-0.682632678233895,
7.0608038408065)) ;
#77774=CARTESIAN_POINT('Ctrl Pts',(3.26731641278819,-0.674845509970036,
7.06059580486544)) ;
#77775=CARTESIAN_POINT('Ctrl Pts',(3.24710198979438,-0.692647775796394,
7.07077875440784)) ;
#77776=CARTESIAN_POINT('Ctrl Pts',(3.24994267520403,-0.685970018257058,
7.06941712332046)) ;
#77777=CARTESIAN_POINT('Ctrl Pts',(3.2523024328244,-0.679097740077076,7.06859808355775)) ;
#77778=CARTESIAN_POINT('Ctrl Pts',(3.25413500684123,-0.672122965993735,
7.06837618534763)) ;
#77779=CARTESIAN_POINT('Origin',(0.,0.662,7.1818)) ;
#77780=CARTESIAN_POINT('',(0.662097436318065,0.662040915864284,7.08180000837054)) ;
#77781=CARTESIAN_POINT('',(0.,0.662,7.0818)) ;
#77782=CARTESIAN_POINT('',(0.598228027472816,0.762,7.1818)) ;
#77783=CARTESIAN_POINT('',(0.,0.762,7.1818)) ;
#77784=CARTESIAN_POINT('Origin',(0.681070739947433,0.662,7.1818)) ;
#77785=CARTESIAN_POINT('Ctrl Pts',(1.94288959754296,0.448102752174838,7.0818)) ;
#77786=CARTESIAN_POINT('Ctrl Pts',(1.94270197516852,0.447562750019821,7.0818)) ;
#77787=CARTESIAN_POINT('Ctrl Pts',(1.94251230527809,0.447017983233615,7.08179766992681)) ;
#77788=CARTESIAN_POINT('Ctrl Pts',(1.91803916779423,0.376442475910995,7.08160456336037)) ;
#77789=CARTESIAN_POINT('Ctrl Pts',(1.88761451839117,0.293719590124098,7.05576035709455)) ;
#77790=CARTESIAN_POINT('Ctrl Pts',(1.87819429271644,0.268591723493114,7.00768190451025)) ;
#77791=CARTESIAN_POINT('Ctrl Pts',(1.94288959754296,0.448102752174838,7.0818)) ;
#77792=CARTESIAN_POINT('Ctrl Pts',(1.94252901127699,0.447573785115438,7.0818)) ;
#77793=CARTESIAN_POINT('Ctrl Pts',(1.94238760925022,0.447241733482732,7.08171624908905)) ;
#77794=CARTESIAN_POINT('Ctrl Pts',(1.90274378880158,0.385137079186532,7.08429620486543)) ;
#77795=CARTESIAN_POINT('Ctrl Pts',(1.86635603372516,0.320809755584945,7.03323707646533)) ;
#77796=CARTESIAN_POINT('Ctrl Pts',(1.86932161172288,0.312347136547031,6.99801930665779)) ;
#77797=CARTESIAN_POINT('Ctrl Pts',(1.94288959754296,0.448102752174838,7.0818)) ;
#77798=CARTESIAN_POINT('Ctrl Pts',(1.94245161464468,0.447640464230166,7.0818)) ;
#77799=CARTESIAN_POINT('Ctrl Pts',(1.94216670833305,0.447413283195622,7.08171624908906)) ;
#77800=CARTESIAN_POINT('Ctrl Pts',(1.89052514973493,0.394910453254149,7.08429620486524)) ;
#77801=CARTESIAN_POINT('Ctrl Pts',(1.83473895434066,0.347957809715557,7.03323707646533)) ;
#77802=CARTESIAN_POINT('Ctrl Pts',(1.82714531063844,0.348921084254577,6.99801930665779)) ;
#77803=CARTESIAN_POINT('Ctrl Pts',(1.94288959754296,0.448102752174838,7.0818)) ;
#77804=CARTESIAN_POINT('Ctrl Pts',(1.94240557475948,0.447798570604672,7.0818)) ;
#77805=CARTESIAN_POINT('Ctrl Pts',(1.94191738994558,0.447492388347723,7.08179766992681)) ;
#77806=CARTESIAN_POINT('Ctrl Pts',(1.878643427677,0.407664231473883,7.08160456336017)) ;
#77807=CARTESIAN_POINT('Ctrl Pts',(1.80491723090524,0.364392752089233,7.05576035709455)) ;
#77808=CARTESIAN_POINT('Ctrl Pts',(1.78257449869961,0.351510169545931,7.00768190451025)) ;
#77809=CARTESIAN_POINT('',(1.78257449869961,0.351510169545931,7.00768190451025)) ;
#77810=CARTESIAN_POINT('',(1.87819429271644,0.268591723493114,7.00768190451025)) ;
#77811=CARTESIAN_POINT('Origin',(1.78257449869961,0.254917586917024,7.0335638090205)) ;
#77812=CARTESIAN_POINT('',(1.89249580907308,0.307272596056854,7.04638255392016)) ;
#77813=CARTESIAN_POINT('Origin',(1.98523598941849,0.564759059985062,6.94301769845579)) ;
#77814=CARTESIAN_POINT('',(1.91807183824094,0.377810206871834,7.07388013397756)) ;
#77815=CARTESIAN_POINT('Origin',(1.93654302938549,0.434616459002425,6.9972761880138)) ;
#77816=CARTESIAN_POINT('',(1.94182783334034,0.445044808441076,7.08178867415542)) ;
#77817=CARTESIAN_POINT('Origin',(1.9279516251551,0.413874762390893,7.02228347027605)) ;
#77818=CARTESIAN_POINT('',(1.94288959754296,0.448102752174838,7.0818)) ;
#77819=CARTESIAN_POINT('',(1.94182783307285,0.445044807670698,7.08178867415257)) ;
#77820=CARTESIAN_POINT('',(1.94014976372696,0.446380214140472,7.08178692473713)) ;
#77821=CARTESIAN_POINT('',(1.94288959754296,0.448102752174838,7.0818)) ;
#77822=CARTESIAN_POINT('',(1.87964216949001,0.409078843672791,7.0738290317143)) ;
#77823=CARTESIAN_POINT('Origin',(1.92743649785841,0.446270284394762,6.99208610030143)) ;
#77824=CARTESIAN_POINT('',(1.81813539254237,0.372312156583862,7.04714690179995)) ;
#77825=CARTESIAN_POINT('Origin',(1.93250408796308,0.444533930106968,6.99487389855795)) ;
#77826=CARTESIAN_POINT('Origin',(2.04686400774823,0.509803748843894,6.9414017611276)) ;
#77827=CARTESIAN_POINT('Ctrl Pts',(1.87819429271644,0.268591723493114,7.00768190451025)) ;
#77828=CARTESIAN_POINT('Ctrl Pts',(1.87559269584779,0.265429455820039,6.99639968079942)) ;
#77829=CARTESIAN_POINT('Ctrl Pts',(1.87277553216538,0.263323474391224,6.98489826419217)) ;
#77830=CARTESIAN_POINT('Ctrl Pts',(1.86979680842785,0.262281765411205,6.97334924403639)) ;
#77831=CARTESIAN_POINT('Ctrl Pts',(1.87312418929155,0.293594816666781,7.00216042002313)) ;
#77832=CARTESIAN_POINT('Ctrl Pts',(1.87084473493899,0.291084530404676,6.99224479183831)) ;
#77833=CARTESIAN_POINT('Ctrl Pts',(1.86834496343776,0.289501530632332,6.9821612484371)) ;
#77834=CARTESIAN_POINT('Ctrl Pts',(1.86572206147513,0.288873179727197,6.9720753047436)) ;
#77835=CARTESIAN_POINT('Ctrl Pts',(1.84631328088201,0.334524427261367,6.99742306677411)) ;
#77836=CARTESIAN_POINT('Ctrl Pts',(1.84417962418044,0.333091612281766,6.98998909901152)) ;
#77837=CARTESIAN_POINT('Ctrl Pts',(1.84187319629001,0.332400676673115,6.98249471608034)) ;
#77838=CARTESIAN_POINT('Ctrl Pts',(1.8394212036961,0.332407181519421,6.97506009028094)) ;
#77839=CARTESIAN_POINT('Ctrl Pts',(1.80167627524482,0.350400561563922,7.00354079114491)) ;
#77840=CARTESIAN_POINT('Ctrl Pts',(1.79920012229604,0.349063108054388,6.99757511629261)) ;
#77841=CARTESIAN_POINT('Ctrl Pts',(1.79652736146151,0.34827651613047,6.99152359092133)) ;
#77842=CARTESIAN_POINT('Ctrl Pts',(1.79370245617676,0.348044577753787,6.98550115761471)) ;
#77843=CARTESIAN_POINT('Ctrl Pts',(1.78257449869961,0.351510169545931,7.00768190451025)) ;
#77844=CARTESIAN_POINT('Ctrl Pts',(1.77995299478772,0.349998638179859,7.00204079265484)) ;
#77845=CARTESIAN_POINT('Ctrl Pts',(1.77712384321892,0.348988486534684,6.99629008435121)) ;
#77846=CARTESIAN_POINT('Ctrl Pts',(1.77414072885052,0.348483282365537,6.99051557427332)) ;
#77847=CARTESIAN_POINT('',(1.77414072885052,0.3484832823656,6.99051557427404)) ;
#77848=CARTESIAN_POINT('',(1.86979680842785,0.262281765411205,6.97334924403639)) ;
#77849=CARTESIAN_POINT('Origin',(1.77414072885052,0.248863812556236,6.99923114854664)) ;
#77850=CARTESIAN_POINT('Origin',(1.84377759624484,0.424925231893568,6.96360853181849)) ;
#77851=CARTESIAN_POINT('Origin',(1.74961486665444,0.424101006244594,6.98537442845805)) ;
#77852=CARTESIAN_POINT('Ctrl Pts',(1.72771014821069,0.332764968591604,6.81085442572606)) ;
#77853=CARTESIAN_POINT('Ctrl Pts',(1.74319473414637,0.338004233132887,6.87073949346092)) ;
#77854=CARTESIAN_POINT('Ctrl Pts',(1.75867139282689,0.34324367563947,6.93062659534848)) ;
#77855=CARTESIAN_POINT('Ctrl Pts',(1.77414072885052,0.348483282365411,6.99051557427187)) ;
#77856=CARTESIAN_POINT('Ctrl Pts',(1.75388379891737,0.332177363448692,6.8041380682092)) ;
#77857=CARTESIAN_POINT('Ctrl Pts',(1.76933665987703,0.337416538558256,6.86403381882679)) ;
#77858=CARTESIAN_POINT('Ctrl Pts',(1.78478377705795,0.342658817604018,6.92393065445535)) ;
#77859=CARTESIAN_POINT('Ctrl Pts',(1.80022303195212,0.347898342882986,6.98382968539381)) ;
#77860=CARTESIAN_POINT('Ctrl Pts',(1.79938284222813,0.310992589547749,6.79422672914133)) ;
#77861=CARTESIAN_POINT('Ctrl Pts',(1.81478360859012,0.316286258253241,6.8541354548437)) ;
#77862=CARTESIAN_POINT('Ctrl Pts',(1.83017778759028,0.321577463411819,6.91404581861776)) ;
#77863=CARTESIAN_POINT('Ctrl Pts',(1.84556760072686,0.326868409115694,6.97395705441164)) ;
#77864=CARTESIAN_POINT('Ctrl Pts',(1.82046616955569,0.266091328799232,6.79270352788323)) ;
#77865=CARTESIAN_POINT('Ctrl Pts',(1.83589739021255,0.271473267897874,6.8525986516149)) ;
#77866=CARTESIAN_POINT('Ctrl Pts',(1.85132258737849,0.276850760615254,6.91249534127326)) ;
#77867=CARTESIAN_POINT('Ctrl Pts',(1.86674074821324,0.282225326148124,6.97239378956652)) ;
#77868=CARTESIAN_POINT('Ctrl Pts',(1.82343508275095,0.246063080838898,6.79368809549057)) ;
#77869=CARTESIAN_POINT('Ctrl Pts',(1.83889654046911,0.251473735590694,6.85357316322543)) ;
#77870=CARTESIAN_POINT('Ctrl Pts',(1.85435024060408,0.256879845047591,6.91346026511299)) ;
#77871=CARTESIAN_POINT('Ctrl Pts',(1.86979680842785,0.262281765411205,6.97334924403639)) ;
#77872=CARTESIAN_POINT('',(1.72771014821069,0.332764968591568,6.81085442572565)) ;
#77873=CARTESIAN_POINT('',(1.77414072885052,0.348483282365411,6.99051557427187)) ;
#77874=CARTESIAN_POINT('',(1.82343508275095,0.246063080838898,6.79368809549016)) ;
#77875=CARTESIAN_POINT('Origin',(1.72771014821069,0.23314549878243,6.81957000000082)) ;
#77876=CARTESIAN_POINT('',(1.82343508275095,0.246063080838898,6.79368809549057)) ;
#77877=CARTESIAN_POINT('Origin',(1.72771014821048,0.233145498782358,6.81957)) ;
#77878=CARTESIAN_POINT('',(1.72771014821048,0.233145498782358,6.71957)) ;
#77879=CARTESIAN_POINT('Origin',(1.72771014821048,0.233145498782358,6.81957)) ;
#77880=CARTESIAN_POINT('Origin',(1.72771014821048,0.233145498782358,6.81957)) ;
#77881=CARTESIAN_POINT('Origin',(0.,0.507999999999997,8.8138)) ;
#77882=CARTESIAN_POINT('',(1.17871069663557,0.348483282365664,6.99051557427477)) ;
#77883=CARTESIAN_POINT('',(4.7625,0.348483282365664,6.99051557427477)) ;
#77884=CARTESIAN_POINT('',(1.17558412963154,0.332764968591532,6.81085442572523)) ;
#77885=CARTESIAN_POINT('',(1.21039177030075,0.507754795155586,8.81099729580349)) ;
#77886=CARTESIAN_POINT('',(0.,0.332764968591532,6.81085442572523)) ;
#77887=CARTESIAN_POINT('Origin',(4.7625,0.448102752174838,6.9818)) ;
#77888=CARTESIAN_POINT('',(1.17871069663557,0.448102752174838,7.0818)) ;
#77889=CARTESIAN_POINT('',(4.7625,0.448102752174838,7.0818)) ;
#77890=CARTESIAN_POINT('Origin',(1.17871069663557,0.448102752174838,6.9818)) ;
#77891=CARTESIAN_POINT('Origin',(0.,0.,6.9818)) ;
#77892=CARTESIAN_POINT('',(1.87819429271644,-0.268591723493119,7.00768190451025)) ;
#77893=CARTESIAN_POINT('Origin',(0.,-3.71851796272644E-17,7.00768190451025)) ;
#77894=CARTESIAN_POINT('',(1.93516376195716,-0.425958697933976,7.08103018110362)) ;
#77895=CARTESIAN_POINT('Ctrl Pts',(1.93516376195716,-0.425958697933976,
7.08103018110362)) ;
#77896=CARTESIAN_POINT('Ctrl Pts',(1.91237404550518,-0.3610438318848,7.07642065496821)) ;
#77897=CARTESIAN_POINT('Ctrl Pts',(1.88670733098015,-0.291299724076243,
7.05113030167638)) ;
#77898=CARTESIAN_POINT('Ctrl Pts',(1.87819429271644,-0.268591723493119,
7.00768190451025)) ;
#77899=CARTESIAN_POINT('',(1.94288959754295,-0.448102752174844,7.0818)) ;
#77900=CARTESIAN_POINT('Ctrl Pts',(1.94288959754296,-0.448102752174824,
7.0818)) ;
#77901=CARTESIAN_POINT('Ctrl Pts',(1.94270198330657,-0.447562773442322,
7.0818)) ;
#77902=CARTESIAN_POINT('Ctrl Pts',(1.94251232165841,-0.447018030321371,
7.08179767010457)) ;
#77903=CARTESIAN_POINT('Ctrl Pts',(1.93998825604565,-0.439739142785562,
7.08177775516637)) ;
#77904=CARTESIAN_POINT('Ctrl Pts',(1.93759234469349,-0.432876340957351,
7.08152139456908)) ;
#77905=CARTESIAN_POINT('Ctrl Pts',(1.93516376195716,-0.425958697933976,
7.08103018110362)) ;
#77906=CARTESIAN_POINT('Origin',(0.,0.,7.0818)) ;
#77907=CARTESIAN_POINT('Origin',(1.72771014821048,-0.233145498782364,6.81957)) ;
#77908=CARTESIAN_POINT('',(1.72771014821048,-0.332764968591539,6.81085442572523)) ;
#77909=CARTESIAN_POINT('',(1.82343508275074,-0.24606308083883,6.79368809548975)) ;
#77910=CARTESIAN_POINT('Origin',(1.72771014821048,-0.233145498782364,6.81957)) ;
#77911=CARTESIAN_POINT('',(1.72771014821048,-0.233145498782364,6.71957)) ;
#77912=CARTESIAN_POINT('Origin',(1.72771014821048,-0.233145498782364,6.81957)) ;
#77913=CARTESIAN_POINT('Origin',(1.72771014821048,-0.233145498782364,6.81957)) ;
#77914=CARTESIAN_POINT('Ctrl Pts',(1.82343508274976,-0.246063080838488,
6.79368809548596)) ;
#77915=CARTESIAN_POINT('Ctrl Pts',(1.8388965404683,-0.251473735590417,6.85357316322228)) ;
#77916=CARTESIAN_POINT('Ctrl Pts',(1.85435024060365,-0.256879845047446,
6.91346026511131)) ;
#77917=CARTESIAN_POINT('Ctrl Pts',(1.86979680842779,-0.262281765411192,
6.97334924403617)) ;
#77918=CARTESIAN_POINT('Ctrl Pts',(1.81947653182275,-0.27276741145227,6.79237533867617)) ;
#77919=CARTESIAN_POINT('Ctrl Pts',(1.83489694400734,-0.278139250484296,
6.85227406114401)) ;
#77920=CARTESIAN_POINT('Ctrl Pts',(1.85031405219097,-0.283508230262897,
6.91217346932062)) ;
#77921=CARTESIAN_POINT('Ctrl Pts',(1.86572206147499,-0.288873179727084,
6.97207530474301)) ;
#77922=CARTESIAN_POINT('Ctrl Pts',(1.79322013108717,-0.316574402604296,
6.79533188669132)) ;
#77923=CARTESIAN_POINT('Ctrl Pts',(1.80862659259988,-0.321853195169852,
6.85523985899825)) ;
#77924=CARTESIAN_POINT('Ctrl Pts',(1.8240260136469,-0.327130342614464,6.91514954549617)) ;
#77925=CARTESIAN_POINT('Ctrl Pts',(1.83942125592947,-0.332407254608771,
6.97506007039324)) ;
#77926=CARTESIAN_POINT('Ctrl Pts',(1.74734038623951,-0.332324264734023,
6.8058171575838)) ;
#77927=CARTESIAN_POINT('Ctrl Pts',(1.76280167491966,-0.337563919259379,
6.86571006109106)) ;
#77928=CARTESIAN_POINT('Ctrl Pts',(1.77825521655385,-0.342804601986199,
6.92560480456484)) ;
#77929=CARTESIAN_POINT('Ctrl Pts',(1.79370245617666,-0.34804457775358,6.98550115761311)) ;
#77930=CARTESIAN_POINT('Ctrl Pts',(1.7277101482095,-0.332764968591207,6.81085442572145)) ;
#77931=CARTESIAN_POINT('Ctrl Pts',(1.74319473414556,-0.338004233132618,
6.87073949345777)) ;
#77932=CARTESIAN_POINT('Ctrl Pts',(1.75867139282646,-0.343243675639329,
6.93062659534679)) ;
#77933=CARTESIAN_POINT('Ctrl Pts',(1.77414072885046,-0.348483282365398,
6.99051557427166)) ;
#77934=CARTESIAN_POINT('',(1.77414072885046,-0.348483282365534,6.99051557427321)) ;
#77935=CARTESIAN_POINT('',(1.86979680842779,-0.262281765411192,6.97334924403617)) ;
#77936=CARTESIAN_POINT('Origin',(1.77414072885046,-0.248863812556223,6.99923114854642)) ;
#77937=CARTESIAN_POINT('',(1.86979680842779,-0.262281765411192,6.97334924403617)) ;
#77938=CARTESIAN_POINT('',(1.7277101482095,-0.332764968591207,6.81085442572145)) ;
#77939=CARTESIAN_POINT('Ctrl Pts',(1.78257449869961,-0.351510169545935,
7.00768190451024)) ;
#77940=CARTESIAN_POINT('Ctrl Pts',(1.7799529947877,-0.349998638179854,7.00204079265479)) ;
#77941=CARTESIAN_POINT('Ctrl Pts',(1.77712384321888,-0.348988486534676,
6.99629008435113)) ;
#77942=CARTESIAN_POINT('Ctrl Pts',(1.77414072885046,-0.348483282365533,
6.9905155742732)) ;
#77943=CARTESIAN_POINT('Ctrl Pts',(1.80804353409323,-0.350030692236589,
7.00216042002312)) ;
#77944=CARTESIAN_POINT('Ctrl Pts',(1.80562039408462,-0.348758544781078,
6.99609033866212)) ;
#77945=CARTESIAN_POINT('Ctrl Pts',(1.80298985197567,-0.348031691489746,
6.98992923493177)) ;
#77946=CARTESIAN_POINT('Ctrl Pts',(1.80022303195211,-0.347898342883205,
6.98382968539505)) ;
#77947=CARTESIAN_POINT('Ctrl Pts',(1.85235642894571,-0.329284001344736,
6.9974230667741)) ;
#77948=CARTESIAN_POINT('Ctrl Pts',(1.85025698915433,-0.327717973988209,
6.98963152733252)) ;
#77949=CARTESIAN_POINT('Ctrl Pts',(1.84798352930075,-0.326928615466642,
6.98177037827477)) ;
#77950=CARTESIAN_POINT('Ctrl Pts',(1.84556753758067,-0.326868345860442,
6.97395707625726)) ;
#77951=CARTESIAN_POINT('Ctrl Pts',(1.87439171514777,-0.287344043373369,
7.00354079114491)) ;
#77952=CARTESIAN_POINT('Ctrl Pts',(1.87202794762724,-0.284665751804266,
6.99328116783747)) ;
#77953=CARTESIAN_POINT('Ctrl Pts',(1.86945702547209,-0.282962222021312,
6.98284900252257)) ;
#77954=CARTESIAN_POINT('Ctrl Pts',(1.86674074821325,-0.282225326148191,
6.97239378956659)) ;
#77955=CARTESIAN_POINT('Ctrl Pts',(1.87819429271644,-0.268591723493119,
7.00768190451025)) ;
#77956=CARTESIAN_POINT('Ctrl Pts',(1.87559269584777,-0.265429455820026,
6.99639968079935)) ;
#77957=CARTESIAN_POINT('Ctrl Pts',(1.87277553216535,-0.263323474391202,
6.98489826419203)) ;
#77958=CARTESIAN_POINT('Ctrl Pts',(1.86979680842779,-0.262281765411191,
6.97334924403617)) ;
#77959=CARTESIAN_POINT('',(1.78257449869961,-0.351510169545935,7.00768190451024)) ;
#77960=CARTESIAN_POINT('Origin',(1.7496148667176,-0.424101006082149,6.98537442848823)) ;
#77961=CARTESIAN_POINT('Origin',(1.78257449869961,-0.25491758691703,7.0335638090205)) ;
#77962=CARTESIAN_POINT('Origin',(1.8437775962156,-0.424925232050335,6.96360853179461)) ;
#77963=CARTESIAN_POINT('Ctrl Pts',(1.87819429271644,-0.268591723493119,
7.00768190451025)) ;
#77964=CARTESIAN_POINT('Ctrl Pts',(1.88761452163365,-0.293719598773199,
7.05576037364334)) ;
#77965=CARTESIAN_POINT('Ctrl Pts',(1.91803918302408,-0.376442517994261,
7.08160457645395)) ;
#77966=CARTESIAN_POINT('Ctrl Pts',(1.94251232165841,-0.447018030321371,
7.08179767010457)) ;
#77967=CARTESIAN_POINT('Ctrl Pts',(1.94270198330657,-0.447562773442322,
7.0818)) ;
#77968=CARTESIAN_POINT('Ctrl Pts',(1.94288959754295,-0.448102752174828,
7.0818)) ;
#77969=CARTESIAN_POINT('Ctrl Pts',(1.87312418929155,-0.293594816666786,
7.00216042002313)) ;
#77970=CARTESIAN_POINT('Ctrl Pts',(1.87796531081865,-0.311402705036871,
7.04213224265876)) ;
#77971=CARTESIAN_POINT('Ctrl Pts',(1.90981006047448,-0.381903712040289,
7.08210548357766)) ;
#77972=CARTESIAN_POINT('Ctrl Pts',(1.94240290834263,-0.447111003797951,
7.08179401271422)) ;
#77973=CARTESIAN_POINT('Ctrl Pts',(1.94264552853462,-0.447607689700649,
7.0818)) ;
#77974=CARTESIAN_POINT('Ctrl Pts',(1.94288959754295,-0.448102752174828,
7.0818)) ;
#77975=CARTESIAN_POINT('Ctrl Pts',(1.84631288834535,-0.334523890843293,
6.99742330171556)) ;
#77976=CARTESIAN_POINT('Ctrl Pts',(1.85235243119886,-0.341052363542231,
7.03081187673426)) ;
#77977=CARTESIAN_POINT('Ctrl Pts',(1.89649530787172,-0.391656352746195,
7.08258953702515)) ;
#77978=CARTESIAN_POINT('Ctrl Pts',(1.9422056175273,-0.447272672620484,7.08179067948988)) ;
#77979=CARTESIAN_POINT('Ctrl Pts',(1.94254673268371,-0.447686293152721,
7.0818)) ;
#77980=CARTESIAN_POINT('Ctrl Pts',(1.94288959754295,-0.448102752174828,
7.0818)) ;
#77981=CARTESIAN_POINT('Ctrl Pts',(1.80167627524483,-0.35040056156393,7.00354079114492)) ;
#77982=CARTESIAN_POINT('Ctrl Pts',(1.81914768429025,-0.359424731059544,
7.04558504389617)) ;
#77983=CARTESIAN_POINT('Ctrl Pts',(1.88400085754965,-0.402627171220613,
7.08196334045259)) ;
#77984=CARTESIAN_POINT('Ctrl Pts',(1.94200387814229,-0.447427752099798,
7.0817950153739)) ;
#77985=CARTESIAN_POINT('Ctrl Pts',(1.9424479368328,-0.447764896604793,7.0818)) ;
#77986=CARTESIAN_POINT('Ctrl Pts',(1.94288959754295,-0.448102752174828,
7.0818)) ;
#77987=CARTESIAN_POINT('Ctrl Pts',(1.78257449869961,-0.351510169545939,
7.00768190451026)) ;
#77988=CARTESIAN_POINT('Ctrl Pts',(1.8049172385957,-0.364392756523468,7.05576037364334)) ;
#77989=CARTESIAN_POINT('Ctrl Pts',(1.87864346526083,-0.407664253866157,
7.0816045764537)) ;
#77990=CARTESIAN_POINT('Ctrl Pts',(1.94191743214658,-0.447492414836479,
7.08179767010457)) ;
#77991=CARTESIAN_POINT('Ctrl Pts',(1.94240559575384,-0.447798583798538,
7.0818)) ;
#77992=CARTESIAN_POINT('Ctrl Pts',(1.94288959754295,-0.448102752174828,
7.0818)) ;
#77993=CARTESIAN_POINT('',(1.92349887676295,-0.435977594951427,7.08106549417672)) ;
#77994=CARTESIAN_POINT('Ctrl Pts',(1.78257449869961,-0.351510169545939,
7.00768190451026)) ;
#77995=CARTESIAN_POINT('Ctrl Pts',(1.80281774439894,-0.363182210425523,
7.0512425541009)) ;
#77996=CARTESIAN_POINT('Ctrl Pts',(1.86524142026312,-0.399800345703204,
7.07655121308398)) ;
#77997=CARTESIAN_POINT('Ctrl Pts',(1.92349887676295,-0.435977594951427,
7.08106549417672)) ;
#77998=CARTESIAN_POINT('Ctrl Pts',(1.92349887676295,-0.435977594951427,
7.08106549417672)) ;
#77999=CARTESIAN_POINT('Ctrl Pts',(1.92954095092715,-0.439729657539593,
7.08153368525129)) ;
#78000=CARTESIAN_POINT('Ctrl Pts',(1.93553821135059,-0.443476977758118,
7.08177820258746)) ;
#78001=CARTESIAN_POINT('Ctrl Pts',(1.94191743214658,-0.447492414836479,
7.08179767010457)) ;
#78002=CARTESIAN_POINT('Ctrl Pts',(1.94240559575384,-0.447798583798538,
7.0818)) ;
#78003=CARTESIAN_POINT('Ctrl Pts',(1.94288959754295,-0.448102752174832,
7.0818)) ;
#78004=CARTESIAN_POINT('Origin',(4.7625,-0.448102752174854,6.9818)) ;
#78005=CARTESIAN_POINT('',(1.17871069663557,-0.348483282365668,6.99051557427477)) ;
#78006=CARTESIAN_POINT('',(4.7625,-0.348483282365679,6.99051557427477)) ;
#78007=CARTESIAN_POINT('',(1.17871069663557,-0.448102752174842,7.0818)) ;
#78008=CARTESIAN_POINT('Origin',(1.17871069663557,-0.448102752174842,6.9818)) ;
#78009=CARTESIAN_POINT('',(4.7625,-0.448102752174854,7.0818)) ;
#78010=CARTESIAN_POINT('Origin',(-5.85328412995265E-15,-0.507999999999996,
8.8138)) ;
#78011=CARTESIAN_POINT('',(1.17558412963154,-0.332764968591537,6.81085442572523)) ;
#78012=CARTESIAN_POINT('',(-3.17578922261404E-15,-0.332764968591533,6.81085442572523)) ;
#78013=CARTESIAN_POINT('',(1.21039177030075,-0.507754795155589,8.81099729580349)) ;
#78014=CARTESIAN_POINT('Origin',(-2.86067568683591E-15,-0.233145498782359,
6.81957)) ;
#78015=CARTESIAN_POINT('',(1.13595304047784,-0.233145498782362,6.71957)) ;
#78016=CARTESIAN_POINT('',(-2.86067568683591E-15,-0.233145498782359,6.71957)) ;
#78017=CARTESIAN_POINT('Origin',(1.13595304047784,-0.233145498782362,6.81957)) ;
#78018=CARTESIAN_POINT('Origin',(9.525,-0.761999999999999,7.0818)) ;
#78019=CARTESIAN_POINT('',(4.53079829687583,-0.940377394107333,7.0818)) ;
#78020=CARTESIAN_POINT('',(0.662097436534802,-0.662040915602625,7.08180000837043)) ;
#78021=CARTESIAN_POINT('',(4.26139061324377,0.828785077739394,7.0818)) ;
#78022=CARTESIAN_POINT('',(0.,-0.662,7.0818)) ;
#78023=CARTESIAN_POINT('Origin',(0.78316098986,-0.783160989860008,8.78984143258953)) ;
#78024=CARTESIAN_POINT('',(0.570056476721783,-0.62397014614747,6.99051559580155)) ;
#78025=CARTESIAN_POINT('',(0.623970146872346,-0.570056475384991,6.99051558503157)) ;
#78026=CARTESIAN_POINT('Origin',(0.662092866158832,-0.662092866158839,6.98180002150834)) ;
#78027=CARTESIAN_POINT('',(0.611939867549498,-0.558026198990146,6.81085442572523)) ;
#78028=CARTESIAN_POINT('',(0.745038269223036,-0.691124600663685,8.7985570068643)) ;
#78029=CARTESIAN_POINT('',(0.558026198990139,-0.611939867549503,6.81085442572523)) ;
#78030=CARTESIAN_POINT('Origin',(0.650062588186462,-0.650062588186468,6.80213885145047)) ;
#78031=CARTESIAN_POINT('',(0.691124600663678,-0.745038269223043,8.7985570068643)) ;
#78032=CARTESIAN_POINT('Ctrl Pts',(0.611939867549498,-0.558026198990146,
6.81085442572523)) ;
#78033=CARTESIAN_POINT('Ctrl Pts',(0.606991841672517,-0.555410694880565,
6.7615916062195)) ;
#78034=CARTESIAN_POINT('Ctrl Pts',(0.554343935683234,-0.527581249784811,
6.71957)) ;
#78035=CARTESIAN_POINT('Ctrl Pts',(0.497571705638601,-0.497571705638606,
6.71957)) ;
#78036=CARTESIAN_POINT('Ctrl Pts',(0.587896866738726,-0.568073880351624,
6.81179156524867)) ;
#78037=CARTESIAN_POINT('Ctrl Pts',(0.584594051674637,-0.565801572147174,
6.76779239028237)) ;
#78038=CARTESIAN_POINT('Ctrl Pts',(0.545423040383758,-0.536502145084287,
6.71957)) ;
#78039=CARTESIAN_POINT('Ctrl Pts',(0.497571705638601,-0.497571705638606,
6.71957)) ;
#78040=CARTESIAN_POINT('Ctrl Pts',(0.568073880351618,-0.587896866738732,
6.81179156524867)) ;
#78041=CARTESIAN_POINT('Ctrl Pts',(0.565801572147168,-0.584594051674643,
6.76779239028237)) ;
#78042=CARTESIAN_POINT('Ctrl Pts',(0.536502145084281,-0.545423040383763,
6.71957)) ;
#78043=CARTESIAN_POINT('Ctrl Pts',(0.497571705638601,-0.497571705638606,
6.71957)) ;
#78044=CARTESIAN_POINT('Ctrl Pts',(0.558026198990139,-0.611939867549503,
6.81085442572523)) ;
#78045=CARTESIAN_POINT('Ctrl Pts',(0.555410694880558,-0.606991841672523,
6.7615916062195)) ;
#78046=CARTESIAN_POINT('Ctrl Pts',(0.527581249784805,-0.554343935683239,
6.71957)) ;
#78047=CARTESIAN_POINT('Ctrl Pts',(0.497571705638601,-0.497571705638606,
6.71957)) ;
#78048=CARTESIAN_POINT('',(0.497571705638601,-0.497571705638606,6.71957)) ;
#78049=CARTESIAN_POINT('Origin',(0.497571705638601,-0.497571705638606,6.81957)) ;
#78050=CARTESIAN_POINT('Origin',(0.497571705638601,-0.497571705638606,6.81957)) ;
#78051=CARTESIAN_POINT('Ctrl Pts',(0.570211858508875,-0.623522814049366,
6.99019330104746)) ;
#78052=CARTESIAN_POINT('Ctrl Pts',(0.551534852302403,-0.66859706764791,
6.99013167321749)) ;
#78053=CARTESIAN_POINT('Ctrl Pts',(0.511323934476222,-0.774035717122834,
7.02669496601772)) ;
#78054=CARTESIAN_POINT('Ctrl Pts',(0.500393372990465,-0.824248755690896,
7.13090837317487)) ;
#78055=CARTESIAN_POINT('Ctrl Pts',(0.506135855656206,-0.824114843544343,
7.19096167963447)) ;
#78056=CARTESIAN_POINT('Ctrl Pts',(0.572389430190026,-0.624473925984885,
7.01847383474068)) ;
#78057=CARTESIAN_POINT('Ctrl Pts',(0.555919328144446,-0.664025668947801,
7.01674468353812)) ;
#78058=CARTESIAN_POINT('Ctrl Pts',(0.51946533211283,-0.758487707726383,
7.04555073697094)) ;
#78059=CARTESIAN_POINT('Ctrl Pts',(0.509392765209136,-0.803866506829236,
7.13733008166825)) ;
#78060=CARTESIAN_POINT('Ctrl Pts',(0.514637480491472,-0.803235395049625,
7.19010329906211)) ;
#78061=CARTESIAN_POINT('Ctrl Pts',(0.596834745786804,-0.634684162135971,
7.06567536889322)) ;
#78062=CARTESIAN_POINT('Ctrl Pts',(0.58148813098266,-0.66359058095359,7.06148755378359)) ;
#78063=CARTESIAN_POINT('Ctrl Pts',(0.547001094686732,-0.736858584687579,
7.07722761166001)) ;
#78064=CARTESIAN_POINT('Ctrl Pts',(0.537223579811327,-0.773275882572783,
7.14735866455721)) ;
#78065=CARTESIAN_POINT('Ctrl Pts',(0.542264225761618,-0.772076546520768,
7.18739432697539)) ;
#78066=CARTESIAN_POINT('Ctrl Pts',(0.642838623428121,-0.653775168663864,
7.08186803342826)) ;
#78067=CARTESIAN_POINT('Ctrl Pts',(0.625161390776304,-0.677065029661441,
7.0799917878996)) ;
#78068=CARTESIAN_POINT('Ctrl Pts',(0.586673015296136,-0.734356346993357,
7.0955665033668)) ;
#78069=CARTESIAN_POINT('Ctrl Pts',(0.576089846021631,-0.762519575633863,
7.15155633346424)) ;
#78070=CARTESIAN_POINT('Ctrl Pts',(0.581621154777631,-0.761962620673718,
7.18360960381621)) ;
#78071=CARTESIAN_POINT('Ctrl Pts',(0.662501876072284,-0.661922887444048,
7.08179967671293)) ;
#78072=CARTESIAN_POINT('Ctrl Pts',(0.643838531330083,-0.684419215447178,
7.08178088077373)) ;
#78073=CARTESIAN_POINT('Ctrl Pts',(0.603650630034209,-0.737021368067473,
7.10004943267476)) ;
#78074=CARTESIAN_POINT('Ctrl Pts',(0.59272586137927,-0.762064059967634,
7.15203867446112)) ;
#78075=CARTESIAN_POINT('Ctrl Pts',(0.59846509565877,-0.761999983546755,
7.18199944835428)) ;
#78076=CARTESIAN_POINT('Origin',(0.662092865478666,-0.662092867812963,6.98180002156108)) ;
#78077=CARTESIAN_POINT('',(0.506191638276484,-0.823877279363035,7.19051557427477)) ;
#78078=CARTESIAN_POINT('Origin',(0.589034350751103,-0.623877279363035,7.19051557427477)) ;
#78079=CARTESIAN_POINT('Origin',(0.598228027472807,-0.862,7.1818)) ;
#78080=CARTESIAN_POINT('Origin',(0.681070739947425,-0.662,7.1818)) ;
#78081=CARTESIAN_POINT('Origin',(0.703226309181215,-0.862,8.29058094955136)) ;
#78082=CARTESIAN_POINT('',(0.639686894805695,-0.823877279363035,8.60022433223444)) ;
#78083=CARTESIAN_POINT('Origin',(0.731723284002017,-0.862,8.59150875795967)) ;
#78084=CARTESIAN_POINT('',(0.611189919984892,-0.823877279363035,8.29929652382612)) ;
#78085=CARTESIAN_POINT('Origin',(0.731723284002018,-0.862,8.59150875795967)) ;
#78086=CARTESIAN_POINT('',(0.745560008319435,-0.878300227999278,8.68919625781168)) ;
#78087=CARTESIAN_POINT('Origin',(0.731723284002018,-0.862,8.59150875795967)) ;
#78088=CARTESIAN_POINT('Origin',(0.731723284002018,-0.862,8.59150875795967)) ;
#78089=CARTESIAN_POINT('Origin',(0.662092866162312,-0.662092866162319,6.98180002156031)) ;
#78090=CARTESIAN_POINT('Origin',(0.662092866162312,-0.662092866162319,6.98180002156031)) ;
#78091=CARTESIAN_POINT('Origin',(0.600622180002914,-0.248785852819298,6.81957)) ;
#78092=CARTESIAN_POINT('',(0.692658569199237,-0.286908573456263,6.81085442572523)) ;
#78093=CARTESIAN_POINT('',(0.600622180002914,-0.248785852819298,6.71957)) ;
#78094=CARTESIAN_POINT('Origin',(0.248785852819292,-0.600622180002917,6.81957)) ;
#78095=CARTESIAN_POINT('',(1.13746140899457,-0.340348049204389,6.81085442572523)) ;
#78096=CARTESIAN_POINT('',(0.286908573456257,-0.692658569199239,6.81085442572523)) ;
#78097=CARTESIAN_POINT('Origin',(1.13595304047784,-0.233145498782362,6.81957)) ;
#78098=CARTESIAN_POINT('',(0.248785852819292,-0.600622180002917,6.71957)) ;
#78099=CARTESIAN_POINT('Origin',(0.353968116746248,-0.854554628096492,8.8138)) ;
#78100=CARTESIAN_POINT('',(1.1405879759986,-0.35606636297852,6.99051557427477)) ;
#78101=CARTESIAN_POINT('',(4.22326789260681,0.920821466935716,6.99051557427477)) ;
#78102=CARTESIAN_POINT('',(1.17226904966378,-0.515337875768441,8.81099729580349)) ;
#78103=CARTESIAN_POINT('Origin',(0.,-0.662,7.1818)) ;
#78104=CARTESIAN_POINT('Origin',(1.17871069663556,-0.448102752174842,6.9818)) ;
#78105=CARTESIAN_POINT('Origin',(1.17871069663557,-0.448102752174842,6.9818)) ;
#78106=CARTESIAN_POINT('Origin',(1.17871069663556,-0.448102752174842,6.9818)) ;
#78107=CARTESIAN_POINT('Origin',(4.26139061324377,0.828785077739394,6.9818)) ;
#78108=CARTESIAN_POINT('Ctrl Pts',(1.13595304047784,-0.233145498782362,
6.71957)) ;
#78109=CARTESIAN_POINT('Ctrl Pts',(1.136701792954,-0.286360727148735,6.71957)) ;
#78110=CARTESIAN_POINT('Ctrl Pts',(1.13739615091638,-0.335710036450631,
6.7615916062195)) ;
#78111=CARTESIAN_POINT('Ctrl Pts',(1.13746140899457,-0.340348049204389,
6.81085442572523)) ;
#78112=CARTESIAN_POINT('Ctrl Pts',(1.13595304047784,-0.233145498782362,
6.71957)) ;
#78113=CARTESIAN_POINT('Ctrl Pts',(1.14300981851451,-0.285105982851002,
6.71957)) ;
#78114=CARTESIAN_POINT('Ctrl Pts',(1.14898571310984,-0.331172502747836,
6.76307285057327)) ;
#78115=CARTESIAN_POINT('Ctrl Pts',(1.14951407564647,-0.335376993538154,
6.81107958928014)) ;
#78116=CARTESIAN_POINT('Ctrl Pts',(1.13595304047784,-0.233145498782362,
6.71957)) ;
#78117=CARTESIAN_POINT('Ctrl Pts',(1.14931784407502,-0.283851238553268,
6.71957)) ;
#78118=CARTESIAN_POINT('Ctrl Pts',(1.16142573132119,-0.328698029275172,
6.76307285057327)) ;
#78119=CARTESIAN_POINT('Ctrl Pts',(1.16254657695483,-0.33278466785003,6.81107958928014)) ;
#78120=CARTESIAN_POINT('Ctrl Pts',(1.13595304047784,-0.233145498782362,
6.71957)) ;
#78121=CARTESIAN_POINT('Ctrl Pts',(1.15562586963554,-0.282596494255535,
6.71957)) ;
#78122=CARTESIAN_POINT('Ctrl Pts',(1.17386952959435,-0.328455030351461,
6.7615916062195)) ;
#78123=CARTESIAN_POINT('Ctrl Pts',(1.17558412963154,-0.332764968591537,
6.81085442572523)) ;
#78124=CARTESIAN_POINT('Origin',(1.17558412963154,-0.432384438400711,6.80213885145047)) ;
#78125=CARTESIAN_POINT('Origin',(1.21039177030075,-0.607374264964764,8.80228172152873)) ;
#78126=CARTESIAN_POINT('Origin',(0.854554628096488,-0.353968116746257,8.8138)) ;
#78127=CARTESIAN_POINT('Origin',(0.415843288169369,-0.172247929781575,3.38615128096072)) ;
#78128=CARTESIAN_POINT('Ctrl Pts',(0.506127211989078,0.824152009451317,
7.1910316321799)) ;
#78129=CARTESIAN_POINT('Ctrl Pts',(0.501809041773239,0.824264612261489,
7.14592568561393)) ;
#78130=CARTESIAN_POINT('Ctrl Pts',(0.506923471858882,0.787787261003787,
7.04037309112129)) ;
#78131=CARTESIAN_POINT('Ctrl Pts',(0.545334841097466,0.683543325948836,
6.99003852412023)) ;
#78132=CARTESIAN_POINT('Ctrl Pts',(0.570236346572285,0.623452669067181,
6.99014289220396)) ;
#78133=CARTESIAN_POINT('Ctrl Pts',(0.514624648029491,0.803255895526573,
7.19016526186579)) ;
#78134=CARTESIAN_POINT('Ctrl Pts',(0.510681466432052,0.803741078245769,
7.15053005081949)) ;
#78135=CARTESIAN_POINT('Ctrl Pts',(0.515355266764848,0.771079003955546,
7.05746161448055)) ;
#78136=CARTESIAN_POINT('Ctrl Pts',(0.5504425504214,0.67713259929863,7.01611788244044)) ;
#78137=CARTESIAN_POINT('Ctrl Pts',(0.57239780574008,0.624406914644273,7.01844435868783)) ;
#78138=CARTESIAN_POINT('Ctrl Pts',(0.542247535402146,0.772088823972611,
7.18744210329384)) ;
#78139=CARTESIAN_POINT('Ctrl Pts',(0.538457964015581,0.772998673850379,
7.15737445763862)) ;
#78140=CARTESIAN_POINT('Ctrl Pts',(0.543010521485573,0.747243596469417,
7.08604143097494)) ;
#78141=CARTESIAN_POINT('Ctrl Pts',(0.576378560033105,0.673163426046941,
7.06005906538994)) ;
#78142=CARTESIAN_POINT('Ctrl Pts',(0.59683440132531,0.63463042821009,7.06566080680977)) ;
#78143=CARTESIAN_POINT('Ctrl Pts',(0.581601710084173,0.761968609442201,
7.18364859165186)) ;
#78144=CARTESIAN_POINT('Ctrl Pts',(0.577443273929768,0.76239427234713,7.15957559988958)) ;
#78145=CARTESIAN_POINT('Ctrl Pts',(0.582387971427533,0.74224455378735,7.10272807587653)) ;
#78146=CARTESIAN_POINT('Ctrl Pts',(0.619273986488659,0.68477307387316,7.07934238702147)) ;
#78147=CARTESIAN_POINT('Ctrl Pts',(0.64283537587001,0.65372731533594,7.08186031155257)) ;
#78148=CARTESIAN_POINT('Ctrl Pts',(0.598433070228347,0.761999835561857,
7.18203726713029)) ;
#78149=CARTESIAN_POINT('Ctrl Pts',(0.594118371016825,0.762055140288617,
7.15953504583831)) ;
#78150=CARTESIAN_POINT('Ctrl Pts',(0.599228555379945,0.743859867492796,
7.1068802277593)) ;
#78151=CARTESIAN_POINT('Ctrl Pts',(0.637610173763254,0.691856882134685,
7.08175608939188)) ;
#78152=CARTESIAN_POINT('Ctrl Pts',(0.66248519941671,0.661870077095634,7.08179987235985)) ;
#78153=CARTESIAN_POINT('Origin',(0.598228027472816,0.862,7.1818)) ;
#78154=CARTESIAN_POINT('Origin',(0.662092864798463,0.66209286945531,6.98180002156184)) ;
#78155=CARTESIAN_POINT('Origin',(0.703226309181224,0.862,8.29058094955135)) ;
#78156=CARTESIAN_POINT('',(0.731723284002027,0.762,8.59150875795967)) ;
#78157=CARTESIAN_POINT('Origin',(0.731723284002027,0.862,8.59150875795967)) ;
#78158=CARTESIAN_POINT('',(0.703226309181224,0.762,8.29058094955135)) ;
#78159=CARTESIAN_POINT('Origin',(0.731723284002027,0.862,8.59150875795967)) ;
#78160=CARTESIAN_POINT('',(0.745560008319444,0.878300227999278,8.68919625781167)) ;
#78161=CARTESIAN_POINT('Origin',(0.731723284002027,0.862,8.59150875795967)) ;
#78162=CARTESIAN_POINT('Origin',(0.731723284002027,0.862,8.59150875795967)) ;
#78163=CARTESIAN_POINT('Origin',(0.78316098986001,0.783160989860007,8.78984143258953)) ;
#78164=CARTESIAN_POINT('',(0.62397014687062,0.570056475383259,6.99051558500572)) ;
#78165=CARTESIAN_POINT('Origin',(0.662092866155378,0.662092866155375,6.98180002145664)) ;
#78166=CARTESIAN_POINT('',(0.611939867549505,0.558026198990145,6.81085442572523)) ;
#78167=CARTESIAN_POINT('Origin',(0.65006258818647,0.650062588186467,6.80213885145047)) ;
#78168=CARTESIAN_POINT('',(0.745038269223045,0.691124600663685,8.7985570068643)) ;
#78169=CARTESIAN_POINT('Ctrl Pts',(0.558026198990147,0.611939867549503,
6.81085442572523)) ;
#78170=CARTESIAN_POINT('Ctrl Pts',(0.555410694880566,0.606991841672522,
6.7615916062195)) ;
#78171=CARTESIAN_POINT('Ctrl Pts',(0.527581249784812,0.554343935683239,
6.71957)) ;
#78172=CARTESIAN_POINT('Ctrl Pts',(0.497571705638608,0.497571705638606,
6.71957)) ;
#78173=CARTESIAN_POINT('Ctrl Pts',(0.568073880351625,0.587896866738731,
6.81179156524867)) ;
#78174=CARTESIAN_POINT('Ctrl Pts',(0.565801572147175,0.584594051674642,
6.76779239028237)) ;
#78175=CARTESIAN_POINT('Ctrl Pts',(0.536502145084289,0.545423040383763,
6.71957)) ;
#78176=CARTESIAN_POINT('Ctrl Pts',(0.497571705638608,0.497571705638606,
6.71957)) ;
#78177=CARTESIAN_POINT('Ctrl Pts',(0.587896866738733,0.568073880351623,
6.81179156524867)) ;
#78178=CARTESIAN_POINT('Ctrl Pts',(0.584594051674644,0.565801572147173,
6.76779239028237)) ;
#78179=CARTESIAN_POINT('Ctrl Pts',(0.545423040383765,0.536502145084287,
6.71957)) ;
#78180=CARTESIAN_POINT('Ctrl Pts',(0.497571705638608,0.497571705638606,
6.71957)) ;
#78181=CARTESIAN_POINT('Ctrl Pts',(0.611939867549505,0.558026198990145,
6.81085442572523)) ;
#78182=CARTESIAN_POINT('Ctrl Pts',(0.606991841672524,0.555410694880564,
6.7615916062195)) ;
#78183=CARTESIAN_POINT('Ctrl Pts',(0.554343935683241,0.52758124978481,6.71957)) ;
#78184=CARTESIAN_POINT('Ctrl Pts',(0.497571705638608,0.497571705638606,
6.71957)) ;
#78185=CARTESIAN_POINT('Origin',(0.497571705638608,0.497571705638606,6.81957)) ;
#78186=CARTESIAN_POINT('Origin',(0.66209286616232,0.662092866162318,6.98180002156031)) ;
#78187=CARTESIAN_POINT('Origin',(0.66209286616232,0.662092866162318,6.98180002156031)) ;
#78188=CARTESIAN_POINT('Origin',(0.507879677365696,0.210370650418538,3.37743570668595)) ;
#78189=CARTESIAN_POINT('Origin',(0.517483568940244,0.214348712560276,3.376526246514)) ;
#78190=CARTESIAN_POINT('Origin',(0.,0.862,3.42553041237115)) ;
#78191=CARTESIAN_POINT('',(3.07434158440252,0.762,7.64111756647598)) ;
#78192=CARTESIAN_POINT('Origin',(0.,0.762,3.42553041237115)) ;
#78193=CARTESIAN_POINT('',(3.13247669898886,0.878300227999278,7.72083338058588)) ;
#78194=CARTESIAN_POINT('Origin',(3.07434158440252,0.862,7.64111756647598)) ;
#78195=CARTESIAN_POINT('Origin',(0.,0.878300227999278,3.42553041237115)) ;
#78196=CARTESIAN_POINT('Origin',(-9.525,0.762,8.72161438184689)) ;
#78197=CARTESIAN_POINT('',(3.21546217517793,0.762,7.36730649953872)) ;
#78198=CARTESIAN_POINT('',(3.21546217517793,0.762,0.)) ;
#78199=CARTESIAN_POINT('Ctrl Pts',(3.07434158440252,0.762,7.64111756647598)) ;
#78200=CARTESIAN_POINT('Ctrl Pts',(3.12354729023977,0.762,7.60523285051226)) ;
#78201=CARTESIAN_POINT('Ctrl Pts',(3.1930870265562,0.762,7.51957043397612)) ;
#78202=CARTESIAN_POINT('Ctrl Pts',(3.21546217517793,0.762,7.41298214194023)) ;
#78203=CARTESIAN_POINT('Ctrl Pts',(3.21546217517793,0.762,7.36730649953872)) ;
#78204=CARTESIAN_POINT('Origin',(0.353968116746258,0.854554628096494,8.8138)) ;
#78205=CARTESIAN_POINT('',(1.13746140899458,0.340348049204384,6.81085442572523)) ;
#78206=CARTESIAN_POINT('',(0.286908573456264,0.692658569199241,6.81085442572523)) ;
#78207=CARTESIAN_POINT('',(1.14058797599861,0.356066362978515,6.99051557427477)) ;
#78208=CARTESIAN_POINT('',(1.17226904966379,0.515337875768437,8.81099729580349)) ;
#78209=CARTESIAN_POINT('',(4.49267557623886,-1.03241378330366,6.99051557427477)) ;
#78210=CARTESIAN_POINT('Origin',(1.17871069663557,0.448102752174838,6.9818)) ;
#78211=CARTESIAN_POINT('Origin',(1.17871069663557,0.448102752174838,6.9818)) ;
#78212=CARTESIAN_POINT('Origin',(1.17871069663557,0.448102752174838,6.9818)) ;
#78213=CARTESIAN_POINT('Origin',(4.53079829687583,-0.940377394107333,6.9818)) ;
#78214=CARTESIAN_POINT('Origin',(1.21039177030075,0.60737426496476,8.80228172152873)) ;
#78215=CARTESIAN_POINT('Origin',(1.17558412963154,0.432384438400707,6.80213885145047)) ;
#78216=CARTESIAN_POINT('Ctrl Pts',(1.13746140899458,0.340348049204384,6.81085442572523)) ;
#78217=CARTESIAN_POINT('Ctrl Pts',(1.13739615091639,0.335710036450627,6.7615916062195)) ;
#78218=CARTESIAN_POINT('Ctrl Pts',(1.136701792954,0.286360727148731,6.71957)) ;
#78219=CARTESIAN_POINT('Ctrl Pts',(1.13595304047785,0.233145498782358,6.71957)) ;
#78220=CARTESIAN_POINT('Ctrl Pts',(1.14951407564648,0.33537699353815,6.81107958928014)) ;
#78221=CARTESIAN_POINT('Ctrl Pts',(1.14898571310985,0.331172502747832,6.76307285057327)) ;
#78222=CARTESIAN_POINT('Ctrl Pts',(1.14300981851451,0.285105982850998,6.71957)) ;
#78223=CARTESIAN_POINT('Ctrl Pts',(1.13595304047785,0.233145498782358,6.71957)) ;
#78224=CARTESIAN_POINT('Ctrl Pts',(1.16254657695484,0.332784667850026,6.81107958928014)) ;
#78225=CARTESIAN_POINT('Ctrl Pts',(1.16142573132119,0.328698029275168,6.76307285057327)) ;
#78226=CARTESIAN_POINT('Ctrl Pts',(1.14931784407503,0.283851238553264,6.71957)) ;
#78227=CARTESIAN_POINT('Ctrl Pts',(1.13595304047785,0.233145498782358,6.71957)) ;
#78228=CARTESIAN_POINT('Ctrl Pts',(1.17558412963154,0.332764968591532,6.81085442572523)) ;
#78229=CARTESIAN_POINT('Ctrl Pts',(1.17386952959436,0.328455030351457,6.7615916062195)) ;
#78230=CARTESIAN_POINT('Ctrl Pts',(1.15562586963554,0.282596494255531,6.71957)) ;
#78231=CARTESIAN_POINT('Ctrl Pts',(1.13595304047785,0.233145498782358,6.71957)) ;
#78232=CARTESIAN_POINT('',(1.13595304047785,0.233145498782358,6.71957)) ;
#78233=CARTESIAN_POINT('Origin',(1.13595304047785,0.233145498782358,6.81957)) ;
#78234=CARTESIAN_POINT('Origin',(1.13595304047785,0.233145498782358,6.81957)) ;
#78235=CARTESIAN_POINT('Origin',(0.,0.233145498782358,6.81957)) ;
#78236=CARTESIAN_POINT('',(0.,0.233145498782358,6.71957)) ;
#78237=CARTESIAN_POINT('Origin',(0.248785852819299,0.600622180002918,6.81957)) ;
#78238=CARTESIAN_POINT('',(0.248785852819299,0.600622180002918,6.71957)) ;
#78239=CARTESIAN_POINT('Origin',(-5.2341907152369E-16,7.49419702465636E-15,
6.81957)) ;
#78240=CARTESIAN_POINT('Origin',(-5.2341907152369E-16,7.49419702465636E-15,
6.71957)) ;
#78241=CARTESIAN_POINT('Origin',(-1.38777878078145E-16,7.18180894821816E-15,
6.79368809548975)) ;
#78242=CARTESIAN_POINT('Origin',(-4.22508734431004E-15,1.88057342394262E-15,
6.81957)) ;
#78243=CARTESIAN_POINT('Origin',(-4.22508734431004E-15,1.88057342394262E-15,
6.71957)) ;
#78244=CARTESIAN_POINT('Origin',(-4.65139692566778E-15,2.35922392732846E-15,
6.79368809548975)) ;
#78245=CARTESIAN_POINT('Origin',(0.,0.,6.81957)) ;
#78246=CARTESIAN_POINT('Origin',(0.,0.,6.71957)) ;
#78247=CARTESIAN_POINT('Origin',(0.,-7.43633015083647E-17,6.79368809548975)) ;
#78248=CARTESIAN_POINT('Origin',(-0.854554628096486,0.353968116746271,8.8138)) ;
#78249=CARTESIAN_POINT('Origin',(-0.415843288169369,0.172247929781578,3.38615128096072)) ;
#78250=CARTESIAN_POINT('Origin',(0.,0.,8.8138)) ;
#78251=CARTESIAN_POINT('Origin',(0.,0.,6.71957)) ;
#78252=CARTESIAN_POINT('Origin',(0.,-0.862,3.42553041237115)) ;
#78253=CARTESIAN_POINT('',(3.13247669898886,-0.878300227999278,7.72083338058589)) ;
#78254=CARTESIAN_POINT('Origin',(0.,-0.878300227999278,3.42553041237115)) ;
#78255=CARTESIAN_POINT('Origin',(3.07434158440252,-0.862,7.64111756647598)) ;
#78256=CARTESIAN_POINT('Ctrl Pts',(3.13247669898886,-0.878300227999278,
7.72083338058588)) ;
#78257=CARTESIAN_POINT('Ctrl Pts',(3.24194772411599,-0.884393761686983,
7.63975239746791)) ;
#78258=CARTESIAN_POINT('Ctrl Pts',(3.31205160669424,-0.887893661760288,
7.50491108098797)) ;
#78259=CARTESIAN_POINT('Ctrl Pts',(3.31205160669424,-0.887893661760288,
7.36730649953872)) ;
#78260=CARTESIAN_POINT('Ctrl Pts',(3.13406331600289,-0.862001836852293,
7.72300897562607)) ;
#78261=CARTESIAN_POINT('Ctrl Pts',(3.24484531401722,-0.867681983706699,
7.64234029129293)) ;
#78262=CARTESIAN_POINT('Ctrl Pts',(3.3165712033995,-0.871034506014564,7.50637222518225)) ;
#78263=CARTESIAN_POINT('Ctrl Pts',(3.3165712033995,-0.871034506014564,7.36730649953872)) ;
#78264=CARTESIAN_POINT('Ctrl Pts',(3.13236709785152,-0.828113890360543,
7.7206830937248)) ;
#78265=CARTESIAN_POINT('Ctrl Pts',(3.24344041373217,-0.832362489170559,
7.64188726219099)) ;
#78266=CARTESIAN_POINT('Ctrl Pts',(3.31655021571401,-0.83498349586979,7.50636187808678)) ;
#78267=CARTESIAN_POINT('Ctrl Pts',(3.31655021571401,-0.83498349586979,7.36730649953871)) ;
#78268=CARTESIAN_POINT('Ctrl Pts',(3.11315074038068,-0.778100046144805,
7.69433331199796)) ;
#78269=CARTESIAN_POINT('Ctrl Pts',(3.21661438879145,-0.779302983062094,
7.62174351094937)) ;
#78270=CARTESIAN_POINT('Ctrl Pts',(3.28499976832129,-0.780067219187875,
7.49621911028266)) ;
#78271=CARTESIAN_POINT('Ctrl Pts',(3.28499976832129,-0.780067219187875,
7.36730649953872)) ;
#78272=CARTESIAN_POINT('Ctrl Pts',(3.08894215024221,-0.762,7.66113809968827)) ;
#78273=CARTESIAN_POINT('Ctrl Pts',(3.18160442136363,-0.761976718953809,
7.59466385085047)) ;
#78274=CARTESIAN_POINT('Ctrl Pts',(3.24164385284348,-0.762,7.48231337878088)) ;
#78275=CARTESIAN_POINT('Ctrl Pts',(3.24164385284348,-0.762,7.36730649953872)) ;
#78276=CARTESIAN_POINT('Ctrl Pts',(3.07434158440252,-0.762,7.64111756647598)) ;
#78277=CARTESIAN_POINT('Ctrl Pts',(3.16045156961772,-0.762,7.57831931353947)) ;
#78278=CARTESIAN_POINT('Ctrl Pts',(3.21546217517793,-0.762,7.47388299847558)) ;
#78279=CARTESIAN_POINT('Ctrl Pts',(3.21546217517793,-0.762,7.36730649953872)) ;
#78280=CARTESIAN_POINT('Ctrl Pts',(3.13247669898886,-0.878300227999278,
7.72083338058588)) ;
#78281=CARTESIAN_POINT('Ctrl Pts',(3.24194772411599,-0.884393761686983,
7.63975239746791)) ;
#78282=CARTESIAN_POINT('Ctrl Pts',(3.31205160669424,-0.887893661760288,
7.50491108098797)) ;
#78283=CARTESIAN_POINT('Ctrl Pts',(3.31205160669424,-0.887893661760288,
7.36730649953872)) ;
#78284=CARTESIAN_POINT('Origin',(0.507879677365692,-0.21037065041854,3.37743570668596)) ;
#78285=CARTESIAN_POINT('Origin',(0.51748356894024,-0.214348712560278,3.376526246514)) ;
#78286=CARTESIAN_POINT('Origin',(-4.22508734431003E-15,3.18503882869472E-15,
8.18016875778516)) ;
#78287=CARTESIAN_POINT('Origin',(-4.3836885553672E-15,3.19189119579733E-15,
8.20605066229541)) ;
#78288=CARTESIAN_POINT('Origin',(-4.30498280490066E-15,3.24526720351407E-15,
8.27007790985519)) ;
#78289=CARTESIAN_POINT('Origin',(-3.21546217517793,-0.862,0.)) ;
#78290=CARTESIAN_POINT('',(-3.31205160669424,-0.887893661760289,7.36730649953872)) ;
#78291=CARTESIAN_POINT('',(-3.31205160669424,-0.887893661760288,0.)) ;
#78292=CARTESIAN_POINT('Origin',(-3.21546217517793,-0.862,7.36730649953872)) ;
#78293=CARTESIAN_POINT('Ctrl Pts',(-3.31205160669424,-0.887893661760288,
7.36730649953872)) ;
#78294=CARTESIAN_POINT('Ctrl Pts',(-3.31205160669424,-0.887893661760288,
7.50491119623589)) ;
#78295=CARTESIAN_POINT('Ctrl Pts',(-3.24194781580122,-0.884393766790498,
7.63975232956018)) ;
#78296=CARTESIAN_POINT('Ctrl Pts',(-3.13247669898886,-0.878300227999278,
7.72083338058588)) ;
#78297=CARTESIAN_POINT('Ctrl Pts',(-3.3165712033995,-0.871034506014564,
7.36730649953872)) ;
#78298=CARTESIAN_POINT('Ctrl Pts',(-3.3165712033995,-0.871034506014564,
7.50637234165392)) ;
#78299=CARTESIAN_POINT('Ctrl Pts',(-3.24484540680043,-0.867681988463991,
7.64234022373052)) ;
#78300=CARTESIAN_POINT('Ctrl Pts',(-3.13406331600289,-0.862001836852293,
7.72300897562607)) ;
#78301=CARTESIAN_POINT('Ctrl Pts',(-3.31655021571397,-0.834983495869826,
7.36730649953871)) ;
#78302=CARTESIAN_POINT('Ctrl Pts',(-3.31655021571397,-0.834983495869826,
7.50636199454979)) ;
#78303=CARTESIAN_POINT('Ctrl Pts',(-3.24344050675935,-0.832362492728917,
7.64188719619712)) ;
#78304=CARTESIAN_POINT('Ctrl Pts',(-3.13236709785151,-0.828113890360574,
7.72068309372478)) ;
#78305=CARTESIAN_POINT('Ctrl Pts',(-3.28499976832123,-0.780067219188007,
7.36730649953872)) ;
#78306=CARTESIAN_POINT('Ctrl Pts',(-3.28499976832123,-0.780067219188007,
7.49621921825079)) ;
#78307=CARTESIAN_POINT('Ctrl Pts',(-3.2166144754453,-0.779302984069696,
7.62174345015321)) ;
#78308=CARTESIAN_POINT('Ctrl Pts',(-3.11315074038065,-0.778100046144912,
7.69433331199791)) ;
#78309=CARTESIAN_POINT('Ctrl Pts',(-3.24164385284348,-0.762,7.36730649953872)) ;
#78310=CARTESIAN_POINT('Ctrl Pts',(-3.24164385284348,-0.762,7.48231347510255)) ;
#78311=CARTESIAN_POINT('Ctrl Pts',(-3.18160449897102,-0.761976718934311,
7.59466379517632)) ;
#78312=CARTESIAN_POINT('Ctrl Pts',(-3.08894215024221,-0.762,7.66113809968827)) ;
#78313=CARTESIAN_POINT('Ctrl Pts',(-3.21546217517793,-0.762,7.36730649953872)) ;
#78314=CARTESIAN_POINT('Ctrl Pts',(-3.21546217517793,-0.762,7.47388308773656)) ;
#78315=CARTESIAN_POINT('Ctrl Pts',(-3.16045164173738,-0.762,7.57831926094407)) ;
#78316=CARTESIAN_POINT('Ctrl Pts',(-3.07434158440252,-0.762,7.64111756647598)) ;
#78317=CARTESIAN_POINT('Ctrl Pts',(-3.31205160669424,-0.887893661760288,
7.36730649953872)) ;
#78318=CARTESIAN_POINT('Ctrl Pts',(-3.31205160669424,-0.887893661760288,
7.50491119623589)) ;
#78319=CARTESIAN_POINT('Ctrl Pts',(-3.24194781580122,-0.884393766790498,
7.63975232956018)) ;
#78320=CARTESIAN_POINT('Ctrl Pts',(-3.13247669898886,-0.878300227999278,
7.72083338058588)) ;
#78321=CARTESIAN_POINT('Origin',(0.,0.,3.42553041237115)) ;
#78322=CARTESIAN_POINT('Origin',(0.,-5.74654389008192E-16,7.72083338058588)) ;
#78323=CARTESIAN_POINT('Origin',(0.,-8.67361737988404E-16,7.36730649953872)) ;
#78324=CARTESIAN_POINT('Origin',(0.,-7.44125213282148E-16,7.36730649953872)) ;
#78325=CARTESIAN_POINT('Origin',(0.,0.,0.)) ;
#78326=CARTESIAN_POINT('Ctrl Pts',(-3.21546217517793,0.762,7.36730649953872)) ;
#78327=CARTESIAN_POINT('Ctrl Pts',(-3.21546217517793,0.762,7.41298218019493)) ;
#78328=CARTESIAN_POINT('Ctrl Pts',(-3.19308177554602,0.762,7.51957930543031)) ;
#78329=CARTESIAN_POINT('Ctrl Pts',(-3.12354733145101,0.762,7.60523282045775)) ;
#78330=CARTESIAN_POINT('Ctrl Pts',(-3.07434158440252,0.762,7.64111756647598)) ;
#78331=CARTESIAN_POINT('Ctrl Pts',(-3.23291662695496,0.762,7.36730649953872)) ;
#78332=CARTESIAN_POINT('Ctrl Pts',(-3.23291662695496,0.762,7.41538680927401)) ;
#78333=CARTESIAN_POINT('Ctrl Pts',(-3.20919044530172,0.7619991985266,7.52759091140272)) ;
#78334=CARTESIAN_POINT('Ctrl Pts',(-3.1357727028504,0.761998534434387,7.61717961816928)) ;
#78335=CARTESIAN_POINT('Ctrl Pts',(-3.08407529496231,0.762,7.65446458861751)) ;
#78336=CARTESIAN_POINT('Ctrl Pts',(-3.26773265822935,0.771355198514182,
7.36730649953871)) ;
#78337=CARTESIAN_POINT('Ctrl Pts',(-3.26773265822935,0.771355198514182,
7.42018495670109)) ;
#78338=CARTESIAN_POINT('Ctrl Pts',(-3.24132584545736,0.771198194794288,
7.54357471788814)) ;
#78339=CARTESIAN_POINT('Ctrl Pts',(-3.16016819309997,0.770710393590129,
7.6410163084456)) ;
#78340=CARTESIAN_POINT('Ctrl Pts',(-3.10349960406018,0.770364006601212,
7.6810995169956)) ;
#78341=CARTESIAN_POINT('Ctrl Pts',(-3.31260641155451,0.816049431227016,
7.36730649953872)) ;
#78342=CARTESIAN_POINT('Ctrl Pts',(-3.31260641155451,0.816049431227016,
7.42635027754646)) ;
#78343=CARTESIAN_POINT('Ctrl Pts',(-3.28302099203104,0.815206773658776,
7.56414693052081)) ;
#78344=CARTESIAN_POINT('Ctrl Pts',(-3.19241201477822,0.812575144026894,
7.67241987682184)) ;
#78345=CARTESIAN_POINT('Ctrl Pts',(-3.12944289962309,0.81069277169432,7.71667338558099)) ;
#78346=CARTESIAN_POINT('Ctrl Pts',(-3.31883100175212,0.862604928141702,
7.36730649953872)) ;
#78347=CARTESIAN_POINT('Ctrl Pts',(-3.31883100175212,0.862604928141702,
7.42724277748668)) ;
#78348=CARTESIAN_POINT('Ctrl Pts',(-3.2893920752126,0.861258395620179,7.56706915453154)) ;
#78349=CARTESIAN_POINT('Ctrl Pts',(-3.19856097674223,0.856983205993464,
7.67811414352739)) ;
#78350=CARTESIAN_POINT('Ctrl Pts',(-3.13485662450991,0.853852641278801,
7.72409677314616)) ;
#78351=CARTESIAN_POINT('Ctrl Pts',(-3.31205160669424,0.887893661760288,
7.36730649953872)) ;
#78352=CARTESIAN_POINT('Ctrl Pts',(-3.31205160669424,0.887893661760288,
7.42627994098036)) ;
#78353=CARTESIAN_POINT('Ctrl Pts',(-3.28354207485051,0.886445036569108,
7.56391115375268)) ;
#78354=CARTESIAN_POINT('Ctrl Pts',(-3.19503162288163,0.881782250165689,
7.67450135142834)) ;
#78355=CARTESIAN_POINT('Ctrl Pts',(-3.13247669898886,0.878300227999278,
7.72083338058589)) ;
#78356=CARTESIAN_POINT('',(-3.13247669898886,0.878300227999279,7.72083338058589)) ;
#78357=CARTESIAN_POINT('Origin',(-3.07434158440252,0.862,7.64111756647598)) ;
#78358=CARTESIAN_POINT('Ctrl Pts',(-3.13247669898886,0.878300227999278,
7.72083338058589)) ;
#78359=CARTESIAN_POINT('Ctrl Pts',(-3.15125721360594,0.879345616021897,
7.7069233748392)) ;
#78360=CARTESIAN_POINT('Ctrl Pts',(-3.16898822142431,0.880324705415051,
7.69152912899859)) ;
#78361=CARTESIAN_POINT('Ctrl Pts',(-3.20181219242865,0.882115453804949,
7.65815848336878)) ;
#78362=CARTESIAN_POINT('Ctrl Pts',(-3.21691237399404,0.882927612145381,
7.6401903396444)) ;
#78363=CARTESIAN_POINT('Ctrl Pts',(-3.24406613551655,0.88436959350386,7.60211786955277)) ;
#78364=CARTESIAN_POINT('Ctrl Pts',(-3.25612892273065,0.885000021482306,
7.5820210842502)) ;
#78365=CARTESIAN_POINT('Ctrl Pts',(-3.27008056843648,0.885725501365387,
7.55390876065276)) ;
#78366=CARTESIAN_POINT('Ctrl Pts',(-3.2734427045829,0.885900005481902,7.54664209868898)) ;
#78367=CARTESIAN_POINT('Ctrl Pts',(-3.28536345129656,0.886519241337546,
7.51890596267789)) ;
#78368=CARTESIAN_POINT('Ctrl Pts',(-3.29258331858232,0.886895069252813,
7.49782797698803)) ;
#78369=CARTESIAN_POINT('Ctrl Pts',(-3.30372575706298,0.887471400743178,
7.45480156534341)) ;
#78370=CARTESIAN_POINT('Ctrl Pts',(-3.30765080218502,0.887672045043684,
7.43285457715974)) ;
#78371=CARTESIAN_POINT('Ctrl Pts',(-3.31132435060191,0.887857745113204,
7.39630625236233)) ;
#78372=CARTESIAN_POINT('Ctrl Pts',(-3.31205160669424,0.887893661760288,
7.38180486361516)) ;
#78373=CARTESIAN_POINT('Ctrl Pts',(-3.31205160669424,0.887893661760288,
7.36730649953872)) ;
#78374=CARTESIAN_POINT('Origin',(0.,0.862,3.42553041237115)) ;
#78375=CARTESIAN_POINT('Origin',(0.,0.878300227999278,3.42553041237115)) ;
#78376=CARTESIAN_POINT('Origin',(-0.507879677365692,0.210370650418544,3.37743570668596)) ;
#78377=CARTESIAN_POINT('Origin',(-0.51748356894024,0.214348712560283,3.376526246514)) ;
#78378=CARTESIAN_POINT('Origin',(-0.135929041739323,1.4180803283024E-15,
3.41363816217501)) ;
#78379=CARTESIAN_POINT('Origin',(-0.138499429641961,1.44489591144929E-15,
3.41341328237267)) ;
#78380=CARTESIAN_POINT('Ctrl Pts',(3.07434158440252,0.762,7.64111756647598)) ;
#78381=CARTESIAN_POINT('Ctrl Pts',(3.12354729023977,0.762,7.60523285051226)) ;
#78382=CARTESIAN_POINT('Ctrl Pts',(3.1930870265562,0.762,7.51957043397612)) ;
#78383=CARTESIAN_POINT('Ctrl Pts',(3.21546217517793,0.762,7.41298214194023)) ;
#78384=CARTESIAN_POINT('Ctrl Pts',(3.21546217517793,0.762,7.36730649953872)) ;
#78385=CARTESIAN_POINT('Ctrl Pts',(3.08407529496231,0.762,7.65446458861751)) ;
#78386=CARTESIAN_POINT('Ctrl Pts',(3.13577265955232,0.761998534435614,7.61717964939652)) ;
#78387=CARTESIAN_POINT('Ctrl Pts',(3.20919599213541,0.761999198366373,7.52758160791742)) ;
#78388=CARTESIAN_POINT('Ctrl Pts',(3.23291662695496,0.762,7.41538676900536)) ;
#78389=CARTESIAN_POINT('Ctrl Pts',(3.23291662695496,0.762,7.36730649953872)) ;
#78390=CARTESIAN_POINT('Ctrl Pts',(3.10349960406021,0.770364006601186,7.68109951699563)) ;
#78391=CARTESIAN_POINT('Ctrl Pts',(3.1601681456384,0.770710393299994,7.64101634201648)) ;
#78392=CARTESIAN_POINT('Ctrl Pts',(3.24133198224179,0.771198231737204,7.54356455202267)) ;
#78393=CARTESIAN_POINT('Ctrl Pts',(3.2677326582294,0.771355198514153,7.42018491241385)) ;
#78394=CARTESIAN_POINT('Ctrl Pts',(3.2677326582294,0.771355198514153,7.36730649953871)) ;
#78395=CARTESIAN_POINT('Ctrl Pts',(3.12944289962316,0.810692771694295,7.71667338558108)) ;
#78396=CARTESIAN_POINT('Ctrl Pts',(3.19241196203983,0.812575142450328,7.67241991388553)) ;
#78397=CARTESIAN_POINT('Ctrl Pts',(3.28302784295196,0.815206972212267,7.56413561454693)) ;
#78398=CARTESIAN_POINT('Ctrl Pts',(3.31260641155465,0.816049431226997,7.42635022809559)) ;
#78399=CARTESIAN_POINT('Ctrl Pts',(3.31260641155465,0.816049431226997,7.36730649953872)) ;
#78400=CARTESIAN_POINT('Ctrl Pts',(3.13485662450991,0.853852641278801,7.72409677314616)) ;
#78401=CARTESIAN_POINT('Ctrl Pts',(3.19856092338799,0.856983203371525,7.67811418203917)) ;
#78402=CARTESIAN_POINT('Ctrl Pts',(3.28939894471721,0.861258718801572,7.56705759107582)) ;
#78403=CARTESIAN_POINT('Ctrl Pts',(3.31883100175212,0.862604928141702,7.42724272728831)) ;
#78404=CARTESIAN_POINT('Ctrl Pts',(3.31883100175212,0.862604928141702,7.36730649953872)) ;
#78405=CARTESIAN_POINT('Ctrl Pts',(3.13247669898886,0.878300227999278,7.72083338058588)) ;
#78406=CARTESIAN_POINT('Ctrl Pts',(3.19503157049007,0.881782247249395,7.67450139023276)) ;
#78407=CARTESIAN_POINT('Ctrl Pts',(3.2835487590593,0.886445388078747,7.56389969951321)) ;
#78408=CARTESIAN_POINT('Ctrl Pts',(3.31205160669424,0.887893661760288,7.42627989158839)) ;
#78409=CARTESIAN_POINT('Ctrl Pts',(3.31205160669424,0.887893661760288,7.36730649953872)) ;
#78410=CARTESIAN_POINT('',(3.31205160669424,0.887893661760288,7.36730649953872)) ;
#78411=CARTESIAN_POINT('Origin',(3.21546217517793,0.862,7.36730649953872)) ;
#78412=CARTESIAN_POINT('Ctrl Pts',(3.31205160669424,0.887893661760288,7.36730649953872)) ;
#78413=CARTESIAN_POINT('Ctrl Pts',(3.31205160669424,0.887893661760288,7.38956143771478)) ;
#78414=CARTESIAN_POINT('Ctrl Pts',(3.31033560020008,0.887808601466395,7.41182249790195)) ;
#78415=CARTESIAN_POINT('Ctrl Pts',(3.30351690635115,0.887460286770387,7.45583467472282)) ;
#78416=CARTESIAN_POINT('Ctrl Pts',(3.29841004269922,0.887196799265865,7.47758437086555)) ;
#78417=CARTESIAN_POINT('Ctrl Pts',(3.28732603928197,0.886621411389359,7.5125396219205)) ;
#78418=CARTESIAN_POINT('Ctrl Pts',(3.28228994385203,0.886359400067986,7.52605670555331)) ;
#78419=CARTESIAN_POINT('Ctrl Pts',(3.26737490624966,0.885584721481954,7.56076103741013)) ;
#78420=CARTESIAN_POINT('Ctrl Pts',(3.25642579234752,0.885016920148674,7.58148532526352)) ;
#78421=CARTESIAN_POINT('Ctrl Pts',(3.23139243072244,0.883699376658414,7.62095135160198)) ;
#78422=CARTESIAN_POINT('Ctrl Pts',(3.21730269907916,0.882949261558222,7.63968874680989)) ;
#78423=CARTESIAN_POINT('Ctrl Pts',(3.18634388333276,0.881275273044124,7.67476016953305)) ;
#78424=CARTESIAN_POINT('Ctrl Pts',(3.16946465452307,0.88035071777546,7.69108408662551)) ;
#78425=CARTESIAN_POINT('Ctrl Pts',(3.14525705790316,0.879010759195164,7.71110108522053)) ;
#78426=CARTESIAN_POINT('Ctrl Pts',(3.13892867704792,0.878659367283939,7.71605464828228)) ;
#78427=CARTESIAN_POINT('Ctrl Pts',(3.13247669898886,0.878300227999279,7.72083338058589)) ;
#78428=CARTESIAN_POINT('Origin',(3.21546217517793,0.861999999999999,0.)) ;
#78429=CARTESIAN_POINT('',(3.31205160669424,0.887893661760288,0.)) ;
#78430=CARTESIAN_POINT('Origin',(0.,0.,3.42553041237115)) ;
#78431=CARTESIAN_POINT('Origin',(0.,-5.74654389008192E-16,7.72083338058588)) ;
#78432=CARTESIAN_POINT('Origin',(0.,-8.67361737988404E-16,7.36730649953872)) ;
#78433=CARTESIAN_POINT('Origin',(0.,-7.44125213282148E-16,7.36730649953872)) ;
#78434=CARTESIAN_POINT('Origin',(0.,0.,0.)) ;
#78435=CARTESIAN_POINT('Origin',(0.,0.,0.5953125)) ;
#78436=CARTESIAN_POINT('',(-1.56389349909515,6.20727076724186E-13,0.406605999095151)) ;
#78437=CARTESIAN_POINT('Ctrl Pts',(-1.56389349909515,1.24170639048682E-12,
0.40660599909515)) ;
#78438=CARTESIAN_POINT('Ctrl Pts',(-1.56745804029789,-0.0734174872881957,
0.410170540297885)) ;
#78439=CARTESIAN_POINT('Ctrl Pts',(-1.56574208917974,-0.143162522998449,
0.413636286609932)) ;
#78440=CARTESIAN_POINT('Ctrl Pts',(-1.55193928496058,-0.310682384668358,
0.422105828519627)) ;
#78441=CARTESIAN_POINT('Ctrl Pts',(-1.53358392757052,-0.412143684651979,
0.427385555715839)) ;
#78442=CARTESIAN_POINT('Ctrl Pts',(-1.447702417125,-0.715662399845767,0.443633913138531)) ;
#78443=CARTESIAN_POINT('Ctrl Pts',(-1.34947303687865,-0.906569448029718,
0.454496467611271)) ;
#78444=CARTESIAN_POINT('Ctrl Pts',(-1.15133056045185,-1.15429653660643,
0.469686241696881)) ;
#78445=CARTESIAN_POINT('Ctrl Pts',(-1.07768308713858,-1.22969696342727,
0.474530087857337)) ;
#78446=CARTESIAN_POINT('Ctrl Pts',(-0.836867957885233,-1.43446115704913,
0.489835648281197)) ;
#78447=CARTESIAN_POINT('Ctrl Pts',(-0.650095663570034,-1.53964452624183,
0.500458351416618)) ;
#78448=CARTESIAN_POINT('Ctrl Pts',(-0.216304224148064,-1.68393625033617,
0.522791960259464)) ;
#78449=CARTESIAN_POINT('Ctrl Pts',(0.00797445504568436,-1.70157489439822,
0.532602184785555)) ;
#78450=CARTESIAN_POINT('Ctrl Pts',(0.39442070359125,-1.67235506214807,0.550645164261604)) ;
#78451=CARTESIAN_POINT('Ctrl Pts',(0.578381302744751,-1.62749177136662,
0.559673597083784)) ;
#78452=CARTESIAN_POINT('Ctrl Pts',(0.838857844667483,-1.51645723159726,
0.57311954012989)) ;
#78453=CARTESIAN_POINT('Ctrl Pts',(0.923066437402856,-1.47199035969867,
0.577586656827061)) ;
#78454=CARTESIAN_POINT('Ctrl Pts',(1.11065896487304,-1.35208673309619,0.587837823942977)) ;
#78455=CARTESIAN_POINT('Ctrl Pts',(1.18850492238163,-1.2858292868164,0.592330998254932)) ;
#78456=CARTESIAN_POINT('Ctrl Pts',(1.23927534453555,-1.23927534486525,0.5953124999899)) ;
#78457=CARTESIAN_POINT('',(-1.1572875,-1.41726843256824E-16,6.93889390390723E-17)) ;
#78458=CARTESIAN_POINT('',(-1.7526,-2.14631598018565E-16,0.5953125)) ;
#78459=CARTESIAN_POINT('Origin',(0.,0.,0.)) ;
#78460=CARTESIAN_POINT('Ctrl Pts',(0.726199640324296,-1.00145522282725,
0.0797567518095781)) ;
#78461=CARTESIAN_POINT('Ctrl Pts',(0.85827032683805,-0.91812330569503,0.0898263199638132)) ;
#78462=CARTESIAN_POINT('Ctrl Pts',(0.966230127421333,-0.81477793631574,
0.0985476242080515)) ;
#78463=CARTESIAN_POINT('Ctrl Pts',(1.14142047749138,-0.584869602376768,
0.116935473138185)) ;
#78464=CARTESIAN_POINT('Ctrl Pts',(1.20940238333913,-0.45431006970221,0.126370642327099)) ;
#78465=CARTESIAN_POINT('Ctrl Pts',(1.31992804059758,-0.108087210236051,
0.14918186937396)) ;
#78466=CARTESIAN_POINT('Ctrl Pts',(1.320127313916,0.0729480435983187,0.159158271321901)) ;
#78467=CARTESIAN_POINT('Ctrl Pts',(1.29419866014635,0.367183226884352,0.176917483314036)) ;
#78468=CARTESIAN_POINT('Ctrl Pts',(1.24602456229177,0.534537805855587,0.187567821710453)) ;
#78469=CARTESIAN_POINT('Ctrl Pts',(1.06285410240392,0.89276995042693,0.211685938535209)) ;
#78470=CARTESIAN_POINT('Ctrl Pts',(0.928597035203795,1.02719764559811,0.221685613693348)) ;
#78471=CARTESIAN_POINT('Ctrl Pts',(0.693985903348748,1.22533564983316,0.239291466200409)) ;
#78472=CARTESIAN_POINT('Ctrl Pts',(0.534496651620149,1.31426473081559,0.249960727937322)) ;
#78473=CARTESIAN_POINT('Ctrl Pts',(0.140400650614174,1.44310966165732,0.273743112836897)) ;
#78474=CARTESIAN_POINT('Ctrl Pts',(-0.0567292878068117,1.44660339865736,
0.283709043024783)) ;
#78475=CARTESIAN_POINT('Ctrl Pts',(-0.384490687238328,1.42007491780602,
0.301724326338965)) ;
#78476=CARTESIAN_POINT('Ctrl Pts',(-0.568439624563353,1.36843547863331,
0.312409905281157)) ;
#78477=CARTESIAN_POINT('Ctrl Pts',(-0.943592421571356,1.17947003346788,
0.335505788342169)) ;
#78478=CARTESIAN_POINT('Ctrl Pts',(-1.09490202949618,1.04247043391369,0.345447089068427)) ;
#78479=CARTESIAN_POINT('Ctrl Pts',(-1.32988994898806,0.765621603495837,
0.364510040364269)) ;
#78480=CARTESIAN_POINT('Ctrl Pts',(-1.42735349524037,0.59169431681732,0.375202747150079)) ;
#78481=CARTESIAN_POINT('Ctrl Pts',(-1.53569636645461,0.262270120156304,
0.393498668676532)) ;
#78482=CARTESIAN_POINT('Ctrl Pts',(-1.5577870170388,0.125772867603548,0.400499517038806)) ;
#78483=CARTESIAN_POINT('Ctrl Pts',(-1.56389349909515,1.24143750834804E-12,
0.406605999095151)) ;
#78484=CARTESIAN_POINT('Origin',(-4.22508734431003E-15,3.79252875187005E-15,
8.8138)) ;
#78485=CARTESIAN_POINT('Origin',(4.32558592440026E-16,8.45017468862007E-15,
8.8138)) ;
#78486=CARTESIAN_POINT('Origin',(0.,0.,0.)) ;
#78487=CARTESIAN_POINT('Ctrl Pts',(0.,1.23704425180958,-0.396875000000002)) ;
#78488=CARTESIAN_POINT('Ctrl Pts',(-0.512400506355204,1.23704425180958,
-0.347265625000002)) ;
#78489=CARTESIAN_POINT('Ctrl Pts',(-0.874722379082389,0.874722379082389,
-0.297656250000002)) ;
#78490=CARTESIAN_POINT('Ctrl Pts',(-1.23704425180958,0.512400506355204,
-0.248046875000002)) ;
#78491=CARTESIAN_POINT('Ctrl Pts',(-1.23704425180958,7.57471141691114E-17,
-0.198437500000002)) ;
#78492=CARTESIAN_POINT('Ctrl Pts',(-1.23704425180958,-0.512400506355204,
-0.148828125000002)) ;
#78493=CARTESIAN_POINT('Ctrl Pts',(-0.874722379082389,-0.874722379082389,
-0.0992187500000016)) ;
#78494=CARTESIAN_POINT('Ctrl Pts',(-0.512400506355204,-1.23704425180958,
-0.0496093750000016)) ;
#78495=CARTESIAN_POINT('Ctrl Pts',(-1.51494228338223E-16,-1.23704425180958,
-1.62630325872826E-15)) ;
#78496=CARTESIAN_POINT('Ctrl Pts',(0.512400506355204,-1.23704425180958,
0.0496093749999984)) ;
#78497=CARTESIAN_POINT('Ctrl Pts',(0.874722379082389,-0.87472237908239,
0.0992187499999984)) ;
#78498=CARTESIAN_POINT('Ctrl Pts',(1.23704425180957,-0.512400506355205,
0.148828124999998)) ;
#78499=CARTESIAN_POINT('Ctrl Pts',(1.23704425180958,-2.27241342507334E-16,
0.198437499999998)) ;
#78500=CARTESIAN_POINT('Ctrl Pts',(1.23704425180957,0.512400506355204,0.248046874999998)) ;
#78501=CARTESIAN_POINT('Ctrl Pts',(0.87472237908239,0.874722379082389,0.297656249999998)) ;
#78502=CARTESIAN_POINT('Ctrl Pts',(0.512400506355205,1.23704425180957,0.347265624999998)) ;
#78503=CARTESIAN_POINT('Ctrl Pts',(0.,1.23704425180958,0.396874999999998)) ;
#78504=CARTESIAN_POINT('Ctrl Pts',(-0.512400506355204,1.23704425180958,
0.446484374999998)) ;
#78505=CARTESIAN_POINT('Ctrl Pts',(-0.874722379082389,0.874722379082389,
0.496093749999998)) ;
#78506=CARTESIAN_POINT('Ctrl Pts',(-1.23704425180958,0.512400506355204,
0.545703124999998)) ;
#78507=CARTESIAN_POINT('Ctrl Pts',(-1.23704425180958,7.57471141691114E-17,
0.595312499999998)) ;
#78508=CARTESIAN_POINT('Ctrl Pts',(-1.23704425180958,-0.512400506355204,
0.644921874999998)) ;
#78509=CARTESIAN_POINT('Ctrl Pts',(-0.874722379082389,-0.874722379082389,
0.694531249999998)) ;
#78510=CARTESIAN_POINT('Ctrl Pts',(-0.512400506355204,-1.23704425180958,
0.744140624999998)) ;
#78511=CARTESIAN_POINT('Ctrl Pts',(-1.51494228338223E-16,-1.23704425180958,
0.793749999999998)) ;
#78512=CARTESIAN_POINT('Ctrl Pts',(0.512400506355204,-1.23704425180958,
0.843359374999998)) ;
#78513=CARTESIAN_POINT('Ctrl Pts',(0.874722379082389,-0.87472237908239,
0.892968749999998)) ;
#78514=CARTESIAN_POINT('Ctrl Pts',(1.23704425180957,-0.512400506355205,
0.942578124999999)) ;
#78515=CARTESIAN_POINT('Ctrl Pts',(1.23704425180958,-2.27241342507334E-16,
0.992187499999998)) ;
#78516=CARTESIAN_POINT('Ctrl Pts',(1.23704425180957,0.512400506355204,1.041796875)) ;
#78517=CARTESIAN_POINT('Ctrl Pts',(0.87472237908239,0.874722379082389,1.09140625)) ;
#78518=CARTESIAN_POINT('Ctrl Pts',(0.512400506355205,1.23704425180957,1.141015625)) ;
#78519=CARTESIAN_POINT('Ctrl Pts',(0.,1.23704425180958,1.190625)) ;
#78520=CARTESIAN_POINT('Ctrl Pts',(-0.512400506355204,1.23704425180958,
1.240234375)) ;
#78521=CARTESIAN_POINT('Ctrl Pts',(-0.874722379082389,0.874722379082389,
1.28984375)) ;
#78522=CARTESIAN_POINT('Ctrl Pts',(-1.23704425180958,0.512400506355204,
1.339453125)) ;
#78523=CARTESIAN_POINT('Ctrl Pts',(-1.23704425180958,7.57471141691114E-17,
1.3890625)) ;
#78524=CARTESIAN_POINT('Ctrl Pts',(-1.23704425180958,-0.512400506355204,
1.438671875)) ;
#78525=CARTESIAN_POINT('Ctrl Pts',(-0.874722379082389,-0.874722379082389,
1.48828125)) ;
#78526=CARTESIAN_POINT('Ctrl Pts',(-0.512400506355204,-1.23704425180958,
1.537890625)) ;
#78527=CARTESIAN_POINT('Ctrl Pts',(-1.51494228338223E-16,-1.23704425180958,
1.5875)) ;
#78528=CARTESIAN_POINT('Ctrl Pts',(0.512400506355204,-1.23704425180958,
1.637109375)) ;
#78529=CARTESIAN_POINT('Ctrl Pts',(0.874722379082389,-0.87472237908239,
1.68671875)) ;
#78530=CARTESIAN_POINT('Ctrl Pts',(1.23704425180957,-0.512400506355205,
1.736328125)) ;
#78531=CARTESIAN_POINT('Ctrl Pts',(1.23704425180958,-2.27241342507334E-16,
1.7859375)) ;
#78532=CARTESIAN_POINT('Ctrl Pts',(1.23704425180957,0.512400506355204,1.835546875)) ;
#78533=CARTESIAN_POINT('Ctrl Pts',(0.87472237908239,0.874722379082389,1.88515625)) ;
#78534=CARTESIAN_POINT('Ctrl Pts',(0.512400506355205,1.23704425180957,1.934765625)) ;
#78535=CARTESIAN_POINT('Ctrl Pts',(0.,1.23704425180958,1.984375)) ;
#78536=CARTESIAN_POINT('Ctrl Pts',(-0.512400506355204,1.23704425180958,
2.033984375)) ;
#78537=CARTESIAN_POINT('Ctrl Pts',(-0.874722379082389,0.874722379082389,
2.08359375)) ;
#78538=CARTESIAN_POINT('Ctrl Pts',(-1.23704425180958,0.512400506355204,
2.133203125)) ;
#78539=CARTESIAN_POINT('Ctrl Pts',(-1.23704425180958,7.57471141691114E-17,
2.1828125)) ;
#78540=CARTESIAN_POINT('Ctrl Pts',(-1.23704425180958,-0.512400506355204,
2.232421875)) ;
#78541=CARTESIAN_POINT('Ctrl Pts',(-0.874722379082389,-0.874722379082389,
2.28203125)) ;
#78542=CARTESIAN_POINT('Ctrl Pts',(-0.512400506355204,-1.23704425180958,
2.331640625)) ;
#78543=CARTESIAN_POINT('Ctrl Pts',(-1.51494228338223E-16,-1.23704425180958,
2.38125)) ;
#78544=CARTESIAN_POINT('Ctrl Pts',(0.512400506355204,-1.23704425180958,
2.430859375)) ;
#78545=CARTESIAN_POINT('Ctrl Pts',(0.874722379082389,-0.87472237908239,
2.48046875)) ;
#78546=CARTESIAN_POINT('Ctrl Pts',(1.23704425180957,-0.512400506355205,
2.530078125)) ;
#78547=CARTESIAN_POINT('Ctrl Pts',(1.23704425180958,-2.27241342507334E-16,
2.5796875)) ;
#78548=CARTESIAN_POINT('Ctrl Pts',(1.23704425180957,0.512400506355204,2.629296875)) ;
#78549=CARTESIAN_POINT('Ctrl Pts',(0.87472237908239,0.874722379082389,2.67890625)) ;
#78550=CARTESIAN_POINT('Ctrl Pts',(0.512400506355205,1.23704425180957,2.728515625)) ;
#78551=CARTESIAN_POINT('Ctrl Pts',(0.,1.23704425180958,2.778125)) ;
#78552=CARTESIAN_POINT('Ctrl Pts',(-0.512400506355204,1.23704425180958,
2.827734375)) ;
#78553=CARTESIAN_POINT('Ctrl Pts',(-0.874722379082389,0.874722379082389,
2.87734375)) ;
#78554=CARTESIAN_POINT('Ctrl Pts',(-1.23704425180958,0.512400506355204,
2.926953125)) ;
#78555=CARTESIAN_POINT('Ctrl Pts',(-1.23704425180958,7.57471141691114E-17,
2.9765625)) ;
#78556=CARTESIAN_POINT('Ctrl Pts',(-1.23704425180958,-0.512400506355204,
3.026171875)) ;
#78557=CARTESIAN_POINT('Ctrl Pts',(-0.874722379082389,-0.874722379082389,
3.07578125)) ;
#78558=CARTESIAN_POINT('Ctrl Pts',(-0.512400506355204,-1.23704425180958,
3.125390625)) ;
#78559=CARTESIAN_POINT('Ctrl Pts',(-1.51494228338223E-16,-1.23704425180958,
3.175)) ;
#78560=CARTESIAN_POINT('Ctrl Pts',(0.512400506355204,-1.23704425180958,
3.224609375)) ;
#78561=CARTESIAN_POINT('Ctrl Pts',(0.874722379082389,-0.87472237908239,
3.27421875)) ;
#78562=CARTESIAN_POINT('Ctrl Pts',(1.23704425180957,-0.512400506355205,
3.323828125)) ;
#78563=CARTESIAN_POINT('Ctrl Pts',(1.23704425180958,-2.27241342507334E-16,
3.3734375)) ;
#78564=CARTESIAN_POINT('Ctrl Pts',(1.23704425180957,0.512400506355204,3.423046875)) ;
#78565=CARTESIAN_POINT('Ctrl Pts',(0.87472237908239,0.874722379082389,3.47265625)) ;
#78566=CARTESIAN_POINT('Ctrl Pts',(0.512400506355205,1.23704425180957,3.522265625)) ;
#78567=CARTESIAN_POINT('Ctrl Pts',(0.,1.23704425180958,3.571875)) ;
#78568=CARTESIAN_POINT('Ctrl Pts',(-0.512400506355204,1.23704425180958,
3.621484375)) ;
#78569=CARTESIAN_POINT('Ctrl Pts',(-0.874722379082389,0.874722379082389,
3.67109375)) ;
#78570=CARTESIAN_POINT('Ctrl Pts',(-1.23704425180958,0.512400506355204,
3.720703125)) ;
#78571=CARTESIAN_POINT('Ctrl Pts',(-1.23704425180958,7.57471141691114E-17,
3.7703125)) ;
#78572=CARTESIAN_POINT('Ctrl Pts',(-1.23704425180958,-0.512400506355204,
3.819921875)) ;
#78573=CARTESIAN_POINT('Ctrl Pts',(-0.874722379082389,-0.874722379082389,
3.86953125)) ;
#78574=CARTESIAN_POINT('Ctrl Pts',(-0.512400506355204,-1.23704425180958,
3.919140625)) ;
#78575=CARTESIAN_POINT('Ctrl Pts',(-1.51494228338223E-16,-1.23704425180958,
3.96875)) ;
#78576=CARTESIAN_POINT('Ctrl Pts',(0.512400506355204,-1.23704425180958,
4.018359375)) ;
#78577=CARTESIAN_POINT('Ctrl Pts',(0.874722379082389,-0.87472237908239,
4.06796875)) ;
#78578=CARTESIAN_POINT('Ctrl Pts',(1.23704425180957,-0.512400506355205,
4.117578125)) ;
#78579=CARTESIAN_POINT('Ctrl Pts',(1.23704425180958,-2.27241342507334E-16,
4.1671875)) ;
#78580=CARTESIAN_POINT('Ctrl Pts',(1.23704425180957,0.512400506355204,4.216796875)) ;
#78581=CARTESIAN_POINT('Ctrl Pts',(0.87472237908239,0.874722379082389,4.26640625)) ;
#78582=CARTESIAN_POINT('Ctrl Pts',(0.512400506355205,1.23704425180957,4.316015625)) ;
#78583=CARTESIAN_POINT('Ctrl Pts',(0.,1.23704425180958,4.365625)) ;
#78584=CARTESIAN_POINT('Ctrl Pts',(-0.512400506355204,1.23704425180958,
4.415234375)) ;
#78585=CARTESIAN_POINT('Ctrl Pts',(-0.874722379082389,0.874722379082389,
4.46484375)) ;
#78586=CARTESIAN_POINT('Ctrl Pts',(-1.23704425180958,0.512400506355204,
4.514453125)) ;
#78587=CARTESIAN_POINT('Ctrl Pts',(-1.23704425180958,7.57471141691114E-17,
4.5640625)) ;
#78588=CARTESIAN_POINT('Ctrl Pts',(-1.23704425180958,-0.512400506355204,
4.613671875)) ;
#78589=CARTESIAN_POINT('Ctrl Pts',(-0.874722379082389,-0.874722379082389,
4.66328125)) ;
#78590=CARTESIAN_POINT('Ctrl Pts',(-0.512400506355204,-1.23704425180958,
4.712890625)) ;
#78591=CARTESIAN_POINT('Ctrl Pts',(-1.51494228338223E-16,-1.23704425180958,
4.7625)) ;
#78592=CARTESIAN_POINT('Ctrl Pts',(0.512400506355204,-1.23704425180958,
4.812109375)) ;
#78593=CARTESIAN_POINT('Ctrl Pts',(0.874722379082389,-0.87472237908239,
4.86171875)) ;
#78594=CARTESIAN_POINT('Ctrl Pts',(1.23704425180957,-0.512400506355205,
4.911328125)) ;
#78595=CARTESIAN_POINT('Ctrl Pts',(1.23704425180958,-2.27241342507334E-16,
4.9609375)) ;
#78596=CARTESIAN_POINT('Ctrl Pts',(1.23704425180957,0.512400506355204,5.010546875)) ;
#78597=CARTESIAN_POINT('Ctrl Pts',(0.87472237908239,0.874722379082389,5.06015625)) ;
#78598=CARTESIAN_POINT('Ctrl Pts',(0.512400506355205,1.23704425180957,5.109765625)) ;
#78599=CARTESIAN_POINT('Ctrl Pts',(0.,1.23704425180958,5.159375)) ;
#78600=CARTESIAN_POINT('Ctrl Pts',(-0.512400506355204,1.23704425180958,
5.208984375)) ;
#78601=CARTESIAN_POINT('Ctrl Pts',(-0.874722379082389,0.874722379082389,
5.25859375)) ;
#78602=CARTESIAN_POINT('Ctrl Pts',(-1.23704425180958,0.512400506355204,
5.308203125)) ;
#78603=CARTESIAN_POINT('Ctrl Pts',(-1.23704425180958,7.57471141691114E-17,
5.3578125)) ;
#78604=CARTESIAN_POINT('Ctrl Pts',(-1.23704425180958,-0.512400506355204,
5.407421875)) ;
#78605=CARTESIAN_POINT('Ctrl Pts',(-0.874722379082389,-0.874722379082389,
5.45703125)) ;
#78606=CARTESIAN_POINT('Ctrl Pts',(-0.512400506355204,-1.23704425180958,
5.506640625)) ;
#78607=CARTESIAN_POINT('Ctrl Pts',(-1.51494228338223E-16,-1.23704425180958,
5.55625)) ;
#78608=CARTESIAN_POINT('Ctrl Pts',(0.512400506355204,-1.23704425180958,
5.605859375)) ;
#78609=CARTESIAN_POINT('Ctrl Pts',(0.874722379082389,-0.87472237908239,
5.65546875)) ;
#78610=CARTESIAN_POINT('Ctrl Pts',(1.23704425180957,-0.512400506355205,
5.705078125)) ;
#78611=CARTESIAN_POINT('Ctrl Pts',(1.23704425180958,-2.27241342507334E-16,
5.7546875)) ;
#78612=CARTESIAN_POINT('Ctrl Pts',(1.23704425180957,0.512400506355204,5.804296875)) ;
#78613=CARTESIAN_POINT('Ctrl Pts',(0.87472237908239,0.874722379082389,5.85390625)) ;
#78614=CARTESIAN_POINT('Ctrl Pts',(0.512400506355205,1.23704425180957,5.903515625)) ;
#78615=CARTESIAN_POINT('Ctrl Pts',(0.,1.23704425180958,5.953125)) ;
#78616=CARTESIAN_POINT('Ctrl Pts',(-0.512400506355204,1.23704425180958,
6.002734375)) ;
#78617=CARTESIAN_POINT('Ctrl Pts',(-0.874722379082389,0.874722379082389,
6.05234375)) ;
#78618=CARTESIAN_POINT('Ctrl Pts',(-1.23704425180958,0.512400506355204,
6.101953125)) ;
#78619=CARTESIAN_POINT('Ctrl Pts',(-1.23704425180958,7.57471141691114E-17,
6.1515625)) ;
#78620=CARTESIAN_POINT('Ctrl Pts',(-1.23704425180958,-0.512400506355204,
6.201171875)) ;
#78621=CARTESIAN_POINT('Ctrl Pts',(-0.874722379082389,-0.874722379082389,
6.25078125)) ;
#78622=CARTESIAN_POINT('Ctrl Pts',(-0.512400506355204,-1.23704425180958,
6.300390625)) ;
#78623=CARTESIAN_POINT('Ctrl Pts',(-1.51494228338223E-16,-1.23704425180958,
6.35)) ;
#78624=CARTESIAN_POINT('Ctrl Pts',(0.512400506355204,-1.23704425180958,
6.399609375)) ;
#78625=CARTESIAN_POINT('Ctrl Pts',(0.874722379082389,-0.87472237908239,
6.44921875)) ;
#78626=CARTESIAN_POINT('Ctrl Pts',(1.23704425180957,-0.512400506355205,
6.498828125)) ;
#78627=CARTESIAN_POINT('Ctrl Pts',(1.23704425180958,-2.27241342507334E-16,
6.5484375)) ;
#78628=CARTESIAN_POINT('Ctrl Pts',(1.23704425180957,0.512400506355204,6.598046875)) ;
#78629=CARTESIAN_POINT('Ctrl Pts',(0.87472237908239,0.874722379082389,6.64765625)) ;
#78630=CARTESIAN_POINT('Ctrl Pts',(0.512400506355205,1.23704425180957,6.697265625)) ;
#78631=CARTESIAN_POINT('Ctrl Pts',(0.,1.23704425180958,6.746875)) ;
#78632=CARTESIAN_POINT('Ctrl Pts',(0.,1.75262906179543,-0.694548028835418)) ;
#78633=CARTESIAN_POINT('Ctrl Pts',(-0.725962727204902,1.75262906179543,
-0.644938653835418)) ;
#78634=CARTESIAN_POINT('Ctrl Pts',(-1.23929589450017,1.23929589450017,-0.595329278835418)) ;
#78635=CARTESIAN_POINT('Ctrl Pts',(-1.75262906179543,0.725962727204902,
-0.545719903835418)) ;
#78636=CARTESIAN_POINT('Ctrl Pts',(-1.75262906179543,1.0731757853102E-16,
-0.496110528835418)) ;
#78637=CARTESIAN_POINT('Ctrl Pts',(-1.75262906179543,-0.725962727204902,
-0.446501153835418)) ;
#78638=CARTESIAN_POINT('Ctrl Pts',(-1.23929589450017,-1.23929589450017,
-0.396891778835418)) ;
#78639=CARTESIAN_POINT('Ctrl Pts',(-0.725962727204902,-1.75262906179543,
-0.347282403835418)) ;
#78640=CARTESIAN_POINT('Ctrl Pts',(-2.14635157062041E-16,-1.75262906179543,
-0.297673028835418)) ;
#78641=CARTESIAN_POINT('Ctrl Pts',(0.725962727204902,-1.75262906179543,
-0.248063653835418)) ;
#78642=CARTESIAN_POINT('Ctrl Pts',(1.23929589450017,-1.23929589450017,-0.198454278835418)) ;
#78643=CARTESIAN_POINT('Ctrl Pts',(1.75262906179543,-0.725962727204903,
-0.148844903835418)) ;
#78644=CARTESIAN_POINT('Ctrl Pts',(1.75262906179543,-3.21952735593061E-16,
-0.0992355288354184)) ;
#78645=CARTESIAN_POINT('Ctrl Pts',(1.75262906179543,0.725962727204903,-0.0496261538354183)) ;
#78646=CARTESIAN_POINT('Ctrl Pts',(1.23929589450017,1.23929589450017,-1.67788354183017E-5)) ;
#78647=CARTESIAN_POINT('Ctrl Pts',(0.725962727204903,1.75262906179543,0.0495925961645818)) ;
#78648=CARTESIAN_POINT('Ctrl Pts',(0.,1.75262906179543,0.0992019711645818)) ;
#78649=CARTESIAN_POINT('Ctrl Pts',(-0.725962727204902,1.75262906179543,
0.148811346164582)) ;
#78650=CARTESIAN_POINT('Ctrl Pts',(-1.23929589450017,1.23929589450017,0.198420721164582)) ;
#78651=CARTESIAN_POINT('Ctrl Pts',(-1.75262906179543,0.725962727204902,
0.248030096164582)) ;
#78652=CARTESIAN_POINT('Ctrl Pts',(-1.75262906179543,1.0731757853102E-16,
0.297639471164582)) ;
#78653=CARTESIAN_POINT('Ctrl Pts',(-1.75262906179543,-0.725962727204902,
0.347248846164582)) ;
#78654=CARTESIAN_POINT('Ctrl Pts',(-1.23929589450017,-1.23929589450017,
0.396858221164582)) ;
#78655=CARTESIAN_POINT('Ctrl Pts',(-0.725962727204902,-1.75262906179543,
0.446467596164582)) ;
#78656=CARTESIAN_POINT('Ctrl Pts',(-2.14635157062041E-16,-1.75262906179543,
0.496076971164582)) ;
#78657=CARTESIAN_POINT('Ctrl Pts',(0.725962727204902,-1.75262906179543,
0.545686346164582)) ;
#78658=CARTESIAN_POINT('Ctrl Pts',(1.23929589450017,-1.23929589450017,0.595295721164582)) ;
#78659=CARTESIAN_POINT('Ctrl Pts',(1.75262906179543,-0.725962727204903,
0.644905096164582)) ;
#78660=CARTESIAN_POINT('Ctrl Pts',(1.75262906179543,-3.21952735593061E-16,
0.694514471164582)) ;
#78661=CARTESIAN_POINT('Ctrl Pts',(1.75262906179543,0.725962727204903,0.744123846164582)) ;
#78662=CARTESIAN_POINT('Ctrl Pts',(1.23929589450017,1.23929589450017,0.793733221164582)) ;
#78663=CARTESIAN_POINT('Ctrl Pts',(0.725962727204903,1.75262906179543,0.843342596164582)) ;
#78664=CARTESIAN_POINT('Ctrl Pts',(0.,1.75262906179543,0.892951971164582)) ;
#78665=CARTESIAN_POINT('Ctrl Pts',(-0.725962727204902,1.75262906179543,
0.942561346164582)) ;
#78666=CARTESIAN_POINT('Ctrl Pts',(-1.23929589450017,1.23929589450017,0.992170721164582)) ;
#78667=CARTESIAN_POINT('Ctrl Pts',(-1.75262906179543,0.725962727204902,
1.04178009616459)) ;
#78668=CARTESIAN_POINT('Ctrl Pts',(-1.75262906179543,1.0731757853102E-16,
1.09138947116459)) ;
#78669=CARTESIAN_POINT('Ctrl Pts',(-1.75262906179543,-0.725962727204902,
1.14099884616459)) ;
#78670=CARTESIAN_POINT('Ctrl Pts',(-1.23929589450017,-1.23929589450017,
1.19060822116459)) ;
#78671=CARTESIAN_POINT('Ctrl Pts',(-0.725962727204902,-1.75262906179543,
1.24021759616459)) ;
#78672=CARTESIAN_POINT('Ctrl Pts',(-2.14635157062041E-16,-1.75262906179543,
1.28982697116459)) ;
#78673=CARTESIAN_POINT('Ctrl Pts',(0.725962727204902,-1.75262906179543,
1.33943634616459)) ;
#78674=CARTESIAN_POINT('Ctrl Pts',(1.23929589450017,-1.23929589450017,1.38904572116459)) ;
#78675=CARTESIAN_POINT('Ctrl Pts',(1.75262906179543,-0.725962727204903,
1.43865509616459)) ;
#78676=CARTESIAN_POINT('Ctrl Pts',(1.75262906179543,-3.21952735593061E-16,
1.48826447116459)) ;
#78677=CARTESIAN_POINT('Ctrl Pts',(1.75262906179543,0.725962727204903,1.53787384616459)) ;
#78678=CARTESIAN_POINT('Ctrl Pts',(1.23929589450017,1.23929589450017,1.58748322116459)) ;
#78679=CARTESIAN_POINT('Ctrl Pts',(0.725962727204903,1.75262906179543,1.63709259616459)) ;
#78680=CARTESIAN_POINT('Ctrl Pts',(0.,1.75262906179543,1.68670197116459)) ;
#78681=CARTESIAN_POINT('Ctrl Pts',(-0.725962727204902,1.75262906179543,
1.73631134616459)) ;
#78682=CARTESIAN_POINT('Ctrl Pts',(-1.23929589450017,1.23929589450017,1.78592072116459)) ;
#78683=CARTESIAN_POINT('Ctrl Pts',(-1.75262906179543,0.725962727204902,
1.83553009616459)) ;
#78684=CARTESIAN_POINT('Ctrl Pts',(-1.75262906179543,1.0731757853102E-16,
1.88513947116459)) ;
#78685=CARTESIAN_POINT('Ctrl Pts',(-1.75262906179543,-0.725962727204902,
1.93474884616459)) ;
#78686=CARTESIAN_POINT('Ctrl Pts',(-1.23929589450017,-1.23929589450017,
1.98435822116459)) ;
#78687=CARTESIAN_POINT('Ctrl Pts',(-0.725962727204902,-1.75262906179543,
2.03396759616459)) ;
#78688=CARTESIAN_POINT('Ctrl Pts',(-2.14635157062041E-16,-1.75262906179543,
2.08357697116459)) ;
#78689=CARTESIAN_POINT('Ctrl Pts',(0.725962727204902,-1.75262906179543,
2.13318634616459)) ;
#78690=CARTESIAN_POINT('Ctrl Pts',(1.23929589450017,-1.23929589450017,2.18279572116459)) ;
#78691=CARTESIAN_POINT('Ctrl Pts',(1.75262906179543,-0.725962727204903,
2.23240509616459)) ;
#78692=CARTESIAN_POINT('Ctrl Pts',(1.75262906179543,-3.21952735593061E-16,
2.28201447116459)) ;
#78693=CARTESIAN_POINT('Ctrl Pts',(1.75262906179543,0.725962727204903,2.33162384616459)) ;
#78694=CARTESIAN_POINT('Ctrl Pts',(1.23929589450017,1.23929589450017,2.38123322116459)) ;
#78695=CARTESIAN_POINT('Ctrl Pts',(0.725962727204903,1.75262906179543,2.43084259616459)) ;
#78696=CARTESIAN_POINT('Ctrl Pts',(0.,1.75262906179543,2.48045197116459)) ;
#78697=CARTESIAN_POINT('Ctrl Pts',(-0.725962727204902,1.75262906179543,
2.53006134616459)) ;
#78698=CARTESIAN_POINT('Ctrl Pts',(-1.23929589450017,1.23929589450017,2.57967072116459)) ;
#78699=CARTESIAN_POINT('Ctrl Pts',(-1.75262906179543,0.725962727204902,
2.62928009616459)) ;
#78700=CARTESIAN_POINT('Ctrl Pts',(-1.75262906179543,1.0731757853102E-16,
2.67888947116459)) ;
#78701=CARTESIAN_POINT('Ctrl Pts',(-1.75262906179543,-0.725962727204902,
2.72849884616459)) ;
#78702=CARTESIAN_POINT('Ctrl Pts',(-1.23929589450017,-1.23929589450017,
2.77810822116459)) ;
#78703=CARTESIAN_POINT('Ctrl Pts',(-0.725962727204902,-1.75262906179543,
2.82771759616459)) ;
#78704=CARTESIAN_POINT('Ctrl Pts',(-2.14635157062041E-16,-1.75262906179543,
2.87732697116459)) ;
#78705=CARTESIAN_POINT('Ctrl Pts',(0.725962727204902,-1.75262906179543,
2.92693634616458)) ;
#78706=CARTESIAN_POINT('Ctrl Pts',(1.23929589450017,-1.23929589450017,2.97654572116459)) ;
#78707=CARTESIAN_POINT('Ctrl Pts',(1.75262906179543,-0.725962727204903,
3.02615509616459)) ;
#78708=CARTESIAN_POINT('Ctrl Pts',(1.75262906179543,-3.21952735593061E-16,
3.07576447116459)) ;
#78709=CARTESIAN_POINT('Ctrl Pts',(1.75262906179543,0.725962727204903,3.12537384616459)) ;
#78710=CARTESIAN_POINT('Ctrl Pts',(1.23929589450017,1.23929589450017,3.17498322116459)) ;
#78711=CARTESIAN_POINT('Ctrl Pts',(0.725962727204903,1.75262906179543,3.22459259616459)) ;
#78712=CARTESIAN_POINT('Ctrl Pts',(0.,1.75262906179543,3.27420197116459)) ;
#78713=CARTESIAN_POINT('Ctrl Pts',(-0.725962727204902,1.75262906179543,
3.32381134616459)) ;
#78714=CARTESIAN_POINT('Ctrl Pts',(-1.23929589450017,1.23929589450017,3.37342072116459)) ;
#78715=CARTESIAN_POINT('Ctrl Pts',(-1.75262906179543,0.725962727204902,
3.42303009616459)) ;
#78716=CARTESIAN_POINT('Ctrl Pts',(-1.75262906179543,1.0731757853102E-16,
3.47263947116459)) ;
#78717=CARTESIAN_POINT('Ctrl Pts',(-1.75262906179543,-0.725962727204902,
3.52224884616459)) ;
#78718=CARTESIAN_POINT('Ctrl Pts',(-1.23929589450017,-1.23929589450017,
3.57185822116459)) ;
#78719=CARTESIAN_POINT('Ctrl Pts',(-0.725962727204902,-1.75262906179543,
3.62146759616459)) ;
#78720=CARTESIAN_POINT('Ctrl Pts',(-2.14635157062041E-16,-1.75262906179543,
3.67107697116459)) ;
#78721=CARTESIAN_POINT('Ctrl Pts',(0.725962727204902,-1.75262906179543,
3.72068634616459)) ;
#78722=CARTESIAN_POINT('Ctrl Pts',(1.23929589450017,-1.23929589450017,3.77029572116459)) ;
#78723=CARTESIAN_POINT('Ctrl Pts',(1.75262906179543,-0.725962727204903,
3.81990509616459)) ;
#78724=CARTESIAN_POINT('Ctrl Pts',(1.75262906179543,-3.21952735593061E-16,
3.86951447116459)) ;
#78725=CARTESIAN_POINT('Ctrl Pts',(1.75262906179543,0.725962727204903,3.91912384616459)) ;
#78726=CARTESIAN_POINT('Ctrl Pts',(1.23929589450017,1.23929589450017,3.96873322116459)) ;
#78727=CARTESIAN_POINT('Ctrl Pts',(0.725962727204903,1.75262906179543,4.01834259616459)) ;
#78728=CARTESIAN_POINT('Ctrl Pts',(0.,1.75262906179543,4.06795197116459)) ;
#78729=CARTESIAN_POINT('Ctrl Pts',(-0.725962727204902,1.75262906179543,
4.11756134616459)) ;
#78730=CARTESIAN_POINT('Ctrl Pts',(-1.23929589450017,1.23929589450017,4.16717072116459)) ;
#78731=CARTESIAN_POINT('Ctrl Pts',(-1.75262906179543,0.725962727204902,
4.21678009616459)) ;
#78732=CARTESIAN_POINT('Ctrl Pts',(-1.75262906179543,1.0731757853102E-16,
4.26638947116459)) ;
#78733=CARTESIAN_POINT('Ctrl Pts',(-1.75262906179543,-0.725962727204902,
4.31599884616459)) ;
#78734=CARTESIAN_POINT('Ctrl Pts',(-1.23929589450017,-1.23929589450017,
4.36560822116459)) ;
#78735=CARTESIAN_POINT('Ctrl Pts',(-0.725962727204902,-1.75262906179543,
4.41521759616459)) ;
#78736=CARTESIAN_POINT('Ctrl Pts',(-2.14635157062041E-16,-1.75262906179543,
4.46482697116459)) ;
#78737=CARTESIAN_POINT('Ctrl Pts',(0.725962727204902,-1.75262906179543,
4.51443634616459)) ;
#78738=CARTESIAN_POINT('Ctrl Pts',(1.23929589450017,-1.23929589450017,4.56404572116459)) ;
#78739=CARTESIAN_POINT('Ctrl Pts',(1.75262906179543,-0.725962727204903,
4.61365509616459)) ;
#78740=CARTESIAN_POINT('Ctrl Pts',(1.75262906179543,-3.21952735593061E-16,
4.66326447116459)) ;
#78741=CARTESIAN_POINT('Ctrl Pts',(1.75262906179543,0.725962727204903,4.71287384616459)) ;
#78742=CARTESIAN_POINT('Ctrl Pts',(1.23929589450017,1.23929589450017,4.76248322116459)) ;
#78743=CARTESIAN_POINT('Ctrl Pts',(0.725962727204903,1.75262906179543,4.81209259616459)) ;
#78744=CARTESIAN_POINT('Ctrl Pts',(0.,1.75262906179543,4.86170197116459)) ;
#78745=CARTESIAN_POINT('Ctrl Pts',(-0.725962727204902,1.75262906179543,
4.91131134616459)) ;
#78746=CARTESIAN_POINT('Ctrl Pts',(-1.23929589450017,1.23929589450017,4.96092072116459)) ;
#78747=CARTESIAN_POINT('Ctrl Pts',(-1.75262906179543,0.725962727204902,
5.01053009616459)) ;
#78748=CARTESIAN_POINT('Ctrl Pts',(-1.75262906179543,1.0731757853102E-16,
5.06013947116459)) ;
#78749=CARTESIAN_POINT('Ctrl Pts',(-1.75262906179543,-0.725962727204902,
5.10974884616459)) ;
#78750=CARTESIAN_POINT('Ctrl Pts',(-1.23929589450017,-1.23929589450017,
5.15935822116457)) ;
#78751=CARTESIAN_POINT('Ctrl Pts',(-0.725962727204902,-1.75262906179543,
5.20896759616459)) ;
#78752=CARTESIAN_POINT('Ctrl Pts',(-2.14635157062041E-16,-1.75262906179543,
5.25857697116458)) ;
#78753=CARTESIAN_POINT('Ctrl Pts',(0.725962727204902,-1.75262906179543,
5.30818634616459)) ;
#78754=CARTESIAN_POINT('Ctrl Pts',(1.23929589450017,-1.23929589450017,5.35779572116459)) ;
#78755=CARTESIAN_POINT('Ctrl Pts',(1.75262906179543,-0.725962727204903,
5.40740509616459)) ;
#78756=CARTESIAN_POINT('Ctrl Pts',(1.75262906179543,-3.21952735593061E-16,
5.45701447116459)) ;
#78757=CARTESIAN_POINT('Ctrl Pts',(1.75262906179543,0.725962727204903,5.50662384616459)) ;
#78758=CARTESIAN_POINT('Ctrl Pts',(1.23929589450017,1.23929589450017,5.55623322116459)) ;
#78759=CARTESIAN_POINT('Ctrl Pts',(0.725962727204903,1.75262906179543,5.60584259616459)) ;
#78760=CARTESIAN_POINT('Ctrl Pts',(0.,1.75262906179543,5.65545197116459)) ;
#78761=CARTESIAN_POINT('Ctrl Pts',(-0.725962727204902,1.75262906179543,
5.70506134616459)) ;
#78762=CARTESIAN_POINT('Ctrl Pts',(-1.23929589450017,1.23929589450017,5.75467072116458)) ;
#78763=CARTESIAN_POINT('Ctrl Pts',(-1.75262906179543,0.725962727204902,
5.80428009616459)) ;
#78764=CARTESIAN_POINT('Ctrl Pts',(-1.75262906179543,1.0731757853102E-16,
5.85388947116459)) ;
#78765=CARTESIAN_POINT('Ctrl Pts',(-1.75262906179543,-0.725962727204902,
5.90349884616459)) ;
#78766=CARTESIAN_POINT('Ctrl Pts',(-1.23929589450017,-1.23929589450017,
5.95310822116459)) ;
#78767=CARTESIAN_POINT('Ctrl Pts',(-0.725962727204902,-1.75262906179543,
6.00271759616459)) ;
#78768=CARTESIAN_POINT('Ctrl Pts',(-2.14635157062041E-16,-1.75262906179543,
6.05232697116459)) ;
#78769=CARTESIAN_POINT('Ctrl Pts',(0.725962727204902,-1.75262906179543,
6.10193634616459)) ;
#78770=CARTESIAN_POINT('Ctrl Pts',(1.23929589450017,-1.23929589450017,6.15154572116459)) ;
#78771=CARTESIAN_POINT('Ctrl Pts',(1.75262906179543,-0.725962727204903,
6.20115509616459)) ;
#78772=CARTESIAN_POINT('Ctrl Pts',(1.75262906179543,-3.21952735593061E-16,
6.25076447116458)) ;
#78773=CARTESIAN_POINT('Ctrl Pts',(1.75262906179543,0.725962727204903,6.30037384616459)) ;
#78774=CARTESIAN_POINT('Ctrl Pts',(1.23929589450017,1.23929589450017,6.34998322116458)) ;
#78775=CARTESIAN_POINT('Ctrl Pts',(0.725962727204903,1.75262906179543,6.39959259616457)) ;
#78776=CARTESIAN_POINT('Ctrl Pts',(0.,1.75262906179543,6.44920197116459)) ;
#86291=UNCERTAINTY_MEASURE_WITH_UNIT(LENGTH_MEASURE(0.01),#86331,
'DISTANCE_ACCURACY_VALUE',
'Maximum model space distance between geometric entities at asserted c
onnectivities') ;
#86304=UNCERTAINTY_MEASURE_WITH_UNIT(LENGTH_MEASURE(0.01),#86331,
'DISTANCE_ACCURACY_VALUE',
'Maximum model space distance between geometric entities at asserted c
onnectivities') ;
#86317=(
GEOMETRIC_REPRESENTATION_CONTEXT(3)
GLOBAL_UNCERTAINTY_ASSIGNED_CONTEXT((#86291))
GLOBAL_UNIT_ASSIGNED_CONTEXT((#86331,#86333,#86334))
REPRESENTATION_CONTEXT('','3D')
) ;
#86330=(
GEOMETRIC_REPRESENTATION_CONTEXT(3)
GLOBAL_UNCERTAINTY_ASSIGNED_CONTEXT((#86304))
GLOBAL_UNIT_ASSIGNED_CONTEXT((#86331,#86333,#86334))
REPRESENTATION_CONTEXT('','3D')
) ;
#86331=(
LENGTH_UNIT()
NAMED_UNIT(*)
SI_UNIT(.MILLI.,.METRE.)
) ;
#86333=(
NAMED_UNIT(*)
PLANE_ANGLE_UNIT()
SI_UNIT($,.RADIAN.)
) ;
#86334=(
NAMED_UNIT(*)
SI_UNIT($,.STERADIAN.)
SOLID_ANGLE_UNIT()
) ;
#86347=SHAPE_DEFINITION_REPRESENTATION(#86387,#86463) ;
#86387=PRODUCT_DEFINITION_SHAPE('',$,#86489) ;
#86463=SHAPE_REPRESENTATION('',(#35475),#86317) ;
#86476=PRODUCT_DEFINITION_CONTEXT('part definition',#86553,'design') ;
#86489=PRODUCT_DEFINITION('Pan_Head_Screw','Pan_Head_Screw',#86514,#86476) ;
#86514=PRODUCT_DEFINITION_FORMATION('',$,#86567) ;
#86553=APPLICATION_CONTEXT(
'Core Data for Automotive Mechanical Design Process') ;
#86554=PRODUCT_CONTEXT('part definition',#86553,'mechanical') ;
#86567=PRODUCT('Pan_Head_Screw','Pan_Head_Screw',$,(#86554)) ;
#86582=PRESENTATION_STYLE_ASSIGNMENT((#86587)) ;
#86587=SURFACE_STYLE_USAGE(.BOTH.,#86592) ;
#86592=SURFACE_SIDE_STYLE('',(#86597)) ;
#86597=SURFACE_STYLE_FILL_AREA(#86602) ;
#86602=FILL_AREA_STYLE('Opaque(203,203,203)',(#86607)) ;
#86607=FILL_AREA_STYLE_COLOUR('Opaque(203,203,203)',#86612) ;
#86612=COLOUR_RGB('Opaque(203,203,203)', 0.66274510, 0.83137255, 0.94901961) ;
ENDSEC;
END-ISO-10303-21;
